ISO-10303-21;
HEADER;
FILE_DESCRIPTION (('STEP AP214'),
    '1' );
FILE_NAME ('Handle.step',
    '2026-10-23T18:01:19',
    ( '' ),
    ( '' ),
    'SwSTEP 2.0',
    'SolidWorks 2025',
    '' );
FILE_SCHEMA (( 'AUTOMOTIVE_DESIGN' ));
ENDSEC;

DATA;
#2=CARTESIAN_POINT ( 'NONE',  ( 0.6742552310713171293, -0.4178340986603278351, 0.4797493044159374387 ) ) ;
#5=ORIENTED_EDGE ( 'NONE', *, *, #15122, .F. ) ;
#14=CARTESIAN_POINT ( 'NONE',  ( 2.184227569363842658, 0.01449120636726281344, -0.4691493281163300333 ) ) ;
#15=DIRECTION ( 'NONE',  ( 0.01412288512831213171, -3.675428035873182550E-19, -0.9999002670844991947 ) ) ;
#20=EDGE_LOOP ( 'NONE', ( #12977, #13926, #80, #12330, #3550, #1195, #10646, #7919 ) ) ;
#21=CARTESIAN_POINT ( 'NONE',  ( 1.014389565038390506, -0.4429482523290907969, -0.3623444146133236177 ) ) ;
#22=EDGE_LOOP ( 'NONE', ( #257, #9527, #1751, #1680 ) ) ;
#25=CARTESIAN_POINT ( 'NONE',  ( 0.9160226681002169302, -0.4626215099191109403, -0.4483450520235250925 ) ) ;
#26=CARTESIAN_POINT ( 'NONE',  ( 0.7513246802501661881, 0.000000000000000000, -0.4293820849162031661 ) ) ;
#34=VERTEX_POINT ( 'NONE', #12922 ) ;
#36=EDGE_LOOP ( 'NONE', ( #14330, #7722, #9947, #11329, #1823, #9061, #6511, #9617 ) ) ;
#41=VECTOR ( 'NONE', #2622, 39.37007874015748143 ) ;
#54=VECTOR ( 'NONE', #5461, 39.37007874015748143 ) ;
#64=CARTESIAN_POINT ( 'NONE',  ( 3.601417382415921686, 1.056999999999999718, -0.3891265382754440227 ) ) ;
#68=CARTESIAN_POINT ( 'NONE',  ( 0.6601485485260571995, -0.3723516483516483011, -0.5137583810202324131 ) ) ;
#70=CARTESIAN_POINT ( 'NONE',  ( 0.9652173913043479159, -0.4829999999999998739, -0.3379636412230419551 ) ) ;
#72=ORIENTED_EDGE ( 'NONE', *, *, #13429, .F. ) ;
#74=CARTESIAN_POINT ( 'NONE',  ( 0.6773748815706875925, -0.3764079396444214298, 0.4904325581699060521 ) ) ;
#80=ORIENTED_EDGE ( 'NONE', *, *, #10085, .T. ) ;
#86=DIRECTION ( 'NONE',  ( 0.000000000000000000, 0.000000000000000000, 1.000000000000000000 ) ) ;
#97=CARTESIAN_POINT ( 'NONE',  ( 0.7020471549603389816, -0.02897145875702579823, -0.4816513823572634578 ) ) ;
#103=CARTESIAN_POINT ( 'NONE',  ( 3.390179639970223313, 0.6913388717410868800, -0.3921396980529558429 ) ) ;
#105=VECTOR ( 'NONE', #3673, 39.37007874015748854 ) ;
#113=CARTESIAN_POINT ( 'NONE',  ( 0.8418300605894719624, -0.4829999999999998739, -0.3276580719765713745 ) ) ;
#128=DIRECTION ( 'NONE',  ( 0.7071067811865459074, -0.7071067811865492381, 0.000000000000000000 ) ) ;
#148=CARTESIAN_POINT ( 'NONE',  ( 0.6894183887957248125, -0.4431162156558585696, 0.4464953827605262493 ) ) ;
#162=FACE_OUTER_BOUND ( 'NONE', #5866, .T. ) ;
#163=TOROIDAL_SURFACE ( 'NONE', #642, 0.3203340137431718859, 0.05999999999999999778 ) ;
#173=CARTESIAN_POINT ( 'NONE',  ( -0.3725000000000000533, -0.6590000000000000302, 0.3724999999999999423 ) ) ;
#175=CARTESIAN_POINT ( 'NONE',  ( 0.8848438321385330152, -0.4627371489994540066, -0.4487466038575088079 ) ) ;
#176=DIRECTION ( 'NONE',  ( 0.01412288512831128343, 0.000000000000000000, 0.9999002670844990837 ) ) ;
#181=CARTESIAN_POINT ( 'NONE',  ( 1.397260334976607732, 0.007251848866960360247, 0.4201477693899102750 ) ) ;
#184=VERTEX_POINT ( 'NONE', #11856 ) ;
#196=PLANE ( 'NONE',  #6331 ) ;
#197=AXIS2_PLACEMENT_3D ( 'NONE', #7203, #5970, #10632 ) ;
#202=AXIS2_PLACEMENT_3D ( 'NONE', #13035, #253, #10606 ) ;
#217=ORIENTED_EDGE ( 'NONE', *, *, #5293, .F. ) ;
#220=CARTESIAN_POINT ( 'NONE',  ( 3.601417382415921686, 1.056999999999999718, 0.5000000000000000000 ) ) ;
#221=DIRECTION ( 'NONE',  ( 0.01412288512831213171, -3.675428035873182550E-19, 0.9999002670844991947 ) ) ;
#224=CARTESIAN_POINT ( 'NONE',  ( 0.4425000000000003375, 0.2159999999999999420, 0.3724999999999999423 ) ) ;
#236=EDGE_CURVE ( 'NONE', #4318, #1348, #8143, .T. ) ;
#238=CARTESIAN_POINT ( 'NONE',  ( 1.000847373107697891, -0.4430000000000000049, 0.4858637376679703634 ) ) ;
#243=AXIS2_PLACEMENT_3D ( 'NONE', #9319, #1107, #15044 ) ;
#247=CARTESIAN_POINT ( 'NONE',  ( 1.012992808803494293, -0.4429593110677563228, -0.3529645107950314387 ) ) ;
#249=CARTESIAN_POINT ( 'NONE',  ( 3.602264755523620465, 0.9969999999999996643, 0.4491205543005138412 ) ) ;
#251=VERTEX_POINT ( 'NONE', #2745 ) ;
#253=DIRECTION ( 'NONE',  ( 1.365923996832131609E-16, -1.000000000000000000, -0.000000000000000000 ) ) ;
#257=ORIENTED_EDGE ( 'NONE', *, *, #5350, .T. ) ;
#259=VERTEX_POINT ( 'NONE', #10708 ) ;
#262=CARTESIAN_POINT ( 'NONE',  ( 0.7058998964907862161, -0.05999999999999994227, -0.4900296624789436950 ) ) ;
#265=CARTESIAN_POINT ( 'NONE',  ( 0.6601485485260571995, -0.07064835164835162051, 0.5137583810202324131 ) ) ;
#271=PRODUCT_DEFINITION_SHAPE ( 'NONE', 'NONE',  #3615 ) ;
#273=CARTESIAN_POINT ( 'NONE',  ( 0.8490493353346898475, -0.4471313898566136036, -0.4310079353635160593 ) ) ;
#276=DIRECTION ( 'NONE',  ( -0.9743309173630050335, 0.2251205531944274196, 1.138269997360108984E-15 ) ) ;
#278=ADVANCED_FACE ( 'NONE', ( #14215 ), #6778, .F. ) ;
#284=CARTESIAN_POINT ( 'NONE',  ( 0.8999999999999999112, -0.6230000000000016636, -0.3750000000000000555 ) ) ;
#286=CARTESIAN_POINT ( 'NONE',  ( 3.250637184708970562, 0.6799532182389177448, 0.4540870454136761714 ) ) ;
#288=LINE ( 'NONE', #2465, #664 ) ;
#290=CARTESIAN_POINT ( 'NONE',  ( 0.7206835787589852549, -0.006955211921962108426, 0.4581197915133168319 ) ) ;
#291=DIRECTION ( 'NONE',  ( -0.7071067811865600072, -0.7071067811865350272, 1.170732267570241832E-16 ) ) ;
#297=CARTESIAN_POINT ( 'NONE',  ( 7.623651669702752511E-17, -0.6589999999999998082, 0.000000000000000000 ) ) ;
#298=EDGE_LOOP ( 'NONE', ( #11252, #3224, #10809, #13371 ) ) ;
#310=ORIENTED_EDGE ( 'NONE', *, *, #14681, .T. ) ;
#311=ORIENTED_EDGE ( 'NONE', *, *, #2045, .F. ) ;
#313=CYLINDRICAL_SURFACE ( 'NONE', #4057, 0.03999999999999998002 ) ;
#319=CARTESIAN_POINT ( 'NONE',  ( 1.613287804444627715, 0.05773177243535584924, 0.4772134490897159131 ) ) ;
#340=DIRECTION ( 'NONE',  ( -1.000000000000000000, 0.000000000000000000, 0.000000000000000000 ) ) ;
#354=ORIENTED_EDGE ( 'NONE', *, *, #6727, .F. ) ;
#357=CARTESIAN_POINT ( 'NONE',  ( 1.000000000000000222, -0.3829999999999998961, -0.4258697216429003785 ) ) ;
#359=CARTESIAN_POINT ( 'NONE',  ( 3.601417382415921686, 0.9969999999999999973, 0.3891265382754439117 ) ) ;
#362=AXIS2_PLACEMENT_3D ( 'NONE', #8874, #4935, #7723 ) ;
#364=EDGE_CURVE ( 'NONE', #2708, #7869, #8176, .T. ) ;
#366=CARTESIAN_POINT ( 'NONE',  ( 0.6844575745811053435, -0.004403083989539873129, 0.4560057122456970258 ) ) ;
#368=ORIENTED_EDGE ( 'NONE', *, *, #14078, .F. ) ;
#373=CIRCLE ( 'NONE', #2836, 0.05999999999999996309 ) ;
#377=EDGE_LOOP ( 'NONE', ( #1901, #13992, #9857, #660 ) ) ;
#378=CARTESIAN_POINT ( 'NONE',  ( 1.552356239822776596, 2.176428591712472865E-16, 0.4178403161916762754 ) ) ;
#393=CARTESIAN_POINT ( 'NONE',  ( 8.792093969802149189, 0.8799778768672790186, 6.829619984160658046E-17 ) ) ;
#396=DIRECTION ( 'NONE',  ( -1.365923996832131609E-16, 1.000000000000000000, -0.000000000000000000 ) ) ;
#397=CARTESIAN_POINT ( 'NONE',  ( 8.849999999999999645, 0.9399413264884247665, 6.829619984160658046E-17 ) ) ;
#403=ORIENTED_EDGE ( 'NONE', *, *, #4180, .F. ) ;
#413=DIRECTION ( 'NONE',  ( 0.000000000000000000, 0.000000000000000000, 1.000000000000000000 ) ) ;
#416=ADVANCED_FACE ( 'NONE', ( #11763 ), #6950, .T. ) ;
#421=CARTESIAN_POINT ( 'NONE',  ( 0.8032009730227706035, -0.4429999999999999494, -0.4342979540647063930 ) ) ;
#431=ORIENTED_EDGE ( 'NONE', *, *, #11597, .T. ) ;
#436=VERTEX_POINT ( 'NONE', #1191 ) ;
#441=CARTESIAN_POINT ( 'NONE',  ( 0.6766938413713005085, 0.03160638642086351091, 0.4478646436804253339 ) ) ;
#442=VECTOR ( 'NONE', #5367, 39.37007874015748143 ) ;
#443=LINE ( 'NONE', #1679, #13645 ) ;
#453=ORIENTED_EDGE ( 'NONE', *, *, #4195, .F. ) ;
#456=ORIENTED_EDGE ( 'NONE', *, *, #5293, .T. ) ;
#463=CARTESIAN_POINT ( 'NONE',  ( 1.936801488370565982, 0.2309360081137091791, -0.4726440467746176877 ) ) ;
#465=ORIENTED_EDGE ( 'NONE', *, *, #5796, .T. ) ;
#466=ORIENTED_EDGE ( 'NONE', *, *, #11100, .T. ) ;
#469=FACE_OUTER_BOUND ( 'NONE', #14095, .T. ) ;
#478=ORIENTED_EDGE ( 'NONE', *, *, #3162, .F. ) ;
#479=TOROIDAL_SURFACE ( 'NONE', #243, 0.7057575716915831521, 0.04000000000000000083 ) ;
#481=ADVANCED_FACE ( 'NONE', ( #9320 ), #2760, .F. ) ;
#483=CARTESIAN_POINT ( 'NONE',  ( 1.863568193433660758, 0.06187774891384346942, -0.4736784153469822400 ) ) ;
#485=CARTESIAN_POINT ( 'NONE',  ( 3.470516203623992713, 1.056999999999999718, 0.3909199583802897005 ) ) ;
#486=ORIENTED_EDGE ( 'NONE', *, *, #13237, .F. ) ;
#487=( BOUNDED_CURVE ( )  B_SPLINE_CURVE ( 3, ( #249, #9614, #6464, #3179 ),
 .UNSPECIFIED., .F., .T. ) 
 B_SPLINE_CURVE_WITH_KNOTS ( ( 4, 4 ),
 ( 1.570796326794896558, 2.356194490192347057 ),
 .UNSPECIFIED. ) 
 CURVE ( )  GEOMETRIC_REPRESENTATION_ITEM ( )  RATIONAL_B_SPLINE_CURVE ( ( 1.000000000000000000, 0.9492530216741907889, 0.9492530216741907889, 1.000000000000000000 ) ) 
 REPRESENTATION_ITEM ( '' )  );
#490=DIRECTION ( 'NONE',  ( -1.000000000000000000, -1.578435611247398256E-16, 0.000000000000000000 ) ) ;
#498=VERTEX_POINT ( 'NONE', #4806 ) ;
#502=DIRECTION ( 'NONE',  ( 1.000000000000000000, 0.000000000000000000, 0.000000000000000000 ) ) ;
#509=EDGE_LOOP ( 'NONE', ( #10431, #1646, #3690, #10294 ) ) ;
#513=ADVANCED_FACE ( 'NONE', ( #3662 ), #8439, .T. ) ;
#515=DIRECTION ( 'NONE',  ( 1.000000000000000000, 0.000000000000000000, 0.000000000000000000 ) ) ;
#528=CARTESIAN_POINT ( 'NONE',  ( 1.831696981322115780, 0.1157067236523833115, -0.4136843993219123106 ) ) ;
#535=ORIENTED_EDGE ( 'NONE', *, *, #1965, .T. ) ;
#538=CARTESIAN_POINT ( 'NONE',  ( 8.849999999999999645, 0.9399413264884969310, -0.04934655444149117082 ) ) ;
#543=CARTESIAN_POINT ( 'NONE',  ( 8.849999999999999645, 0.9399413264884247665, -0.2203075555454639678 ) ) ;
#547=DIRECTION ( 'NONE',  ( -1.000000000000000000, 0.000000000000000000, 1.655665450705613915E-16 ) ) ;
#549=CLOSED_SHELL ( 'NONE', ( #5488, #481, #7292, #11440, #11908, #9531, #3714, #2619, #5887, #8436, #6105, #1471, #8156, #11332, #12780, #2405, #7263, #14183, #6009, #11214, #11092, #1051, #416, #12347, #10729, #6027, #11234, #7644, #7915, #5914, #9798, #14421, #14956, #1945, #6230, #12029, #9162, #10430, #15014, #657, #3349, #12038, #13659, #9739, #6270, #8151, #13249, #11391, #1877, #5212, #513, #12775, #1170, #13088, #4368, #635, #8400, #12740, #13598, #8336, #7884, #9967, #8541, #15045, #9982, #13065, #14395, #8709, #14079, #13106, #14372, #2783, #2220, #12247, #8585, #5823, #14354, #7669, #4557, #4229, #14131, #8678, #8076, #2011, #13221, #15022, #8482, #2314, #278, #1941, #10668 ) ) ;
#550=EDGE_LOOP ( 'NONE', ( #3522, #12359, #5503, #368 ) ) ;
#553=DIRECTION ( 'NONE',  ( -1.000000000000000000, -1.365923996832131609E-16, 0.000000000000000000 ) ) ;
#556=CARTESIAN_POINT ( 'NONE',  ( 2.956986065683078202, 0.9548522091760921482, 0.3979556114002301137 ) ) ;
#565=CARTESIAN_POINT ( 'NONE',  ( 0.9125303617078899254, -0.4616528667627542992, -0.4492488068439366988 ) ) ;
#568=CARTESIAN_POINT ( 'NONE',  ( 0.7067472695984848841, -0.3830000000000000071, 0.5500236785040136800 ) ) ;
#574=( BOUNDED_CURVE ( )  B_SPLINE_CURVE ( 3, ( #13959, #7028, #11687, #3578 ),
 .UNSPECIFIED., .F., .F. ) 
 B_SPLINE_CURVE_WITH_KNOTS ( ( 4, 4 ),
 ( 3.926990816987246724, 4.712388980384689674 ),
 .UNSPECIFIED. ) 
 CURVE ( )  GEOMETRIC_REPRESENTATION_ITEM ( )  RATIONAL_B_SPLINE_CURVE ( ( 1.000000000000000000, 0.9492530216741918991, 0.9492530216741918991, 1.000000000000000000 ) ) 
 REPRESENTATION_ITEM ( '' )  );
#576=CARTESIAN_POINT ( 'NONE',  ( 0.6766651500320096657, 0.03157991788063375938, 0.4479228816209581687 ) ) ;
#579=CYLINDRICAL_SURFACE ( 'NONE', #362, 0.06000000000000021982 ) ;
#581=VECTOR ( 'NONE', #5660, 39.37007874015748143 ) ;
#587=VERTEX_POINT ( 'NONE', #15009 ) ;
#601=EDGE_CURVE ( 'NONE', #8372, #9653, #8938, .T. ) ;
#602=EDGE_CURVE ( 'NONE', #10522, #4605, #13769, .T. ) ;
#604=CARTESIAN_POINT ( 'NONE',  ( 1.261796151055322168, -0.4301078242393397977, 0.4222829664659954463 ) ) ;
#607=CARTESIAN_POINT ( 'NONE',  ( 1.003096136995460075, -0.4429976034824905651, -0.4258273028168328977 ) ) ;
#608=AXIS2_PLACEMENT_3D ( 'NONE', #2450, #9183, #10407 ) ;
#611=CARTESIAN_POINT ( 'NONE',  ( 1.250847373107696114, 9.390727478220904197E-17, -0.4823326642216427818 ) ) ;
#615=ORIENTED_EDGE ( 'NONE', *, *, #5487, .T. ) ;
#619=CARTESIAN_POINT ( 'NONE',  ( 8.775135155112147700, 0.9377394161891228208, -0.2318982201004599064 ) ) ;
#622=CARTESIAN_POINT ( 'NONE',  ( 0.6757896753473673357, -0.3817456040190621014, -0.4909021876970636744 ) ) ;
#627=EDGE_CURVE ( 'NONE', #5452, #9898, #761, .T. ) ;
#633=FACE_OUTER_BOUND ( 'NONE', #11405, .T. ) ;
#635=ADVANCED_FACE ( 'NONE', ( #4537 ), #692, .T. ) ;
#637=CARTESIAN_POINT ( 'NONE',  ( 2.742551415177972185, 0.8007359432430831703, 0.4612633980907066000 ) ) ;
#642=AXIS2_PLACEMENT_3D ( 'NONE', #1430, #11848, #4665 ) ;
#649=ORIENTED_EDGE ( 'NONE', *, *, #7956, .F. ) ;
#656=DIRECTION ( 'NONE',  ( -0.9999002670844991947, -0.000000000000000000, -0.01412288512831128343 ) ) ;
#657=ADVANCED_FACE ( 'NONE', ( #1153 ), #3465, .T. ) ;
#660=ORIENTED_EDGE ( 'NONE', *, *, #12679, .F. ) ;
#664=VECTOR ( 'NONE', #2691, 39.37007874015748854 ) ;
#682=AXIS2_PLACEMENT_3D ( 'NONE', #12165, #221, #7367 ) ;
#684=VECTOR ( 'NONE', #3368, 39.37007874015748143 ) ;
#687=CARTESIAN_POINT ( 'NONE',  ( 0.9666012435391547752, -0.4437180647443542680, -0.4095160967654646877 ) ) ;
#690=CIRCLE ( 'NONE', #4881, 0.06000000000000001860 ) ;
#691=CARTESIAN_POINT ( 'NONE',  ( 0.8249999999999999556, -0.6230000000000016636, -0.3750000000000000555 ) ) ;
#692=CYLINDRICAL_SURFACE ( 'NONE', #7165, 0.06000000000000001860 ) ;
#693=CARTESIAN_POINT ( 'NONE',  ( 0.7058998964907862161, -0.3830000000000000071, -0.4900296624789436950 ) ) ;
#695=ORIENTED_EDGE ( 'NONE', *, *, #1081, .T. ) ;
#697=EDGE_CURVE ( 'NONE', #587, #10371, #13969, .T. ) ;
#701=AXIS2_PLACEMENT_3D ( 'NONE', #10499, #14927, #12704 ) ;
#706=EDGE_CURVE ( 'NONE', #9538, #13964, #2311, .T. ) ;
#708=ORIENTED_EDGE ( 'NONE', *, *, #10830, .F. ) ;
#711=ORIENTED_EDGE ( 'NONE', *, *, #8011, .F. ) ;
#718=DIRECTION ( 'NONE',  ( 0.9743309173630049225, 0.2251205531944282245, 0.000000000000000000 ) ) ;
#724=CARTESIAN_POINT ( 'NONE',  ( 0.9662251482428008131, -0.4440312122665854289, -0.4102559963803746323 ) ) ;
#732=ORIENTED_EDGE ( 'NONE', *, *, #9430, .T. ) ;
#736=FACE_OUTER_BOUND ( 'NONE', #7085, .T. ) ;
#741=CARTESIAN_POINT ( 'NONE',  ( 2.715751415184352702, 0.8549853309854710259, -0.4616419291638462208 ) ) ;
#744=ORIENTED_EDGE ( 'NONE', *, *, #2333, .F. ) ;
#748=DIRECTION ( 'NONE',  ( 0.7071067811865446862, -0.7071067811865503483, 0.000000000000000000 ) ) ;
#752=ORIENTED_EDGE ( 'NONE', *, *, #4248, .T. ) ;
#753=CYLINDRICAL_SURFACE ( 'NONE', #10833, 0.06000000000000001860 ) ;
#758=CARTESIAN_POINT ( 'NONE',  ( 1.000048944713735732, -0.4428998280398803722, -0.4293350073753850471 ) ) ;
#761=LINE ( 'NONE', #7984, #1027 ) ;
#763=ORIENTED_EDGE ( 'NONE', *, *, #3098, .T. ) ;
#766=DIRECTION ( 'NONE',  ( -0.000000000000000000, 1.000000000000000000, -0.000000000000000000 ) ) ;
#769=CARTESIAN_POINT ( 'NONE',  ( 0.6583850202313374922, -0.3799842706883578280, -0.5137832895838266856 ) ) ;
#771=AXIS2_PLACEMENT_3D ( 'NONE', #2349, #11688, #5650 ) ;
#772=CARTESIAN_POINT ( 'NONE',  ( 0.8999999999999999112, -0.4429999999999998939, -0.3750000000000000555 ) ) ;
#777=EDGE_LOOP ( 'NONE', ( #9479, #72, #11887, #9960 ) ) ;
#785=CARTESIAN_POINT ( 'NONE',  ( 0.8999999999999999112, -0.4829999999999998739, -0.3750000000000000555 ) ) ;
#790=CARTESIAN_POINT ( 'NONE',  ( 3.602264755523620465, 0.9969999999999996643, -0.4491205543005138412 ) ) ;
#792=DIRECTION ( 'NONE',  ( -0.01412288512831583534, 0.000000000000000000, 0.9999002670844989726 ) ) ;
#802=LINE ( 'NONE', #5576, #10673 ) ;
#808=CARTESIAN_POINT ( 'NONE',  ( -0.4125000000000001998, -0.6290000000000005587, -0.4125000000000000333 ) ) ;
#815=AXIS2_PLACEMENT_3D ( 'NONE', #568, #5264, #276 ) ;
#820=CARTESIAN_POINT ( 'NONE',  ( 1.000000000000000222, -0.4429999999999998939, -0.3182109165419975683 ) ) ;
#823=CARTESIAN_POINT ( 'NONE',  ( 0.7038870757886628304, -0.3873557849635640427, 0.4900580921498779996 ) ) ;
#829=CARTESIAN_POINT ( 'NONE',  ( -5.764454660286586870E-18, 0.1759999999999999065, 0.000000000000000000 ) ) ;
#837=CARTESIAN_POINT ( 'NONE',  ( 0.4425000000000002820, 0.2159999999999999420, -0.3725000000000000533 ) ) ;
#838=CARTESIAN_POINT ( 'NONE',  ( 0.8337700833007937185, -0.4835922659884503982, -0.3396222324529075687 ) ) ;
#842=CARTESIAN_POINT ( 'NONE',  ( 0.7371172985291584157, -0.4420715194279608018, -0.4420151072446013574 ) ) ;
#848=CARTESIAN_POINT ( 'NONE',  ( 0.6773748815706881476, -0.3764079396444222625, -0.4904325581699054970 ) ) ;
#851=FACE_OUTER_BOUND ( 'NONE', #20, .T. ) ;
#853=CONICAL_SURFACE ( 'NONE', #14058, 0.07000000000000047851, 0.7853981633974297383 ) ;
#862=PLANE ( 'NONE',  #8468 ) ;
#871=VECTOR ( 'NONE', #15054, 39.37007874015748143 ) ;
#879=AXIS2_PLACEMENT_3D ( 'NONE', #13795, #13568, #5559 ) ;
#895=EDGE_CURVE ( 'NONE', #15127, #2763, #9957, .T. ) ;
#897=CARTESIAN_POINT ( 'NONE',  ( 2.381934877626368241, 0.6476033094205475571, -0.4663568520109309112 ) ) ;
#898=CARTESIAN_POINT ( 'NONE',  ( 3.601417382415921686, 1.056999999999999718, -0.3891265382754440227 ) ) ;
#907=ORIENTED_EDGE ( 'NONE', *, *, #14977, .T. ) ;
#910=DIRECTION ( 'NONE',  ( -1.000000000000000000, -1.689854595570744117E-16, 0.000000000000000000 ) ) ;
#914=CIRCLE ( 'NONE', #14855, 0.05999999999999994227 ) ;
#920=CARTESIAN_POINT ( 'NONE',  ( 0.8418300605894719624, -0.4829999999999998739, -0.3276580719765713745 ) ) ;
#927=CARTESIAN_POINT ( 'NONE',  ( 1.250847373107698779, -0.05999999999999997696, 0.4823326642216426707 ) ) ;
#950=DIRECTION ( 'NONE',  ( 0.7070715176384863021, 0.7070715176384774203, 0.009986885842351498482 ) ) ;
#958=EDGE_CURVE ( 'NONE', #7795, #14642, #9107, .T. ) ;
#961=ORIENTED_EDGE ( 'NONE', *, *, #6008, .F. ) ;
#974=CARTESIAN_POINT ( 'NONE',  ( -0.7287617923574203349, -0.6590000000000000302, -0.4424999999999983391 ) ) ;
#990=CARTESIAN_POINT ( 'NONE',  ( 2.824624536279081610, 0.5882431044538637410, -0.4601041732163972386 ) ) ;
#991=( BOUNDED_SURFACE ( )  B_SPLINE_SURFACE ( 3, 2, ( 
 ( #3476, #8235, #2403 ),
 ( #7008, #10589, #2631 ),
 ( #8384, #7089, #14 ),
 ( #11964, #4704, #1316 ),
 ( #6003, #8153, #4936 ),
 ( #11745, #5773, #9455 ),
 ( #8318, #10437, #13097 ),
 ( #13020, #1163, #15097 ),
 ( #10667, #11662, #2482 ),
 ( #4861, #1240, #5859 ) ),
 .UNSPECIFIED., .F., .F., .T. ) 
 B_SPLINE_SURFACE_WITH_KNOTS ( ( 4, 2, 2, 2, 4 ),
 ( 3, 3 ),
 ( 3.926990816987246280, 4.123340357836607240, 4.319689898685967755, 4.516039439535328270, 4.712388980384689674 ),
 ( 0.000000000000000000, 1.000000000000000000 ),
 .UNSPECIFIED. ) 
 GEOMETRIC_REPRESENTATION_ITEM ( )  RATIONAL_B_SPLINE_SURFACE ( (
 ( 1.000000000000000000, 0.7106287314217404338, 1.000000000000000000),
 ( 1.000000000000000000, 0.7103988163329607586, 1.000000000000000000),
 ( 1.000000000000000000, 0.7101460984486431816, 1.000000000000000000),
 ( 1.000000000000000000, 0.7096047632039514941, 1.000000000000000000),
 ( 1.000000000000000000, 0.7093161336535294126, 1.000000000000000000),
 ( 1.000000000000000000, 0.7087139042199988026, 1.000000000000000000),
 ( 1.000000000000000000, 0.7084003186178147171, 1.000000000000000000),
 ( 1.000000000000000000, 0.7077601512495510505, 1.000000000000000000),
 ( 1.000000000000000000, 0.7074335897358576819, 1.000000000000000000),
 ( 1.000000000000000000, 0.7071067811865475727, 1.000000000000000000) ) ) 
 REPRESENTATION_ITEM ( '' )  SURFACE ( )  );
#998=CARTESIAN_POINT ( 'NONE',  ( 0.4124999999999997558, -0.6290000000000003366, -0.4125000000000000333 ) ) ;
#1003=ORIENTED_EDGE ( 'NONE', *, *, #4844, .T. ) ;
#1004=CARTESIAN_POINT ( 'NONE',  ( 8.476283996537762988, 0.8689495495877206377, -0.3203020658980470503 ) ) ;
#1005=VERTEX_POINT ( 'NONE', #820 ) ;
#1009=CIRCLE ( 'NONE', #13710, 0.05999999999999994227 ) ;
#1010=CARTESIAN_POINT ( 'NONE',  ( 0.8533815140473888228, -0.4340691947652905447, -0.4596148562493023171 ) ) ;
#1013=CARTESIAN_POINT ( 'NONE',  ( 8.783907589752271150, 0.8796920021765856079, 0.08309344507351693054 ) ) ;
#1014=SHAPE_REPRESENTATION ( 'Handle', ( #8424 ), #9874 ) ;
#1023=CARTESIAN_POINT ( 'NONE',  ( 2.088768908813758873, 0.2870784642939425146, 0.4704976142822915319 ) ) ;
#1024=VERTEX_POINT ( 'NONE', #1134 ) ;
#1025=CARTESIAN_POINT ( 'NONE',  ( -0.3725000000000002198, -0.6590000000000000302, -0.4424999999999983391 ) ) ;
#1027=VECTOR ( 'NONE', #3234, 39.37007874015748143 ) ;
#1037=VERTEX_POINT ( 'NONE', #4597 ) ;
#1044=VECTOR ( 'NONE', #4168, 39.37007874015748143 ) ;
#1046=CARTESIAN_POINT ( 'NONE',  ( 0.7017867892446607581, -0.4844395604395603239, -0.4010711782184315233 ) ) ;
#1050=CARTESIAN_POINT ( 'NONE',  ( 3.601417382415921686, -0.9430000000000002824, 0.5000000000000000000 ) ) ;
#1051=ADVANCED_FACE ( 'NONE', ( #9272 ), #11784, .F. ) ;
#1056=DIRECTION ( 'NONE',  ( 1.874307916738608820E-16, -1.000000000000000000, -0.000000000000000000 ) ) ;
#1065=EDGE_CURVE ( 'NONE', #5891, #9216, #4828, .T. ) ;
#1067=CARTESIAN_POINT ( 'NONE',  ( 2.855088541747186515, 0.5369222675350495688, -0.4596738906532820690 ) ) ;
#1069=CARTESIAN_POINT ( 'NONE',  ( 2.282850251811598064, 0.09542856769877475220, 0.4677563523755423613 ) ) ;
#1071=DIRECTION ( 'NONE',  ( -2.602462600580852055E-17, -1.000000000000000000, -4.814436796019480615E-35 ) ) ;
#1073=CARTESIAN_POINT ( 'NONE',  ( 0.7017867892446613132, -0.4844395604395603239, 0.4010711782184302465 ) ) ;
#1077=FACE_OUTER_BOUND ( 'NONE', #8580, .T. ) ;
#1080=VERTEX_POINT ( 'NONE', #13983 ) ;
#1081=EDGE_CURVE ( 'NONE', #3261, #1080, #6900, .T. ) ;
#1084=EDGE_CURVE ( 'NONE', #1606, #10100, #1432, .T. ) ;
#1088=CIRCLE ( 'NONE', #5496, 0.03999999999999998002 ) ;
#1089=VECTOR ( 'NONE', #11315, 39.37007874015748143 ) ;
#1090=EDGE_CURVE ( 'NONE', #7832, #9046, #9515, .T. ) ;
#1097=DIRECTION ( 'NONE',  ( -0.9992912762382412106, -0.03489602031262427351, 0.01411428356269048105 ) ) ;
#1101=CARTESIAN_POINT ( 'NONE',  ( 0.8410094793127153023, -0.4816416392817352565, -0.4218009027733075067 ) ) ;
#1106=CARTESIAN_POINT ( 'NONE',  ( 0.7026382878071448790, -0.05185562024730498015, -0.4896667335905589558 ) ) ;
#1107=DIRECTION ( 'NONE',  ( 0.000000000000000000, -1.000000000000000000, 0.000000000000000000 ) ) ;
#1128=DIRECTION ( 'NONE',  ( 0.01412288512831213171, -3.675428035873183031E-19, 0.9999002670844990837 ) ) ;
#1129=FACE_OUTER_BOUND ( 'NONE', #9634, .T. ) ;
#1131=LINE ( 'NONE', #974, #3161 ) ;
#1134=CARTESIAN_POINT ( 'NONE',  ( 2.045495128834867060, 0.3295048711651353268, 0.4105035982572216025 ) ) ;
#1140=DIRECTION ( 'NONE',  ( -1.365923996832131609E-16, 1.000000000000000000, -0.000000000000000000 ) ) ;
#1144=CARTESIAN_POINT ( 'NONE',  ( 0.6676154558030191755, 0.02175203226844540927, -0.4667586584590060483 ) ) ;
#1153=FACE_OUTER_BOUND ( 'NONE', #2958, .T. ) ;
#1162=DIRECTION ( 'NONE',  ( 0.9702019082525984439, 0.2422978687958614041, 1.188154661468198570E-16 ) ) ;
#1163=CARTESIAN_POINT ( 'NONE',  ( 1.262572881824740367, -0.4300086559499006200, -0.4821670496918215032 ) ) ;
#1166=AXIS2_PLACEMENT_3D ( 'NONE', #3839, #10869, #14228 ) ;
#1170=ADVANCED_FACE ( 'NONE', ( #11573 ), #7964, .F. ) ;
#1176=PLANE ( 'NONE',  #13566 ) ;
#1179=CARTESIAN_POINT ( 'NONE',  ( 0.8722377123985701752, -0.4669784293568965405, -0.4449823291402679182 ) ) ;
#1180=AXIS2_PLACEMENT_3D ( 'NONE', #1875, #14665, #413 ) ;
#1185=AXIS2_PLACEMENT_3D ( 'NONE', #12145, #10998, #490 ) ;
#1189=AXIS2_PLACEMENT_3D ( 'NONE', #8652, #10947, #11020 ) ;
#1191=CARTESIAN_POINT ( 'NONE',  ( -0.4125000000000001998, -0.6290000000000005587, -0.3725000000000000533 ) ) ;
#1195=ORIENTED_EDGE ( 'NONE', *, *, #601, .T. ) ;
#1208=CARTESIAN_POINT ( 'NONE',  ( 8.475037399843312613, 0.8689060174719044349, 0.3802960819231170908 ) ) ;
#1224=DIRECTION ( 'NONE',  ( 1.365923996832131609E-16, -1.000000000000000000, -0.000000000000000000 ) ) ;
#1230=CARTESIAN_POINT ( 'NONE',  ( 0.6601485485260575325, -0.3723516483516470243, 0.5137583810202325241 ) ) ;
#1238=ORIENTED_EDGE ( 'NONE', *, *, #12127, .F. ) ;
#1239=LINE ( 'NONE', #5927, #8683 ) ;
#1240=CARTESIAN_POINT ( 'NONE',  ( 1.000847373107695226, -0.4430000000000000049, -0.4858637376679705855 ) ) ;
#1246=EDGE_LOOP ( 'NONE', ( #2787, #5368, #4334, #7319 ) ) ;
#1247=ORIENTED_EDGE ( 'NONE', *, *, #8778, .T. ) ;
#1248=UNCERTAINTY_MEASURE_WITH_UNIT (LENGTH_MEASURE( 1.000000000000000082E-05 ), #2906, 'distance_accuracy_value', 'NONE');
#1252=CARTESIAN_POINT ( 'NONE',  ( 0.8502743344449713581, -0.4776025933964622716, -0.4315470089081906435 ) ) ;
#1254=CARTESIAN_POINT ( 'NONE',  ( 0.7058998964907862161, -0.05999999999999994227, -0.4900296624789436950 ) ) ;
#1255=ORIENTED_EDGE ( 'NONE', *, *, #7916, .T. ) ;
#1258=PLANE ( 'NONE',  #10237 ) ;
#1262=EDGE_CURVE ( 'NONE', #2201, #14331, #2840, .T. ) ;
#1269=ORIENTED_EDGE ( 'NONE', *, *, #2217, .F. ) ;
#1274=VERTEX_POINT ( 'NONE', #6369 ) ;
#1275=CARTESIAN_POINT ( 'NONE',  ( 8.474190026735612946, 1.056999999999999940, 0.3203020658980470503 ) ) ;
#1283=EDGE_CURVE ( 'NONE', #6530, #498, #12667, .T. ) ;
#1288=DIRECTION ( 'NONE',  ( 0.7071067811865612285, 0.7071067811865339170, -1.170732267570244050E-16 ) ) ;
#1299=FACE_OUTER_BOUND ( 'NONE', #7207, .T. ) ;
#1303=DIRECTION ( 'NONE',  ( 1.655665450705613915E-16, 0.000000000000000000, 1.000000000000000000 ) ) ;
#1304=CARTESIAN_POINT ( 'NONE',  ( 0.6733128806866760518, -0.4720829350095157029, 0.4545362700951272594 ) ) ;
#1309=CARTESIAN_POINT ( 'NONE',  ( 0.3724999999999997757, 0.1859999999999983611, -0.4125000000000000333 ) ) ;
#1315=DIRECTION ( 'NONE',  ( 0.000000000000000000, -1.000000000000000000, 0.000000000000000000 ) ) ;
#1316=CARTESIAN_POINT ( 'NONE',  ( 1.973079680967599892, -0.1265933021011455828, -0.4721316429241865231 ) ) ;
#1317=CARTESIAN_POINT ( 'NONE',  ( 1.000847373107697891, -0.3830000000000000071, 0.4858637376679703634 ) ) ;
#1322=EDGE_LOOP ( 'NONE', ( #5245, #3256, #6400, #5138 ) ) ;
#1324=EDGE_CURVE ( 'NONE', #1733, #10897, #5794, .T. ) ;
#1329=CARTESIAN_POINT ( 'NONE',  ( 0.8999999999999999112, -0.6429999999999999050, -0.4300000000000014921 ) ) ;
#1333=CARTESIAN_POINT ( 'NONE',  ( 2.045495128834869725, 0.3295048711651374362, 0.4105035982572215469 ) ) ;
#1335=CARTESIAN_POINT ( 'NONE',  ( 0.3724999999999999423, -0.6589999999999996971, 0.4424999999999982836 ) ) ;
#1348=VERTEX_POINT ( 'NONE', #3846 ) ;
#1350=DIRECTION ( 'NONE',  ( 0.000000000000000000, -1.000000000000000000, 0.000000000000000000 ) ) ;
#1375=DIRECTION ( 'NONE',  ( -0.9999002670844991947, 0.000000000000000000, -0.01412288512831128343 ) ) ;
#1376=CARTESIAN_POINT ( 'NONE',  ( 0.4424999999999982281, -0.6589999999999996971, 0.3724999999999999423 ) ) ;
#1381=CARTESIAN_POINT ( 'NONE',  ( 8.849152626892301754, -0.05999999999999997696, 0.3150059839749300705 ) ) ;
#1391=CARTESIAN_POINT ( 'NONE',  ( 0.9652705920801474271, -0.4828330467331338749, -0.4119425203458967344 ) ) ;
#1406=CARTESIAN_POINT ( 'NONE',  ( 0.7096982392392988670, -0.01548513119911374726, -0.4703908291968748046 ) ) ;
#1408=VECTOR ( 'NONE', #8253, 39.37007874015748143 ) ;
#1410=CIRCLE ( 'NONE', #4364, 0.03999999999999998002 ) ;
#1411=CARTESIAN_POINT ( 'NONE',  ( 1.324514161726516592, 5.548674797643638688E-05, 0.4812921728570948576 ) ) ;
#1413=EDGE_CURVE ( 'NONE', #9216, #3261, #12518, .T. ) ;
#1414=FACE_OUTER_BOUND ( 'NONE', #7633, .T. ) ;
#1416=CIRCLE ( 'NONE', #3151, 0.06000000000000002554 ) ;
#1430=CARTESIAN_POINT ( 'NONE',  ( 8.469665986256828205, 0.9969999999999998863, 6.829619984160658046E-17 ) ) ;
#1432=CIRCLE ( 'NONE', #4374, 0.05500000000000146438 ) ;
#1437=EDGE_CURVE ( 'NONE', #11419, #1348, #7787, .T. ) ;
#1439=CARTESIAN_POINT ( 'NONE',  ( 0.8091754559563963944, -0.4422237819269027037, -0.4392762457493078476 ) ) ;
#1443=CARTESIAN_POINT ( 'NONE',  ( 0.6676154558030189534, -0.4647520322684451366, 0.4667586584590060483 ) ) ;
#1447=AXIS2_PLACEMENT_3D ( 'NONE', #8996, #11278, #14794 ) ;
#1450=CARTESIAN_POINT ( 'NONE',  ( 2.916325821605814106, 0.5706613545855653280, 0.3991895006237018428 ) ) ;
#1455=EDGE_CURVE ( 'NONE', #10371, #10000, #4614, .T. ) ;
#1456=DIRECTION ( 'NONE',  ( 1.000000000000000000, 1.874307916738609066E-16, 0.000000000000000000 ) ) ;
#1467=EDGE_LOOP ( 'NONE', ( #12906, #13377, #12539, #4430 ) ) ;
#1468=CARTESIAN_POINT ( 'NONE',  ( 0.3724999999999997757, -0.6589999999999996971, -0.4424999999999983391 ) ) ;
#1471=ADVANCED_FACE ( 'NONE', ( #13603 ), #12532, .T. ) ;
#1482=CARTESIAN_POINT ( 'NONE',  ( 8.752374375191426026, 0.8785908380595726097, -0.1599881670920904608 ) ) ;
#1501=FACE_OUTER_BOUND ( 'NONE', #9427, .T. ) ;
#1502=ORIENTED_EDGE ( 'NONE', *, *, #4020, .F. ) ;
#1513=( BOUNDED_CURVE ( )  B_SPLINE_CURVE ( 3, ( #1690, #378, #12100, #5078 ),
 .UNSPECIFIED., .F., .F. ) 
 B_SPLINE_CURVE_WITH_KNOTS ( ( 4, 4 ),
 ( 4.712388980384689674, 5.497787143782138841 ),
 .UNSPECIFIED. ) 
 CURVE ( )  GEOMETRIC_REPRESENTATION_ITEM ( )  RATIONAL_B_SPLINE_CURVE ( ( 1.000000000000000000, 0.9492530216741910110, 0.9492530216741910110, 1.000000000000000000 ) ) 
 REPRESENTATION_ITEM ( '' )  );
#1515=FACE_OUTER_BOUND ( 'NONE', #15108, .T. ) ;
#1520=EDGE_CURVE ( 'NONE', #5710, #10938, #914, .T. ) ;
#1521=DIRECTION ( 'NONE',  ( 1.000000000000000000, 0.000000000000000000, 0.000000000000000000 ) ) ;
#1522=CARTESIAN_POINT ( 'NONE',  ( 3.025735579118525198, 0.6832920890236183764, 0.4572636217638626488 ) ) ;
#1526=CARTESIAN_POINT ( 'NONE',  ( 0.9659737678069143518, -0.4829423716508983166, -0.4107001390575403810 ) ) ;
#1532=DIRECTION ( 'NONE',  ( -1.655665450705613915E-16, -3.103226861728128995E-32, -1.000000000000000000 ) ) ;
#1537=CARTESIAN_POINT ( 'NONE',  ( 0.7174986153957899626, -0.008289224748913706642, 0.4612806347796405415 ) ) ;
#1553=EDGE_CURVE ( 'NONE', #5216, #7690, #5824, .T. ) ;
#1559=FACE_OUTER_BOUND ( 'NONE', #14733, .T. ) ;
#1568=CARTESIAN_POINT ( 'NONE',  ( -0.4424999999999982836, -0.6590000000000000302, 0.3724999999999999423 ) ) ;
#1570=CARTESIAN_POINT ( 'NONE',  ( 2.957700166089386240, 0.9550922613677920170, 0.4582245739251649685 ) ) ;
#1578=AXIS2_PLACEMENT_3D ( 'NONE', #12455, #8949, #13897 ) ;
#1591=CARTESIAN_POINT ( 'NONE',  ( -0.4424999999999985612, -0.6590000000000000302, -0.8499999999999999778 ) ) ;
#1592=CARTESIAN_POINT ( 'NONE',  ( 0.8999999999999999112, -0.6230000000000016636, -0.3750000000000000555 ) ) ;
#1597=CARTESIAN_POINT ( 'NONE',  ( -0.3725000000000002198, -0.6590000000000000302, -0.4125000000000000333 ) ) ;
#1603=AXIS2_PLACEMENT_3D ( 'NONE', #11666, #5862, #10520 ) ;
#1606=VERTEX_POINT ( 'NONE', #12840 ) ;
#1607=DIRECTION ( 'NONE',  ( -0.7070715176384831935, -0.7070715176384805289, -0.009986885842351451645 ) ) ;
#1608=EDGE_LOOP ( 'NONE', ( #5201, #5091, #11749, #7779 ) ) ;
#1612=FACE_OUTER_BOUND ( 'NONE', #1246, .T. ) ;
#1613=CARTESIAN_POINT ( 'NONE',  ( 5.103871432852032264, 3.303028361439904081, 0.3679054358681541625 ) ) ;
#1619=CONICAL_SURFACE ( 'NONE', #5792, 0.06999999999999829969, 0.7853981633974298493 ) ;
#1640=EDGE_LOOP ( 'NONE', ( #9824, #615, #14579, #12098 ) ) ;
#1646=ORIENTED_EDGE ( 'NONE', *, *, #1413, .F. ) ;
#1653=CIRCLE ( 'NONE', #10223, 0.8499999999999999778 ) ;
#1654=DIRECTION ( 'NONE',  ( -0.4671160445299247232, 0.000000000000000000, 0.8841960195243572240 ) ) ;
#1655=VECTOR ( 'NONE', #4137, 39.37007874015748143 ) ;
#1656=CARTESIAN_POINT ( 'NONE',  ( 0.8336852985356730805, -0.4829999999999999294, -0.4100337033397443709 ) ) ;
#1668=CARTESIAN_POINT ( 'NONE',  ( 2.567289415621050175, 0.8512991579513188301, -0.4032946756736221494 ) ) ;
#1672=AXIS2_PLACEMENT_3D ( 'NONE', #10806, #11954, #4850 ) ;
#1675=AXIS2_PLACEMENT_3D ( 'NONE', #14282, #8275, #340 ) ;
#1676=EDGE_CURVE ( 'NONE', #13657, #34, #1416, .T. ) ;
#1677=CIRCLE ( 'NONE', #2675, 0.03999999999999998002 ) ;
#1678=CARTESIAN_POINT ( 'NONE',  ( 0.7429783265673484127, 2.717297069309015269E-16, 0.4366554833170019356 ) ) ;
#1679=CARTESIAN_POINT ( 'NONE',  ( -0.7287617923574205570, 0.2159999999999999420, -0.4425000000000005596 ) ) ;
#1680=ORIENTED_EDGE ( 'NONE', *, *, #9849, .T. ) ;
#1689=EDGE_LOOP ( 'NONE', ( #11701, #2417, #13648, #11639 ) ) ;
#1690=CARTESIAN_POINT ( 'NONE',  ( 1.250000000000000000, 0.000000000000000000, 0.4223386481965726857 ) ) ;
#1700=CARTESIAN_POINT ( 'NONE',  ( 1.250847373107695670, -0.05999999999999990757, -0.4823326642216427818 ) ) ;
#1713=DIRECTION ( 'NONE',  ( 0.9999002670844990837, 1.110054405283695815E-35, -0.01412288512831213171 ) ) ;
#1718=CARTESIAN_POINT ( 'NONE',  ( 3.339621231360053955, 1.044107824239231430, 0.3927132934522771790 ) ) ;
#1720=DIRECTION ( 'NONE',  ( -0.9702019082525985549, 0.2422978687958610433, 0.000000000000000000 ) ) ;
#1722=CARTESIAN_POINT ( 'NONE',  ( 8.474190026735612946, 0.9969999999999998863, 0.3203020658980471613 ) ) ;
#1724=CARTESIAN_POINT ( 'NONE',  ( 0.4124999999999999223, -0.6290000000000003366, 0.3724999999999999423 ) ) ;
#1725=CARTESIAN_POINT ( 'NONE',  ( 0.9301956387621866940, -0.4439432733257490660, -0.4442820374925280369 ) ) ;
#1728=ORIENTED_EDGE ( 'NONE', *, *, #14216, .F. ) ;
#1733=VERTEX_POINT ( 'NONE', #3863 ) ;
#1740=DIRECTION ( 'NONE',  ( -2.602462600580851747E-17, -1.000000000000000000, 0.000000000000000000 ) ) ;
#1751=ORIENTED_EDGE ( 'NONE', *, *, #13636, .F. ) ;
#1757=ORIENTED_EDGE ( 'NONE', *, *, #10479, .T. ) ;
#1761=DIRECTION ( 'NONE',  ( -0.000000000000000000, -0.000000000000000000, -1.000000000000000000 ) ) ;
#1763=CARTESIAN_POINT ( 'NONE',  ( 0.8268256298210439059, -0.4366477117775379169, -0.3581175243201347169 ) ) ;
#1782=ORIENTED_EDGE ( 'NONE', *, *, #7638, .F. ) ;
#1787=EDGE_LOOP ( 'NONE', ( #4413, #14242, #5193, #14105 ) ) ;
#1790=CARTESIAN_POINT ( 'NONE',  ( 0.8108060929038570785, -0.4829999999999998739, -0.3024090436974096185 ) ) ;
#1792=CARTESIAN_POINT ( 'NONE',  ( 3.475290612095096598, 0.9969999999995592388, 0.4509139744054365129 ) ) ;
#1798=CARTESIAN_POINT ( 'NONE',  ( 8.775135155112195662, 0.9377394161890534319, 0.2318982201004105848 ) ) ;
#1799=CARTESIAN_POINT ( 'NONE',  ( 0.9149939388359350501, -0.4421793831954792808, -0.4489330281185069382 ) ) ;
#1807=LINE ( 'NONE', #6496, #9692 ) ;
#1812=ORIENTED_EDGE ( 'NONE', *, *, #11226, .T. ) ;
#1815=AXIS2_PLACEMENT_3D ( 'NONE', #1592, #3915, #10942 ) ;
#1819=CARTESIAN_POINT ( 'NONE',  ( 0.6734800455634090133, -0.02996288503340473197, 0.4827503109326272135 ) ) ;
#1821=CARTESIAN_POINT ( 'NONE',  ( 0.9745775721194528396, -0.4829504857673974083, -0.3850199534376020916 ) ) ;
#1822=EDGE_CURVE ( 'NONE', #4605, #11449, #8981, .T. ) ;
#1823=ORIENTED_EDGE ( 'NONE', *, *, #8555, .T. ) ;
#1825=DIRECTION ( 'NONE',  ( -1.000000000000000000, 0.000000000000000000, 0.000000000000000000 ) ) ;
#1828=ORIENTED_EDGE ( 'NONE', *, *, #9081, .T. ) ;
#1830=CARTESIAN_POINT ( 'NONE',  ( 0.7238772453881168190, -0.4379537528022394710, 0.4547576871318959602 ) ) ;
#1839=CARTESIAN_POINT ( 'NONE',  ( -0.4424999999999983946, -0.6590000000000000302, -0.3725000000000000533 ) ) ;
#1842=CARTESIAN_POINT ( 'NONE',  ( 0.8296723582540662667, -0.4310852393111275216, -0.3487905724596098711 ) ) ;
#1843=CARTESIAN_POINT ( 'NONE',  ( 0.9669439593609970851, -0.4433899119250455101, -0.4088229889177615872 ) ) ;
#1848=CARTESIAN_POINT ( 'NONE',  ( -0.4424999999999985056, -0.6590000000000000302, -0.8499999999999999778 ) ) ;
#1866=VERTEX_POINT ( 'NONE', #6759 ) ;
#1875=CARTESIAN_POINT ( 'NONE',  ( 0.8999999999999999112, -0.6429999999999999050, -0.3750000000000000555 ) ) ;
#1877=ADVANCED_FACE ( 'NONE', ( #4309 ), #8035, .F. ) ;
#1896=FACE_OUTER_BOUND ( 'NONE', #298, .T. ) ;
#1901=ORIENTED_EDGE ( 'NONE', *, *, #5473, .T. ) ;
#1902=CARTESIAN_POINT ( 'NONE',  ( 3.085497600961857767, 0.7407061222255643118, 0.4564195254101433008 ) ) ;
#1910=LINE ( 'NONE', #3296, #3577 ) ;
#1917=CARTESIAN_POINT ( 'NONE',  ( 0.9749999999999999778, -0.4829448521957645513, -0.3750000000000000555 ) ) ;
#1921=CARTESIAN_POINT ( 'NONE',  ( 1.860560713453747184, -0.1867359432429938626, 0.4737208938777718870 ) ) ;
#1923=DIRECTION ( 'NONE',  ( -0.000000000000000000, 1.000000000000000000, -0.000000000000000000 ) ) ;
#1924=TOROIDAL_SURFACE ( 'NONE', #10492, 0.7057575716915831521, 0.04000000000000000083 ) ;
#1925=DIRECTION ( 'NONE',  ( 0.7071067811865336949, 0.7071067811865612285, 0.000000000000000000 ) ) ;
#1931=CARTESIAN_POINT ( 'NONE',  ( 0.7023826192914042199, -0.3918571065744204107, -0.4896101277505874316 ) ) ;
#1934=DIRECTION ( 'NONE',  ( -0.4919537527695821422, 0.04988190024277998347, -0.8691911764186832645 ) ) ;
#1941=ADVANCED_FACE ( 'NONE', ( #8825 ), #9513, .F. ) ;
#1945=ADVANCED_FACE ( 'NONE', ( #1299 ), #15006, .T. ) ;
#1955=DIRECTION ( 'NONE',  ( -0.8682164115033652596, 8.537024980200830693E-16, -0.4961857140186719528 ) ) ;
#1958=DIRECTION ( 'NONE',  ( -0.8682164115033652596, 0.000000000000000000, -0.4961857140186719528 ) ) ;
#1965=EDGE_CURVE ( 'NONE', #11671, #14534, #12647, .T. ) ;
#1966=ORIENTED_EDGE ( 'NONE', *, *, #2823, .F. ) ;
#1967=DIRECTION ( 'NONE',  ( 0.7071067811865464625, -0.7071067811865486830, 0.000000000000000000 ) ) ;
#1976=CARTESIAN_POINT ( 'NONE',  ( 2.599715518929682556, 0.7930078835992490083, -0.4632808542524021744 ) ) ;
#1977=CARTESIAN_POINT ( 'NONE',  ( 0.9719599677838458573, -0.4431686115285130012, -0.3970034835699213782 ) ) ;
#1979=DIRECTION ( 'NONE',  ( -0.01412288512831213171, 3.675428035873182550E-19, -0.9999002670844991947 ) ) ;
#1986=VERTEX_POINT ( 'NONE', #5686 ) ;
#1989=CARTESIAN_POINT ( 'NONE',  ( 0.7134904538003048469, -0.4429999999999998939, -0.4077598229816901121 ) ) ;
#1993=DIRECTION ( 'NONE',  ( -0.7070715176384873013, -0.7070715176384764211, 0.009986885842350509690 ) ) ;
#2011=ADVANCED_FACE ( 'NONE', ( #15084 ), #12857, .F. ) ;
#2015=ORIENTED_EDGE ( 'NONE', *, *, #14265, .F. ) ;
#2018=CARTESIAN_POINT ( 'NONE',  ( 3.600570009308222907, 1.057000000000000162, -0.3891385068221628885 ) ) ;
#2025=CARTESIAN_POINT ( 'NONE',  ( 0.6566433263006997700, -0.01168724275744807174, -0.4973513887421225910 ) ) ;
#2028=FACE_OUTER_BOUND ( 'NONE', #12492, .T. ) ;
#2029=CARTESIAN_POINT ( 'NONE',  ( 0.8819080671433473517, -0.4426951315057036096, -0.4482526998616632730 ) ) ;
#2035=CYLINDRICAL_SURFACE ( 'NONE', #14080, 0.05999999999999992839 ) ;
#2038=CYLINDRICAL_SURFACE ( 'NONE', #3134, 0.06000000000000001166 ) ;
#2043=EDGE_CURVE ( 'NONE', #1986, #6203, #5310, .T. ) ;
#2045=EDGE_CURVE ( 'NONE', #13550, #10543, #10504, .T. ) ;
#2046=CARTESIAN_POINT ( 'NONE',  ( 2.187203820042823654, 0.4712135623730920875, -0.4085020630706684974 ) ) ;
#2048=CARTESIAN_POINT ( 'NONE',  ( 0.9745723538550742360, -0.4432286986229772574, -0.3850634666812919882 ) ) ;
#2058=DIRECTION ( 'NONE',  ( -1.000000000000000000, -1.837151692781460616E-16, 0.000000000000000000 ) ) ;
#2059=ORIENTED_EDGE ( 'NONE', *, *, #2359, .T. ) ;
#2062=CIRCLE ( 'NONE', #8198, 0.05999999999999997696 ) ;
#2063=( BOUNDED_CURVE ( )  B_SPLINE_CURVE ( 3, ( #7705, #5648, #13729, #11372 ),
 .UNSPECIFIED., .F., .T. ) 
 B_SPLINE_CURVE_WITH_KNOTS ( ( 4, 4 ),
 ( 4.726512335037234891, 6.283185307179586232 ),
 .UNSPECIFIED. ) 
 CURVE ( )  GEOMETRIC_REPRESENTATION_ITEM ( )  RATIONAL_B_SPLINE_CURVE ( ( 1.000000000000000000, 0.8080549792898082950, 0.8080549792898082950, 1.000000000000000000 ) ) 
 REPRESENTATION_ITEM ( '' )  );
#2066=CARTESIAN_POINT ( 'NONE',  ( 1.886302412727927758, -0.2406659208688838592, 0.4137268778526354551 ) ) ;
#2067=CARTESIAN_POINT ( 'NONE',  ( 0.6940843099860020127, -0.4844395605446530917, -0.4145488311989724561 ) ) ;
#2075=CARTESIAN_POINT ( 'NONE',  ( -0.4125000000000001998, 0.1859999999999983611, -0.3725000000000000533 ) ) ;
#2082=CARTESIAN_POINT ( 'NONE',  ( 0.6678750254534769892, -0.4638942219540296286, -0.4666347774677366278 ) ) ;
#2088=EDGE_CURVE ( 'NONE', #8835, #7795, #11570, .T. ) ;
#2089=ORIENTED_EDGE ( 'NONE', *, *, #7219, .T. ) ;
#2090=CIRCLE ( 'NONE', #13562, 0.05999999999999990757 ) ;
#2093=VERTEX_POINT ( 'NONE', #70 ) ;
#2097=DIRECTION ( 'NONE',  ( 0.000000000000000000, 0.000000000000000000, -1.000000000000000000 ) ) ;
#2106=CARTESIAN_POINT ( 'NONE',  ( 0.7350000851713978101, -0.001253058305733974198, -0.4439478790714003753 ) ) ;
#2107=EDGE_CURVE ( 'NONE', #10756, #5850, #3697, .T. ) ;
#2114=CIRCLE ( 'NONE', #9214, 0.07000000000000047851 ) ;
#2124=CARTESIAN_POINT ( 'NONE',  ( 0.6866196799637447334, -0.4820297792901954703, -0.4282732318476363265 ) ) ;
#2127=DIRECTION ( 'NONE',  ( 0.9999002670844991947, 1.365787769249574922E-16, 0.01412288512831213171 ) ) ;
#2131=CIRCLE ( 'NONE', #2426, 0.05999999999999994227 ) ;
#2134=CIRCLE ( 'NONE', #2641, 0.06000000000000004635 ) ;
#2138=DIRECTION ( 'NONE',  ( 0.7071067811865466846, -0.7071067811865483499, 0.000000000000000000 ) ) ;
#2146=CARTESIAN_POINT ( 'NONE',  ( 3.241046123363275022, 0.7391609583210635437, -0.4542225123818747212 ) ) ;
#2153=CARTESIAN_POINT ( 'NONE',  ( 0.8264518852088634793, -0.4832231282500065728, -0.3598842701486069662 ) ) ;
#2162=EDGE_CURVE ( 'NONE', #436, #9069, #7540, .T. ) ;
#2166=( BOUNDED_SURFACE ( )  B_SPLINE_SURFACE ( 3, 2, ( 
 ( #8892, #3080, #4073 ),
 ( #8975, #13617, #13386 ),
 ( #6675, #9287, #6838 ),
 ( #990, #1067, #12705 ),
 ( #13840, #10340, #4609 ),
 ( #5680, #3382, #15082 ),
 ( #13922, #9120, #15002 ),
 ( #2146, #4530, #7974 ),
 ( #8135, #11563, #9201 ),
 ( #3458, #2230, #8063 ) ),
 .UNSPECIFIED., .F., .F., .F. ) 
 B_SPLINE_SURFACE_WITH_KNOTS ( ( 4, 2, 2, 2, 4 ),
 ( 3, 3 ),
 ( 0.7853981633974539411, 0.9730210579868447951, 1.160643952576235760, 1.348266847165626725, 1.535889741755017690 ),
 ( 0.000000000000000000, 1.000000000000000000 ),
 .UNSPECIFIED. ) 
 GEOMETRIC_REPRESENTATION_ITEM ( )  RATIONAL_B_SPLINE_SURFACE ( (
 ( 1.000000000000000000, 0.7106287314217426543, 1.000000000000000000),
 ( 1.000000000000000000, 0.7104090318602969134, 1.000000000000000000),
 ( 1.000000000000000000, 0.7101685202378590356, 1.000000000000000000),
 ( 1.000000000000000000, 0.7096543062750036990, 1.000000000000000000),
 ( 1.000000000000000000, 0.7093805931376407914, 1.000000000000000000),
 ( 1.000000000000000000, 0.7088094415865170417, 1.000000000000000000),
 ( 1.000000000000000000, 0.7085120144470745673, 1.000000000000000000),
 ( 1.000000000000000000, 0.7079038033994521362, 1.000000000000000000),
 ( 1.000000000000000000, 0.7075930366720840636, 1.000000000000000000),
 ( 1.000000000000000000, 0.7072810196742753686, 1.000000000000000000) ) ) 
 REPRESENTATION_ITEM ( '' )  SURFACE ( )  );
#2167=AXIS2_PLACEMENT_3D ( 'NONE', #13845, #7981, #12776 ) ;
#2168=VECTOR ( 'NONE', #1532, 39.37007874015748143 ) ;
#2174=CARTESIAN_POINT ( 'NONE',  ( 8.850000000000576961, 0.8820000000023067166, 0.04908333765188085257 ) ) ;
#2180=EDGE_CURVE ( 'NONE', #14371, #9069, #3843, .T. ) ;
#2186=CARTESIAN_POINT ( 'NONE',  ( 2.087921535706059650, 0.2870784642939424591, -0.4105035982572216025 ) ) ;
#2190=CARTESIAN_POINT ( 'NONE',  ( 0.6555160077358781479, -0.04016535781661281779, -0.5098802871450590635 ) ) ;
#2192=VECTOR ( 'NONE', #7593, 39.37007874015748854 ) ;
#2195=EDGE_CURVE ( 'NONE', #587, #9577, #11716, .T. ) ;
#2200=PLANE ( 'NONE',  #7013 ) ;
#2201=VERTEX_POINT ( 'NONE', #1376 ) ;
#2213=CARTESIAN_POINT ( 'NONE',  ( 3.063895178286538457, 1.056999999999999496, 0.3964908961568774926 ) ) ;
#2217=EDGE_CURVE ( 'NONE', #13066, #14804, #443, .T. ) ;
#2220=ADVANCED_FACE ( 'NONE', ( #9589 ), #13157, .F. ) ;
#2225=DIRECTION ( 'NONE',  ( -0.01412288512831583534, 0.000000000000000000, 0.9999002670844989726 ) ) ;
#2230=CARTESIAN_POINT ( 'NONE',  ( 3.391025564058367081, 0.6913684120611767181, -0.4521041586997406325 ) ) ;
#2234=EDGE_LOOP ( 'NONE', ( #3808, #13892, #8557, #11658, #11611 ) ) ;
#2240=ORIENTED_EDGE ( 'NONE', *, *, #12623, .T. ) ;
#2245=CARTESIAN_POINT ( 'NONE',  ( 0.7849999999999999201, -0.4829999999999998739, -0.3750000000000000555 ) ) ;
#2246=AXIS2_PLACEMENT_3D ( 'NONE', #4092, #9760, #13253 ) ;
#2247=CARTESIAN_POINT ( 'NONE',  ( 1.000048944713735732, -0.4428998280398802612, -0.4293350073753851581 ) ) ;
#2253=ORIENTED_EDGE ( 'NONE', *, *, #11960, .T. ) ;
#2256=ORIENTED_EDGE ( 'NONE', *, *, #12470, .F. ) ;
#2258=CARTESIAN_POINT ( 'NONE',  ( 0.9057578075688627051, -0.4609683907622129651, -0.4498600698720966462 ) ) ;
#2259=CYLINDRICAL_SURFACE ( 'NONE', #12422, 0.05999999999999992839 ) ;
#2260=DIRECTION ( 'NONE',  ( 0.000000000000000000, -1.000000000000000000, 0.000000000000000000 ) ) ;
#2263=CARTESIAN_POINT ( 'NONE',  ( 0.7058998964907864382, -0.06000000000000039330, -0.4900296624789436950 ) ) ;
#2264=FACE_OUTER_BOUND ( 'NONE', #6706, .T. ) ;
#2270=ORIENTED_EDGE ( 'NONE', *, *, #7729, .T. ) ;
#2271=ORIENTED_EDGE ( 'NONE', *, *, #11401, .T. ) ;
#2272=FACE_OUTER_BOUND ( 'NONE', #1787, .T. ) ;
#2273=VERTEX_POINT ( 'NONE', #898 ) ;
#2277=DIRECTION ( 'NONE',  ( 0.000000000000000000, -1.000000000000000000, 0.000000000000000000 ) ) ;
#2278=ORIENTED_EDGE ( 'NONE', *, *, #11226, .F. ) ;
#2281=CARTESIAN_POINT ( 'NONE',  ( 0.6592054058138496764, -0.4435989489166642930, -0.4885496069960003629 ) ) ;
#2285=DIRECTION ( 'NONE',  ( -1.000000000000000000, -1.874307916738609066E-16, 0.000000000000000000 ) ) ;
#2286=EDGE_CURVE ( 'NONE', #3133, #5982, #4216, .T. ) ;
#2300=ORIENTED_EDGE ( 'NONE', *, *, #3918, .F. ) ;
#2306=LINE ( 'NONE', #220, #3798 ) ;
#2309=VERTEX_POINT ( 'NONE', #14608 ) ;
#2311=LINE ( 'NONE', #6993, #3479 ) ;
#2314=ADVANCED_FACE ( 'NONE', ( #2918 ), #3656, .F. ) ;
#2317=ORIENTED_EDGE ( 'NONE', *, *, #10964, .F. ) ;
#2322=EDGE_LOOP ( 'NONE', ( #5269, #8774, #15052, #5211 ) ) ;
#2326=DIRECTION ( 'NONE',  ( 1.000000000000000000, 0.000000000000000000, 0.000000000000000000 ) ) ;
#2333=EDGE_CURVE ( 'NONE', #2708, #11839, #3893, .T. ) ;
#2335=CARTESIAN_POINT ( 'NONE',  ( 1.003096136995459631, -0.4429976034824900655, -0.4258273028168327867 ) ) ;
#2340=CARTESIAN_POINT ( 'NONE',  ( 0.9575621992971196095, -0.4805093615874324597, -0.4235284989533516509 ) ) ;
#2342=CYLINDRICAL_SURFACE ( 'NONE', #4115, 0.03999999999999998002 ) ;
#2345=CARTESIAN_POINT ( 'NONE',  ( 1.002120845300913610, -0.4429991133026480732, -0.4270309162001265646 ) ) ;
#2349=CARTESIAN_POINT ( 'NONE',  ( -1.152890932057317374E-17, -0.4429999999999998939, -0.5000000000000000000 ) ) ;
#2359=EDGE_CURVE ( 'NONE', #2844, #587, #14385, .T. ) ;
#2363=DIRECTION ( 'NONE',  ( -1.365923996832131609E-16, 1.000000000000000000, -0.000000000000000000 ) ) ;
#2366=DIRECTION ( 'NONE',  ( 0.7071067811865487940, 0.7071067811865461294, 0.000000000000000000 ) ) ;
#2372=AXIS2_PLACEMENT_3D ( 'NONE', #10839, #11055, #553 ) ;
#2379=CARTESIAN_POINT ( 'NONE',  ( -0.4125000000000000333, -0.6590000000000000302, 0.4124999999999999223 ) ) ;
#2389=CIRCLE ( 'NONE', #12879, 0.06000000000000001166 ) ;
#2391=CARTESIAN_POINT ( 'NONE',  ( 0.7007157546338583787, -0.4033010131257052655, 0.4867155808989060417 ) ) ;
#2392=CARTESIAN_POINT ( 'NONE',  ( 3.599851685419308556, 0.9969999999999999973, 0.3891486526398028056 ) ) ;
#2397=EDGE_CURVE ( 'NONE', #14837, #6053, #1131, .T. ) ;
#2398=TOROIDAL_SURFACE ( 'NONE', #3129, 0.7173254825712083171, 0.05999999999999999778 ) ;
#2403=CARTESIAN_POINT ( 'NONE',  ( 2.372634528609594007, 0.1852128444980911670, -0.4664882128727459998 ) ) ;
#2405=ADVANCED_FACE ( 'NONE', ( #13979 ), #13907, .F. ) ;
#2413=EDGE_CURVE ( 'NONE', #1037, #8543, #14096, .T. ) ;
#2417=ORIENTED_EDGE ( 'NONE', *, *, #627, .T. ) ;
#2420=DIRECTION ( 'NONE',  ( -1.874307916738606601E-16, 1.000000000000000000, 0.000000000000000000 ) ) ;
#2424=CARTESIAN_POINT ( 'NONE',  ( 0.7034818293080734586, -0.02506196876506533791, -0.4790337915202405039 ) ) ;
#2426=AXIS2_PLACEMENT_3D ( 'NONE', #9931, #5417, #1958 ) ;
#2429=CARTESIAN_POINT ( 'NONE',  ( 1.328406321535844592, -0.06000000000013446660, 0.4812371988483637453 ) ) ;
#2433=PLANE ( 'NONE',  #2484 ) ;
#2450=CARTESIAN_POINT ( 'NONE',  ( 2.371787155501894784, 0.1852128444980907784, -0.4064941968476759038 ) ) ;
#2460=CARTESIAN_POINT ( 'NONE',  ( 0.8999999999999999112, -0.6429999999999999050, -0.3199999999999985634 ) ) ;
#2461=DIRECTION ( 'NONE',  ( 0.000000000000000000, 1.000000000000000000, 0.000000000000000000 ) ) ;
#2462=CARTESIAN_POINT ( 'NONE',  ( 2.683697947871385381, 0.4122708231251925870, 0.4026504426247390356 ) ) ;
#2465=CARTESIAN_POINT ( 'NONE',  ( 8.474190026735614722, 1.056999999999999940, 0.3203020658980470503 ) ) ;
#2482=CARTESIAN_POINT ( 'NONE',  ( 1.127821516536288593, -0.3829999999995594151, -0.4840703175630469146 ) ) ;
#2483=DIRECTION ( 'NONE',  ( 0.000000000000000000, 0.000000000000000000, -1.000000000000000000 ) ) ;
#2484=AXIS2_PLACEMENT_3D ( 'NONE', #6174, #13115, #2652 ) ;
#2489=VERTEX_POINT ( 'NONE', #4514 ) ;
#2491=CARTESIAN_POINT ( 'NONE',  ( -0.3725000000000002198, 0.2159999999999999698, -0.3725000000000000533 ) ) ;
#2494=CARTESIAN_POINT ( 'NONE',  ( 0.9618064621433325412, -0.4822944676752229931, -0.4180629964233649742 ) ) ;
#2498=CARTESIAN_POINT ( 'NONE',  ( 1.813794508431087138, 0.1486894511060126989, 0.4139507449637807035 ) ) ;
#2500=EDGE_CURVE ( 'NONE', #8103, #10897, #11131, .T. ) ;
#2504=ORIENTED_EDGE ( 'NONE', *, *, #3515, .F. ) ;
#2507=EDGE_CURVE ( 'NONE', #7355, #13774, #12610, .T. ) ;
#2521=CARTESIAN_POINT ( 'NONE',  ( 8.475037399843312613, 0.9289129992088663856, 0.3802960819231171463 ) ) ;
#2525=DIRECTION ( 'NONE',  ( 0.7070715176384863021, 0.7070715176384774203, -0.009986885842351498482 ) ) ;
#2527=EDGE_LOOP ( 'NONE', ( #11052, #3694, #10582, #5196 ) ) ;
#2533=EDGE_CURVE ( 'NONE', #5850, #2201, #6749, .T. ) ;
#2537=CARTESIAN_POINT ( 'NONE',  ( 0.9666441941723522557, -0.4829990576375862155, -0.4094325616265704348 ) ) ;
#2545=CARTESIAN_POINT ( 'NONE',  ( 0.7070627455984153098, -0.4242534173714980206, 0.4737642524341733608 ) ) ;
#2553=AXIS2_PLACEMENT_3D ( 'NONE', #6742, #14695, #748 ) ;
#2554=CIRCLE ( 'NONE', #13038, 0.07000000000000047851 ) ;
#2559=CARTESIAN_POINT ( 'NONE',  ( 2.045495128834867060, 0.3295048711651353268, 0.5000000000000000000 ) ) ;
#2566=DIRECTION ( 'NONE',  ( -1.325335837957478697E-16, 0.7071067811865353603, -0.7071067811865596742 ) ) ;
#2572=CARTESIAN_POINT ( 'NONE',  ( 0.7983174577546989781, -0.4429999999999998939, -0.4287183451209413132 ) ) ;
#2575=CARTESIAN_POINT ( 'NONE',  ( 1.398131049395755277, 0.007369456331732793068, 0.4802523863079456445 ) ) ;
#2576=( BOUNDED_SURFACE ( )  B_SPLINE_SURFACE ( 3, 2, ( 
 ( #14145, #3679, #2521 ),
 ( #7199, #6045, #4905 ),
 ( #9571, #2601, #7273 ),
 ( #4269, #2966, #4037 ),
 ( #7706, #12646, #4116 ),
 ( #2891, #3124, #1798 ),
 ( #5186, #7627, #5420 ),
 ( #1013, #12287, #8704 ),
 ( #12367, #2174, #8787 ),
 ( #7558, #7998, #6488 ) ),
 .UNSPECIFIED., .F., .F., .F. ) 
 B_SPLINE_SURFACE_WITH_KNOTS ( ( 4, 2, 2, 2, 4 ),
 ( 3, 3 ),
 ( 4.726512335037234891, 5.115680578072822726, 5.504848821108410561, 5.894017064143998397, 6.283185307179586232 ),
 ( 0.000000000000000000, 1.000000000000000000 ),
 .UNSPECIFIED. ) 
 GEOMETRIC_REPRESENTATION_ITEM ( )  RATIONAL_B_SPLINE_SURFACE ( (
 ( 1.000000000000000000, 0.7072810196742753686, 1.000000000000000000),
 ( 1.000000000000000000, 0.7088814831346345047, 1.000000000000000000),
 ( 1.000000000000000000, 0.7104704279345043227, 1.000000000000000000),
 ( 1.000000000000000000, 0.7133949008902312761, 1.000000000000000000),
 ( 1.000000000000000000, 0.7147290448012498798, 1.000000000000000000),
 ( 1.000000000000000000, 0.7169492149879285181, 1.000000000000000000),
 ( 1.000000000000000000, 0.7178345465032397454, 1.000000000000000000),
 ( 1.000000000000000000, 0.7190300160696035947, 1.000000000000000000),
 ( 1.000000000000000000, 0.7193411551263462211, 1.000000000000000000),
 ( 1.000000000000000000, 0.7193398003386451967, 1.000000000000000000) ) ) 
 REPRESENTATION_ITEM ( '' )  SURFACE ( )  );
#2578=CIRCLE ( 'NONE', #3802, 0.6412116890856960350 ) ;
#2583=VERTEX_POINT ( 'NONE', #6271 ) ;
#2585=ORIENTED_EDGE ( 'NONE', *, *, #11187, .F. ) ;
#2591=DIRECTION ( 'NONE',  ( 0.9999002670844990837, 1.110054405283695815E-35, -0.01412288512831213171 ) ) ;
#2595=CARTESIAN_POINT ( 'NONE',  ( 0.7058998964907862161, -0.05999999999999994227, 0.4900296624789436950 ) ) ;
#2596=AXIS2_PLACEMENT_3D ( 'NONE', #2608, #1140, #5830 ) ;
#2601=CARTESIAN_POINT ( 'NONE',  ( 8.575402687747825325, 0.8724108505555134840, 0.3686609533459700438 ) ) ;
#2602=CARTESIAN_POINT ( 'NONE',  ( 0.8374477884936026850, -0.4460803254964525455, -0.4171268816085695885 ) ) ;
#2605=TOROIDAL_SURFACE ( 'NONE', #4072, 0.8653656741516848605, 0.05999999999999999778 ) ;
#2607=CARTESIAN_POINT ( 'NONE',  ( 0.6601485485260571995, -0.3723516483516483011, 0.5137583810202324131 ) ) ;
#2608=CARTESIAN_POINT ( 'NONE',  ( 0.8999999999999999112, -0.6429999999999999050, -0.3750000000000000555 ) ) ;
#2613=FACE_OUTER_BOUND ( 'NONE', #509, .T. ) ;
#2614=ORIENTED_EDGE ( 'NONE', *, *, #1520, .T. ) ;
#2615=CARTESIAN_POINT ( 'NONE',  ( 2.034127966794863518, -0.2372991579513219207, 0.4117015842447220852 ) ) ;
#2618=CARTESIAN_POINT ( 'NONE',  ( -0.4425000000000007261, 0.2159999999999999420, -0.8499999999999999778 ) ) ;
#2619=ADVANCED_FACE ( 'NONE', ( #4825 ), #2576, .T. ) ;
#2622=DIRECTION ( 'NONE',  ( -1.655665450705613915E-16, 0.000000000000000000, -1.000000000000000000 ) ) ;
#2625=EDGE_CURVE ( 'NONE', #7690, #1866, #13430, .T. ) ;
#2630=EDGE_LOOP ( 'NONE', ( #9539, #10916, #3560, #6578, #13082, #6957, #8243 ) ) ;
#2631=CARTESIAN_POINT ( 'NONE',  ( 2.282850251811050946, 0.09542856769866185640, -0.4677563523755502994 ) ) ;
#2633=CYLINDRICAL_SURFACE ( 'NONE', #4350, 0.03999999999999998002 ) ;
#2637=CIRCLE ( 'NONE', #11179, 0.03999999999999998002 ) ;
#2641=AXIS2_PLACEMENT_3D ( 'NONE', #6563, #11221, #718 ) ;
#2651=CARTESIAN_POINT ( 'NONE',  ( 1.748545107151218803, 0.1138129195078394773, 0.4149214987681951738 ) ) ;
#2652=DIRECTION ( 'NONE',  ( -1.000000000000000000, 0.000000000000000000, 0.000000000000000000 ) ) ;
#2660=ORIENTED_EDGE ( 'NONE', *, *, #14939, .F. ) ;
#2661=CIRCLE ( 'NONE', #7789, 0.05999999999999996309 ) ;
#2667=CARTESIAN_POINT ( 'NONE',  ( 2.381437798646956594, 0.6472152511680805409, 0.4058409478271199355 ) ) ;
#2669=( BOUNDED_SURFACE ( )  B_SPLINE_SURFACE ( 3, 2, ( 
 ( #2737, #8486, #14352 ),
 ( #485, #12210, #1792 ),
 ( #1718, #11138, #11061 ),
 ( #14662, #12063, #14578 ),
 ( #556, #1570, #4106 ),
 ( #8779, #6261, #637 ),
 ( #7620, #5334, #13127 ),
 ( #2667, #7340, #10924 ),
 ( #11992, #10228, #11293 ),
 ( #10301, #4417, #6787 ) ),
 .UNSPECIFIED., .F., .F., .F. ) 
 B_SPLINE_SURFACE_WITH_KNOTS ( ( 4, 2, 2, 2, 4 ),
 ( 3, 3 ),
 ( 1.570796326794896558, 1.767145867644259294, 1.963495408493621808, 2.159844949342984322, 2.356194490192347057 ),
 ( 0.000000000000000000, 1.000000000000000000 ),
 .UNSPECIFIED. ) 
 GEOMETRIC_REPRESENTATION_ITEM ( )  RATIONAL_B_SPLINE_SURFACE ( (
 ( 1.000000000000000000, 0.7071067811865475727, 1.000000000000000000),
 ( 1.000000000000000000, 0.7067799747771658092, 1.000000000000000000),
 ( 1.000000000000000000, 0.7064529522744581458, 1.000000000000000000),
 ( 1.000000000000000000, 0.7058110186548579579, 1.000000000000000000),
 ( 1.000000000000000000, 0.7054961263481117628, 1.000000000000000000),
 ( 1.000000000000000000, 0.7048906332637320249, 1.000000000000000000),
 ( 1.000000000000000000, 0.7046000480541857458, 1.000000000000000000),
 ( 1.000000000000000000, 0.7040544485618952519, 1.000000000000000000),
 ( 1.000000000000000000, 0.7037994241806829754, 1.000000000000000000),
 ( 1.000000000000000000, 0.7035672008258530008, 1.000000000000000000) ) ) 
 REPRESENTATION_ITEM ( '' )  SURFACE ( )  );
#2675=AXIS2_PLACEMENT_3D ( 'NONE', #14893, #5876, #11603 ) ;
#2677=CARTESIAN_POINT ( 'NONE',  ( 0.8725078605757294881, -0.4668629105576758143, -0.4450936002735125241 ) ) ;
#2682=CARTESIAN_POINT ( 'NONE',  ( 8.474190026735612946, 1.056999999999999940, -0.3203020658980470503 ) ) ;
#2687=CARTESIAN_POINT ( 'NONE',  ( 0.8083085967350902568, -0.4844395604395603239, 0.000000000000000000 ) ) ;
#2691=DIRECTION ( 'NONE',  ( 0.9999002670844989726, -2.602203049398213494E-17, -0.01412288512831212997 ) ) ;
#2692=CARTESIAN_POINT ( 'NONE',  ( 0.6570985677785575740, -0.05542231959448562506, 0.5130299739594185171 ) ) ;
#2697=EDGE_LOOP ( 'NONE', ( #5764, #4410, #8464, #10131 ) ) ;
#2699=CARTESIAN_POINT ( 'NONE',  ( 1.003096136995459631, -0.4429976034824900655, -0.4258273028168327867 ) ) ;
#2706=EDGE_CURVE ( 'NONE', #2583, #11671, #5278, .T. ) ;
#2707=CARTESIAN_POINT ( 'NONE',  ( 0.7038889044926298633, -0.05564817238903751323, 0.4900580663207255716 ) ) ;
#2708=VERTEX_POINT ( 'NONE', #1724 ) ;
#2720=CARTESIAN_POINT ( 'NONE',  ( -0.3725000000000000533, -0.6590000000000000302, 0.4424999999999981726 ) ) ;
#2722=CARTESIAN_POINT ( 'NONE',  ( 1.000048944713735732, -0.4428998280398802612, -0.4293350073753851581 ) ) ;
#2737=CARTESIAN_POINT ( 'NONE',  ( 3.601417382415921686, 1.056999999999999718, 0.3891265382754439117 ) ) ;
#2739=CARTESIAN_POINT ( 'NONE',  ( 1.000000000000000222, -0.3829999999999998961, 0.4258697216429003785 ) ) ;
#2745=CARTESIAN_POINT ( 'NONE',  ( 0.4124999999999997558, 0.1859999999999983611, -0.3725000000000000533 ) ) ;
#2760=TOROIDAL_SURFACE ( 'NONE', #4473, 0.1150000000000000050, 0.04000000000000000083 ) ;
#2761=CARTESIAN_POINT ( 'NONE',  ( 0.6601485485260575325, -0.07064835164835217562, 0.5137583810202324131 ) ) ;
#2763=VERTEX_POINT ( 'NONE', #10591 ) ;
#2780=CYLINDRICAL_SURFACE ( 'NONE', #11916, 0.05999999999999983818 ) ;
#2783=ADVANCED_FACE ( 'NONE', ( #6088 ), #3478, .F. ) ;
#2787=ORIENTED_EDGE ( 'NONE', *, *, #13414, .T. ) ;
#2790=CARTESIAN_POINT ( 'NONE',  ( 8.707077114626844860, 0.8770090228646982844, -0.3011897810130372832 ) ) ;
#2807=DIRECTION ( 'NONE',  ( -0.000000000000000000, -1.000000000000000000, -0.000000000000000000 ) ) ;
#2811=ORIENTED_EDGE ( 'NONE', *, *, #9367, .F. ) ;
#2817=AXIS2_PLACEMENT_3D ( 'NONE', #2245, #11582, #8233 ) ;
#2819=CARTESIAN_POINT ( 'NONE',  ( -5.764454660286586870E-18, 0.1956296296296295978, 0.000000000000000000 ) ) ;
#2823=EDGE_CURVE ( 'NONE', #12211, #5232, #8236, .T. ) ;
#2836=AXIS2_PLACEMENT_3D ( 'NONE', #11592, #1097, #3484 ) ;
#2837=CARTESIAN_POINT ( 'NONE',  ( 0.7050899422473002609, -0.02184511171346635930, 0.4765263839844876004 ) ) ;
#2840=LINE ( 'NONE', #10877, #2168 ) ;
#2841=CARTESIAN_POINT ( 'NONE',  ( 8.474190026735612946, 0.9289129992088663856, -0.3203020658980469948 ) ) ;
#2844=VERTEX_POINT ( 'NONE', #10672 ) ;
#2846=ORIENTED_EDGE ( 'NONE', *, *, #14082, .T. ) ;
#2847=CARTESIAN_POINT ( 'NONE',  ( 0.7513246802501660770, 0.000000000000000000, 0.4293820849162031661 ) ) ;
#2852=CARTESIAN_POINT ( 'NONE',  ( 0.8321316902697376561, -0.4837345936509453437, -0.3428764643457666850 ) ) ;
#2853=AXIS2_PLACEMENT_3D ( 'NONE', #13265, #2807, #2877 ) ;
#2860=ORIENTED_EDGE ( 'NONE', *, *, #9184, .T. ) ;
#2861=CARTESIAN_POINT ( 'NONE',  ( 8.635695252271261779, 0.8745163133035791514, -0.2783269381325276237 ) ) ;
#2876=CARTESIAN_POINT ( 'NONE',  ( 1.000000000000000000, -0.4429999999999998939, 0.5000000000000000000 ) ) ;
#2877=DIRECTION ( 'NONE',  ( 0.000000000000000000, 0.000000000000000000, -1.000000000000000000 ) ) ;
#2891=CARTESIAN_POINT ( 'NONE',  ( 8.729039508763705157, 0.8777759665679295553, 0.1953148678277666916 ) ) ;
#2893=CARTESIAN_POINT ( 'NONE',  ( 0.9947690811584967152, -0.4425817642695075715, -0.4349075309858640992 ) ) ;
#2902=EDGE_LOOP ( 'NONE', ( #354, #3331, #2256, #1269 ) ) ;
#2905=CARTESIAN_POINT ( 'NONE',  ( 0.6592054058138496764, 0.0005989489166641660941, 0.4885496069960006404 ) ) ;
#2906=( CONVERSION_BASED_UNIT ( 'INCH', #3052 ) LENGTH_UNIT ( ) NAMED_UNIT ( #14382 ) );
#2909=VECTOR ( 'NONE', #13227, 39.37007874015748143 ) ;
#2913=AXIS2_PLACEMENT_3D ( 'NONE', #6564, #10927, #14582 ) ;
#2917=CARTESIAN_POINT ( 'NONE',  ( 0.6678750254534742137, 0.02089422195403942834, 0.4666347774677351845 ) ) ;
#2918=FACE_OUTER_BOUND ( 'NONE', #5374, .T. ) ;
#2924=CARTESIAN_POINT ( 'NONE',  ( 0.7372049720039715037, -0.4420901695607309390, 0.4419334053338279666 ) ) ;
#2933=DIRECTION ( 'NONE',  ( -0.7070715176384801959, -0.7070715176384837486, -0.009986885842346790443 ) ) ;
#2935=CARTESIAN_POINT ( 'NONE',  ( 1.405961592616384648, -0.05236138586009408263, -0.4801417854150228370 ) ) ;
#2941=CARTESIAN_POINT ( 'NONE',  ( 8.775820958607647881, 0.8794096107945095220, -0.2309380233944421656 ) ) ;
#2945=CARTESIAN_POINT ( 'NONE',  ( 8.475037399843312613, 0.9289129992088663856, -0.3802960819231170908 ) ) ;
#2949=ORIENTED_EDGE ( 'NONE', *, *, #8668, .T. ) ;
#2954=DIMENSIONAL_EXPONENTS ( 1.000000000000000000, 0.000000000000000000, 0.000000000000000000, 0.000000000000000000, 0.000000000000000000, 0.000000000000000000, 0.000000000000000000 ) ;
#2957=DIRECTION ( 'NONE',  ( -0.000000000000000000, -1.000000000000000000, -0.000000000000000000 ) ) ;
#2958=EDGE_LOOP ( 'NONE', ( #2240, #9012, #4322, #7072 ) ) ;
#2963=DIRECTION ( 'NONE',  ( 0.000000000000000000, 0.000000000000000000, -1.000000000000000000 ) ) ;
#2965=CIRCLE ( 'NONE', #8591, 0.06999999999999823030 ) ;
#2966=CARTESIAN_POINT ( 'NONE',  ( 8.665761398406846894, 0.8755662462625590781, 0.3295708899401733616 ) ) ;
#2967=CARTESIAN_POINT ( 'NONE',  ( 0.9188639271548809662, -0.4301917199507425127, -0.4641181468585011127 ) ) ;
#2973=LINE ( 'NONE', #5709, #5049 ) ;
#2983=CARTESIAN_POINT ( 'NONE',  ( 0.7513246802501660770, -0.4429999999999998939, 0.4293820849162031661 ) ) ;
#2985=CARTESIAN_POINT ( 'NONE',  ( 0.7009834207394378680, -0.04376407966659308368, 0.4880078140243662710 ) ) ;
#2986=DIRECTION ( 'NONE',  ( -0.000000000000000000, -1.000000000000000000, -0.000000000000000000 ) ) ;
#2987=ORIENTED_EDGE ( 'NONE', *, *, #8555, .F. ) ;
#2988=CARTESIAN_POINT ( 'NONE',  ( 0.7513246802501661881, -0.5029999999999998916, -0.4293820849162031661 ) ) ;
#3004=CARTESIAN_POINT ( 'NONE',  ( 0.9672769954795885639, -0.4829975555521404118, -0.4081482409674997980 ) ) ;
#3007=CARTESIAN_POINT ( 'NONE',  ( 1.993429504473854585, 0.2774392468041227411, -0.4112782092410746659 ) ) ;
#3009=ORIENTED_EDGE ( 'NONE', *, *, #10175, .F. ) ;
#3010=ORIENTED_EDGE ( 'NONE', *, *, #5456, .F. ) ;
#3014=ORIENTED_EDGE ( 'NONE', *, *, #5139, .T. ) ;
#3017=CARTESIAN_POINT ( 'NONE',  ( 0.6742332106588940777, -0.4177279727767427842, -0.4798232997575455072 ) ) ;
#3020=ORIENTED_EDGE ( 'NONE', *, *, #4780, .F. ) ;
#3025=VERTEX_POINT ( 'NONE', #11968 ) ;
#3031=DIRECTION ( 'NONE',  ( 0.000000000000000000, 0.000000000000000000, -1.000000000000000000 ) ) ;
#3036=DIRECTION ( 'NONE',  ( 0.01412288512831583534, 0.000000000000000000, 0.9999002670844989726 ) ) ;
#3044=ORIENTED_EDGE ( 'NONE', *, *, #1283, .T. ) ;
#3046=ORIENTED_EDGE ( 'NONE', *, *, #3163, .T. ) ;
#3050=ORIENTED_EDGE ( 'NONE', *, *, #3747, .T. ) ;
#3052=LENGTH_MEASURE_WITH_UNIT ( LENGTH_MEASURE( 0.02539999999999999897 ), #5581 );
#3054=ORIENTED_EDGE ( 'NONE', *, *, #3371, .T. ) ;
#3056=LINE ( 'NONE', #4286, #1655 ) ;
#3061=CARTESIAN_POINT ( 'NONE',  ( 3.082852245407359248, 0.9930332973737066027, -0.3962311736270680007 ) ) ;
#3072=CARTESIAN_POINT ( 'NONE',  ( 0.7034818293080725704, -0.4179380312349338933, 0.4790337915202410590 ) ) ;
#3075=VECTOR ( 'NONE', #7575, 39.37007874015748143 ) ;
#3077=DIRECTION ( 'NONE',  ( -0.03489949670249409275, 0.9993908270190960952, 0.000000000000000000 ) ) ;
#3080=CARTESIAN_POINT ( 'NONE',  ( 2.634365942216866596, 0.3629388174706745240, -0.4627914414941119992 ) ) ;
#3084=CARTESIAN_POINT ( 'NONE',  ( 0.3724999999999997757, 0.1859999999999983611, -0.3725000000000000533 ) ) ;
#3098=EDGE_CURVE ( 'NONE', #13120, #5891, #5753, .T. ) ;
#3100=CARTESIAN_POINT ( 'NONE',  ( 0.9173974589322090312, -0.4301166320577336499, -0.4642204989205186427 ) ) ;
#3104=AXIS2_PLACEMENT_3D ( 'NONE', #8331, #5786, #12962 ) ;
#3106=DIRECTION ( 'NONE',  ( 0.000000000000000000, 0.000000000000000000, -1.000000000000000000 ) ) ;
#3113=DIRECTION ( 'NONE',  ( -1.000000000000000000, 0.000000000000000000, -1.224646799147353207E-16 ) ) ;
#3117=VERTEX_POINT ( 'NONE', #11416 ) ;
#3123=EDGE_CURVE ( 'NONE', #14371, #5452, #1088, .T. ) ;
#3124=CARTESIAN_POINT ( 'NONE',  ( 8.775820958607726041, 0.8794096107943684126, 0.2309380233943977012 ) ) ;
#3129=AXIS2_PLACEMENT_3D ( 'NONE', #7163, #15, #8238 ) ;
#3131=CARTESIAN_POINT ( 'NONE',  ( -0.3725000000000000533, -0.6290000000000005587, 0.4124999999999999223 ) ) ;
#3132=VERTEX_POINT ( 'NONE', #13768 ) ;
#3133=VERTEX_POINT ( 'NONE', #837 ) ;
#3134=AXIS2_PLACEMENT_3D ( 'NONE', #4431, #12680, #8948 ) ;
#3144=CARTESIAN_POINT ( 'NONE',  ( 2.599116034107009199, 0.7926631980424555524, -0.4028586330192087672 ) ) ;
#3146=CARTESIAN_POINT ( 'NONE',  ( 0.9747900039790298177, -0.4432332186376475303, -0.3667232257088772207 ) ) ;
#3148=DIRECTION ( 'NONE',  ( 2.602462600580852055E-17, 1.000000000000000000, -0.000000000000000000 ) ) ;
#3151=AXIS2_PLACEMENT_3D ( 'NONE', #9677, #2933, #11035 ) ;
#3155=DIRECTION ( 'NONE',  ( -0.7070715176384816392, -0.7070715176384821943, 0.009986885842350832349 ) ) ;
#3161=VECTOR ( 'NONE', #4672, 39.37007874015748143 ) ;
#3162=EDGE_CURVE ( 'NONE', #9653, #3646, #10141, .T. ) ;
#3163=EDGE_CURVE ( 'NONE', #13167, #2708, #13469, .T. ) ;
#3168=AXIS2_PLACEMENT_3D ( 'NONE', #4471, #3181, #12489 ) ;
#3169=VERTEX_POINT ( 'NONE', #691 ) ;
#3173=CARTESIAN_POINT ( 'NONE',  ( 0.7238317330277980188, -0.4379309809303465473, -0.4548041668469362531 ) ) ;
#3176=CARTESIAN_POINT ( 'NONE',  ( 0.3724999999999999423, 0.1859999999999983611, 0.4124999999999999223 ) ) ;
#3177=ORIENTED_EDGE ( 'NONE', *, *, #2500, .T. ) ;
#3178=CARTESIAN_POINT ( 'NONE',  ( 1.249152626892299001, 0.000000000000000000, 0.4223506167432916625 ) ) ;
#3179=CARTESIAN_POINT ( 'NONE',  ( 2.230477600021715467, 0.4287871555018996084, 0.4684960790957384824 ) ) ;
#3180=AXIS2_PLACEMENT_3D ( 'NONE', #6302, #10966, #11546 ) ;
#3181=DIRECTION ( 'NONE',  ( -1.365923996832131609E-16, 1.000000000000000000, -0.000000000000000000 ) ) ;
#3191=CARTESIAN_POINT ( 'NONE',  ( 0.7997892116363007897, -0.4435060640070847549, -0.3079891465263297490 ) ) ;
#3196=CARTESIAN_POINT ( 'NONE',  ( 0.7009701624870741110, -0.04368263270409020876, -0.4879883456728131841 ) ) ;
#3197=CARTESIAN_POINT ( 'NONE',  ( 0.9431121448573139832, -0.4733191448316948491, -0.4367219098727821436 ) ) ;
#3211=CARTESIAN_POINT ( 'NONE',  ( -5.764454660286586870E-18, 0.04143956043956045082, 0.000000000000000000 ) ) ;
#3215=CARTESIAN_POINT ( 'NONE',  ( 0.9672649160634322341, -0.4430530727333171770, -0.4081727571047791825 ) ) ;
#3223=ORIENTED_EDGE ( 'NONE', *, *, #15069, .T. ) ;
#3224=ORIENTED_EDGE ( 'NONE', *, *, #14852, .T. ) ;
#3234=DIRECTION ( 'NONE',  ( 1.655665450705613915E-16, 0.000000000000000000, 1.000000000000000000 ) ) ;
#3243=CARTESIAN_POINT ( 'NONE',  ( 0.6782188896242887788, -0.4297562849107281480, -0.4691064452754618586 ) ) ;
#3244=CARTESIAN_POINT ( 'NONE',  ( 0.9936287706375830364, -0.4425130709408415242, -0.4361110481179421017 ) ) ;
#3251=ORIENTED_EDGE ( 'NONE', *, *, #9336, .F. ) ;
#3253=ORIENTED_EDGE ( 'NONE', *, *, #8668, .F. ) ;
#3256=ORIENTED_EDGE ( 'NONE', *, *, #14216, .T. ) ;
#3258=LINE ( 'NONE', #13798, #4330 ) ;
#3259=CARTESIAN_POINT ( 'NONE',  ( 0.7867468462925758521, -0.4450678903015412580, -0.3210486967726864371 ) ) ;
#3261=VERTEX_POINT ( 'NONE', #9218 ) ;
#3263=CARTESIAN_POINT ( 'NONE',  ( 0.6894183887957242574, 0.0001162156558598427650, -0.4464953827605273040 ) ) ;
#3269=EDGE_CURVE ( 'NONE', #9046, #12211, #1239, .T. ) ;
#3275=FACE_OUTER_BOUND ( 'NONE', #3762, .T. ) ;
#3285=CARTESIAN_POINT ( 'NONE',  ( 0.6558056096843536409, -0.4243327889391083074, -0.5013356986195880438 ) ) ;
#3287=CARTESIAN_POINT ( 'NONE',  ( 3.340400805682919305, 1.044207302811546612, -0.4528191976596157020 ) ) ;
#3291=EDGE_CURVE ( 'NONE', #1348, #6530, #10648, .T. ) ;
#3296=CARTESIAN_POINT ( 'NONE',  ( -0.4125000000000000333, 0.1859999999999983611, 0.4124999999999999223 ) ) ;
#3305=CARTESIAN_POINT ( 'NONE',  ( 2.002892399652359323, -0.1783233198217482329, 0.4717105593267386654 ) ) ;
#3307=CARTESIAN_POINT ( 'NONE',  ( -0.4125000000000001998, -0.6290000000000005587, -0.4125000000000000333 ) ) ;
#3312=CARTESIAN_POINT ( 'NONE',  ( 0.8395338176367566074, -0.4829999999999997629, -0.3304795099493806343 ) ) ;
#3324=CIRCLE ( 'NONE', #9196, 0.3803340137431718282 ) ;
#3326=EDGE_CURVE ( 'NONE', #14534, #9554, #12099, .T. ) ;
#3331=ORIENTED_EDGE ( 'NONE', *, *, #11087, .F. ) ;
#3338=CARTESIAN_POINT ( 'NONE',  ( 0.6592465977460930660, 0.0007463589180138885653, -0.4884267951992124490 ) ) ;
#3349=ADVANCED_FACE ( 'NONE', ( #6503 ), #579, .T. ) ;
#3352=DIRECTION ( 'NONE',  ( 0.000000000000000000, 0.000000000000000000, -1.000000000000000000 ) ) ;
#3354=ORIENTED_EDGE ( 'NONE', *, *, #14522, .T. ) ;
#3360=CARTESIAN_POINT ( 'NONE',  ( 0.6940366006580477309, -0.4844395604395604349, -0.4146323121508169729 ) ) ;
#3368=DIRECTION ( 'NONE',  ( 0.9992912762382413216, 0.03489602031262312859, -0.01411428356268701854 ) ) ;
#3371=EDGE_CURVE ( 'NONE', #7260, #9538, #4038, .T. ) ;
#3372=CARTESIAN_POINT ( 'NONE',  ( 3.602264755523620465, 0.9969999999999996643, 0.4491205543005138412 ) ) ;
#3374=ORIENTED_EDGE ( 'NONE', *, *, #12725, .T. ) ;
#3377=CARTESIAN_POINT ( 'NONE',  ( 0.6867356290494768256, 0.03910112949509623320, -0.4280493037418063307 ) ) ;
#3382=CARTESIAN_POINT ( 'NONE',  ( 3.046145694169734242, 0.6270559217006406172, -0.4569753433026481071 ) ) ;
#3383=CARTESIAN_POINT ( 'NONE',  ( 2.322097220813319485, 0.05061516561994754138, 0.4672020166565828414 ) ) ;
#3387=CARTESIAN_POINT ( 'NONE',  ( 0.9743412996626567013, -0.4829530011247266108, -0.3864506351494798597 ) ) ;
#3397=DIRECTION ( 'NONE',  ( -1.000000000000000000, 0.000000000000000000, 0.000000000000000000 ) ) ;
#3399=VECTOR ( 'NONE', #2525, 39.37007874015748143 ) ;
#3403=CARTESIAN_POINT ( 'NONE',  ( 0.9355712947711312122, -0.4319563074674140912, -0.4615054731933312393 ) ) ;
#3407=CARTESIAN_POINT ( 'NONE',  ( 0.7983174577546989781, -0.4829999999999998739, -0.4287183451209413132 ) ) ;
#3408=VECTOR ( 'NONE', #14961, 39.37007874015748854 ) ;
#3409=EDGE_LOOP ( 'NONE', ( #12630, #6373, #13508, #1502 ) ) ;
#3410=ORIENTED_EDGE ( 'NONE', *, *, #958, .T. ) ;
#3417=CARTESIAN_POINT ( 'NONE',  ( 0.7006931131589945183, -0.03737057977092374250, -0.4858697363291134552 ) ) ;
#3421=CARTESIAN_POINT ( 'NONE',  ( 0.6729652567417454545, -0.03979450559140960270, -0.4872362964973816490 ) ) ;
#3423=ORIENTED_EDGE ( 'NONE', *, *, #9805, .T. ) ;
#3428=DIRECTION ( 'NONE',  ( 0.000000000000000000, 0.000000000000000000, -1.000000000000000000 ) ) ;
#3429=EDGE_LOOP ( 'NONE', ( #3939, #12431, #7108, #8738 ) ) ;
#3438=DIRECTION ( 'NONE',  ( -0.000000000000000000, 1.000000000000000000, -0.000000000000000000 ) ) ;
#3452=ORIENTED_EDGE ( 'NONE', *, *, #12127, .T. ) ;
#3458=CARTESIAN_POINT ( 'NONE',  ( 3.388933043275772050, 0.7513023213622327390, -0.4521337140780258834 ) ) ;
#3463=CARTESIAN_POINT ( 'NONE',  ( 0.6731911676471491468, -0.3979338129854863571, 0.4888638514297523607 ) ) ;
#3465=CYLINDRICAL_SURFACE ( 'NONE', #9831, 0.06000000000000001860 ) ;
#3476=CARTESIAN_POINT ( 'NONE',  ( 2.414213562373088262, 0.1427864376268981050, -0.4064941968476760703 ) ) ;
#3478=PLANE ( 'NONE',  #12118 ) ;
#3479=VECTOR ( 'NONE', #7222, 39.37007874015748854 ) ;
#3482=ORIENTED_EDGE ( 'NONE', *, *, #4611, .F. ) ;
#3484=DIRECTION ( 'NONE',  ( 0.03489949670249522379, -0.9993908270190959842, 0.000000000000000000 ) ) ;
#3486=CARTESIAN_POINT ( 'NONE',  ( 2.592367411162173063, 0.4049457270506677808, -0.4633846410852800468 ) ) ;
#3488=CARTESIAN_POINT ( 'NONE',  ( 0.9257356467070699813, -0.4653787754209000038, -0.4457641624418894888 ) ) ;
#3490=CARTESIAN_POINT ( 'NONE',  ( 0.7007544714965479038, -0.04192809431833794537, -0.4875120335496958557 ) ) ;
#3494=CARTESIAN_POINT ( 'NONE',  ( 0.6676004498178161883, 0.02173067840223007890, -0.4667915867939429475 ) ) ;
#3510=CARTESIAN_POINT ( 'NONE',  ( 0.6609607771814278721, -0.4492411629263703410, -0.4835552281312081591 ) ) ;
#3514=DIRECTION ( 'NONE',  ( -1.874307916738609066E-16, 1.000000000000000000, 0.000000000000000000 ) ) ;
#3515=EDGE_CURVE ( 'NONE', #9898, #11449, #12161, .T. ) ;
#3516=CARTESIAN_POINT ( 'NONE',  ( 8.792093969802149189, 0.8799778768672790186, 0.1855527009831954288 ) ) ;
#3522=ORIENTED_EDGE ( 'NONE', *, *, #12613, .T. ) ;
#3530=ORIENTED_EDGE ( 'NONE', *, *, #1324, .F. ) ;
#3534=EDGE_CURVE ( 'NONE', #8801, #1005, #8459, .T. ) ;
#3546=AXIS2_PLACEMENT_3D ( 'NONE', #7983, #6845, #11499 ) ;
#3547=AXIS2_PLACEMENT_3D ( 'NONE', #11730, #1375, #8438 ) ;
#3550=ORIENTED_EDGE ( 'NONE', *, *, #4611, .T. ) ;
#3560=ORIENTED_EDGE ( 'NONE', *, *, #9184, .F. ) ;
#3572=CARTESIAN_POINT ( 'NONE',  ( -0.4125000000000000333, 0.1859999999999983611, 0.3724999999999999423 ) ) ;
#3576=CARTESIAN_POINT ( 'NONE',  ( 1.323631913064689192, 7.693249048049262105E-17, 0.4212431828234003972 ) ) ;
#3577=VECTOR ( 'NONE', #11557, 39.37007874015748143 ) ;
#3578=CARTESIAN_POINT ( 'NONE',  ( 1.000847373107698779, -0.3829999999999998961, -0.4858637376679703634 ) ) ;
#3586=DIRECTION ( 'NONE',  ( 0.000000000000000000, 0.000000000000000000, -1.000000000000000000 ) ) ;
#3589=AXIS2_PLACEMENT_3D ( 'NONE', #7261, #4812, #3428 ) ;
#3597=AXIS2_PLACEMENT_3D ( 'NONE', #785, #4260, #12436 ) ;
#3612=DIRECTION ( 'NONE',  ( -1.365923996832131609E-16, 1.000000000000000000, 0.000000000000000000 ) ) ;
#3615=PRODUCT_DEFINITION ( 'UNKNOWN', '', #14022, #11823 ) ;
#3624=ORIENTED_EDGE ( 'NONE', *, *, #10830, .T. ) ;
#3631=AXIS2_PLACEMENT_3D ( 'NONE', #6499, #10865, #4207 ) ;
#3634=EDGE_CURVE ( 'NONE', #11355, #10371, #9474, .T. ) ;
#3637=CARTESIAN_POINT ( 'NONE',  ( -0.3725000000000002198, 0.2159999999999999420, -0.4425000000000005596 ) ) ;
#3638=VECTOR ( 'NONE', #396, 39.37007874015748143 ) ;
#3646=VERTEX_POINT ( 'NONE', #14909 ) ;
#3652=ORIENTED_EDGE ( 'NONE', *, *, #11090, .F. ) ;
#3655=CARTESIAN_POINT ( 'NONE',  ( 1.993429504473980929, 0.2774392468042482518, 0.4112782092410766643 ) ) ;
#3656=( BOUNDED_SURFACE ( )  B_SPLINE_SURFACE ( 3, 2, ( 
 ( #8958, #14759, #4292 ),
 ( #4059, #5439, #10184 ),
 ( #10105, #9954, #6434 ),
 ( #13599, #13680, #4144 ),
 ( #14836, #3146, #8726 ),
 ( #13368, #4367, #9036 ),
 ( #7808, #2048, #1821 ),
 ( #12461, #1977, #6659 ),
 ( #11317, #7579, #13449 ),
 ( #6510, #3215, #6738 ) ),
 .UNSPECIFIED., .F., .F., .F. ) 
 B_SPLINE_SURFACE_WITH_KNOTS ( ( 4, 2, 2, 2, 4 ),
 ( 3, 3 ),
 ( 0.009445390106978779690, 0.01015357746046147147, 0.01086176481394416499, 0.01156995216742685850, 0.01227813952090955202 ),
 ( 0.000000000000000000, 1.000000000000000000 ),
 .UNSPECIFIED. ) 
 GEOMETRIC_REPRESENTATION_ITEM ( )  RATIONAL_B_SPLINE_SURFACE ( (
 ( 1.000000000000000000, 0.7071067811865481278, 1.000000000000000000),
 ( 1.000000000000000000, 0.7078095846774001831, 1.000000000000000000),
 ( 1.000000000000000000, 0.7084372686669646590, 1.000000000000000000),
 ( 1.000000000000000000, 0.7093555124764521214, 1.000000000000000000),
 ( 1.000000000000000000, 0.7096393529300775160, 1.000000000000000000),
 ( 1.000000000000000000, 0.7097449673932565428, 1.000000000000000000),
 ( 1.000000000000000000, 0.7095699935427098870, 1.000000000000000000),
 ( 1.000000000000000000, 0.7088230032924415225, 1.000000000000000000),
 ( 1.000000000000000000, 0.7082619641421786794, 1.000000000000000000),
 ( 1.000000000000000000, 0.7075975758264665405, 1.000000000000000000) ) ) 
 REPRESENTATION_ITEM ( '' )  SURFACE ( )  );
#3662=FACE_OUTER_BOUND ( 'NONE', #2322, .T. ) ;
#3664=ORIENTED_EDGE ( 'NONE', *, *, #5910, .T. ) ;
#3673=DIRECTION ( 'NONE',  ( 0.7071067811865345831, -0.7071067811865603403, 0.000000000000000000 ) ) ;
#3679=CARTESIAN_POINT ( 'NONE',  ( 8.477129920625907644, 0.8689790899078102537, 0.3802665265448320064 ) ) ;
#3690=ORIENTED_EDGE ( 'NONE', *, *, #12757, .F. ) ;
#3694=ORIENTED_EDGE ( 'NONE', *, *, #14463, .F. ) ;
#3697=LINE ( 'NONE', #3982, #14868 ) ;
#3699=CARTESIAN_POINT ( 'NONE',  ( 0.6940259540059589005, -0.4844395603711075249, 0.4146509415068772020 ) ) ;
#3711=AXIS2_PLACEMENT_3D ( 'NONE', #14799, #3106, #5171 ) ;
#3714=ADVANCED_FACE ( 'NONE', ( #13051 ), #163, .T. ) ;
#3722=CARTESIAN_POINT ( 'NONE',  ( 0.9126855013391443894, -0.4618906521135902610, -0.4490017598779234009 ) ) ;
#3735=ORIENTED_EDGE ( 'NONE', *, *, #9316, .T. ) ;
#3744=( BOUNDED_CURVE ( )  B_SPLINE_CURVE ( 3, ( #6948, #12892, #12970, #103 ),
 .UNSPECIFIED., .F., .F. ) 
 B_SPLINE_CURVE_WITH_KNOTS ( ( 4, 4 ),
 ( 0.7853981633974547183, 1.535889741755017912 ),
 .UNSPECIFIED. ) 
 CURVE ( )  GEOMETRIC_REPRESENTATION_ITEM ( )  RATIONAL_B_SPLINE_CURVE ( ( 1.000000000000000000, 0.9536117119880161974, 0.9536117119880161974, 1.000000000000000000 ) ) 
 REPRESENTATION_ITEM ( '' )  );
#3747=EDGE_CURVE ( 'NONE', #5710, #11671, #7268, .T. ) ;
#3756=CARTESIAN_POINT ( 'NONE',  ( -0.7287617923574205570, 0.2159999999999999420, -0.4425000000000005596 ) ) ;
#3761=CARTESIAN_POINT ( 'NONE',  ( 2.449076186954514686E-17, -0.4430000000000000049, 0.000000000000000000 ) ) ;
#3762=EDGE_LOOP ( 'NONE', ( #12427, #7817, #7944, #744 ) ) ;
#3763=DIRECTION ( 'NONE',  ( 0.000000000000000000, 0.000000000000000000, 1.000000000000000000 ) ) ;
#3775=DIRECTION ( 'NONE',  ( -1.000000000000000000, -2.130223169792495565E-16, 0.000000000000000000 ) ) ;
#3776=ORIENTED_EDGE ( 'NONE', *, *, #10085, .F. ) ;
#3778=VERTEX_POINT ( 'NONE', #1275 ) ;
#3788=ORIENTED_EDGE ( 'NONE', *, *, #10853, .T. ) ;
#3790=CARTESIAN_POINT ( 'NONE',  ( 8.476283996537762988, 0.8689495495877206377, -0.3203020658980470503 ) ) ;
#3793=AXIS2_PLACEMENT_3D ( 'NONE', #10247, #14907, #2591 ) ;
#3798=VECTOR ( 'NONE', #7068, 39.37007874015748143 ) ;
#3802=AXIS2_PLACEMENT_3D ( 'NONE', #297, #9666, #3775 ) ;
#3808=ORIENTED_EDGE ( 'NONE', *, *, #4280, .T. ) ;
#3829=DIRECTION ( 'NONE',  ( 0.000000000000000000, 0.7071067811865600072, -0.7071067811865350272 ) ) ;
#3833=CARTESIAN_POINT ( 'NONE',  ( 3.080868217518119678, 0.9969999999999996643, -0.4564849121819474775 ) ) ;
#3836=DIRECTION ( 'NONE',  ( -0.9743309173630048114, 0.2251205531944285021, 2.276539994720217179E-15 ) ) ;
#3837=CARTESIAN_POINT ( 'NONE',  ( 3.046145694169734242, 0.6270559217007690700, 0.4569753433027124445 ) ) ;
#3839=CARTESIAN_POINT ( 'NONE',  ( 8.789999999999999147, 0.9969999999999998863, 6.829619984160658046E-17 ) ) ;
#3842=CARTESIAN_POINT ( 'NONE',  ( 0.7134904538003040697, 1.075665147505303778E-15, 0.4077598229816906117 ) ) ;
#3843=LINE ( 'NONE', #1597, #9271 ) ;
#3846=CARTESIAN_POINT ( 'NONE',  ( 8.493408712665044769E-17, 0.1956296296296295978, 0.7406097974541305806 ) ) ;
#3862=DIRECTION ( 'NONE',  ( -0.000000000000000000, -0.000000000000000000, -1.000000000000000000 ) ) ;
#3863=CARTESIAN_POINT ( 'NONE',  ( 1.003096136995459631, -0.4429976034824900655, -0.4258273028168327867 ) ) ;
#3865=ORIENTED_EDGE ( 'NONE', *, *, #2333, .T. ) ;
#3867=CIRCLE ( 'NONE', #3631, 0.05500000000000146438 ) ;
#3868=EDGE_LOOP ( 'NONE', ( #3530, #5726, #4984, #10562, #3177 ) ) ;
#3876=CARTESIAN_POINT ( 'NONE',  ( 1.936801488370294866, 0.2309360081137078191, 0.4726440467746176322 ) ) ;
#3881=VECTOR ( 'NONE', #14460, 39.37007874015748143 ) ;
#3887=EDGE_CURVE ( 'NONE', #436, #5452, #10996, .T. ) ;
#3893=CIRCLE ( 'NONE', #12428, 0.03999999999999998002 ) ;
#3895=FACE_OUTER_BOUND ( 'NONE', #6114, .T. ) ;
#3908=CARTESIAN_POINT ( 'NONE',  ( 0.6552609544199018421, -0.4103521735780240598, 0.5074720589858902065 ) ) ;
#3909=DIRECTION ( 'NONE',  ( -0.000000000000000000, -1.000000000000000000, 0.000000000000000000 ) ) ;
#3910=ORIENTED_EDGE ( 'NONE', *, *, #2195, .F. ) ;
#3912=CIRCLE ( 'NONE', #10264, 0.1150000000000000050 ) ;
#3913=DIRECTION ( 'NONE',  ( -0.01412288512831128343, 0.000000000000000000, 0.9999002670844990837 ) ) ;
#3914=CARTESIAN_POINT ( 'NONE',  ( 0.6552609544199017311, -0.03264782642197579937, -0.5074720589858900954 ) ) ;
#3915=DIRECTION ( 'NONE',  ( 0.000000000000000000, 1.000000000000000000, 0.000000000000000000 ) ) ;
#3918=EDGE_CURVE ( 'NONE', #12826, #3132, #2389, .T. ) ;
#3919=CARTESIAN_POINT ( 'NONE',  ( 0.6729666568098726653, -0.03983805101166792983, 0.4872504569466099000 ) ) ;
#3922=VERTEX_POINT ( 'NONE', #11063 ) ;
#3925=CARTESIAN_POINT ( 'NONE',  ( 2.372215031318393841, 0.1847933472068912786, -0.4664941379757289175 ) ) ;
#3926=ORIENTED_EDGE ( 'NONE', *, *, #11203, .T. ) ;
#3929=ORIENTED_EDGE ( 'NONE', *, *, #1084, .F. ) ;
#3934=EDGE_CURVE ( 'NONE', #7832, #5232, #5119, .T. ) ;
#3936=VECTOR ( 'NONE', #15118, 39.37007874015748143 ) ;
#3939=ORIENTED_EDGE ( 'NONE', *, *, #2706, .T. ) ;
#3952=ORIENTED_EDGE ( 'NONE', *, *, #895, .F. ) ;
#3958=SHAPE_DEFINITION_REPRESENTATION ( #271, #1014 ) ;
#3961=CARTESIAN_POINT ( 'NONE',  ( -0.6412116890856959239, -0.6590000000000000302, 0.000000000000000000 ) ) ;
#3975=CARTESIAN_POINT ( 'NONE',  ( 8.849999999999999645, 0.9399413264884247665, 0.2203075555454639400 ) ) ;
#3981=CARTESIAN_POINT ( 'NONE',  ( 0.6766092641689648302, -0.01690956365765576563, 0.4729901586420273696 ) ) ;
#3982=CARTESIAN_POINT ( 'NONE',  ( -0.7287617923574203349, -0.6590000000000000302, 0.4424999999999983391 ) ) ;
#3983=ORIENTED_EDGE ( 'NONE', *, *, #12144, .F. ) ;
#3988=ORIENTED_EDGE ( 'NONE', *, *, #8778, .F. ) ;
#3996=EDGE_CURVE ( 'NONE', #9577, #11355, #2134, .T. ) ;
#3998=CARTESIAN_POINT ( 'NONE',  ( 0.8259541526021394464, -0.4394713480196544286, -0.3620748417912383887 ) ) ;
#4003=CARTESIAN_POINT ( 'NONE',  ( 1.748545107151228573, 0.1138129195078436268, -0.4149214987681278943 ) ) ;
#4009=EDGE_CURVE ( 'NONE', #3169, #9348, #5826, .T. ) ;
#4011=CARTESIAN_POINT ( 'NONE',  ( 8.803302564019885423, 0.8803692896022989878, -0.1890918720381968565 ) ) ;
#4014=LINE ( 'NONE', #10980, #3638 ) ;
#4017=VECTOR ( 'NONE', #3829, 39.37007874015748143 ) ;
#4020=EDGE_CURVE ( 'NONE', #4756, #13120, #9651, .T. ) ;
#4037=CARTESIAN_POINT ( 'NONE',  ( 8.664307099992964112, 0.9344797629247902915, 0.3304588241376503199 ) ) ;
#4038=CIRCLE ( 'NONE', #6489, 0.3803340137431718282 ) ;
#4043=ORIENTED_EDGE ( 'NONE', *, *, #11946, .F. ) ;
#4044=ORIENTED_EDGE ( 'NONE', *, *, #9331, .T. ) ;
#4048=EDGE_LOOP ( 'NONE', ( #7440, #12276, #5163, #3020 ) ) ;
#4057=AXIS2_PLACEMENT_3D ( 'NONE', #5165, #9825, #6461 ) ;
#4059=CARTESIAN_POINT ( 'NONE',  ( 1.004564342297052937, -0.4429999999999998939, -0.3264090227193217064 ) ) ;
#4064=( LENGTH_UNIT ( ) NAMED_UNIT ( * ) SI_UNIT ( $, .METRE. ) );
#4068=ORIENTED_EDGE ( 'NONE', *, *, #14567, .F. ) ;
#4072=AXIS2_PLACEMENT_3D ( 'NONE', #7186, #14046, #3586 ) ;
#4073=CARTESIAN_POINT ( 'NONE',  ( 2.633946444925666874, 0.3625193201794745801, -0.4033906250602101173 ) ) ;
#4074=CARTESIAN_POINT ( 'NONE',  ( 1.552356239822777484, 3.287267395616053572E-16, -0.4178403161916763864 ) ) ;
#4075=CARTESIAN_POINT ( 'NONE',  ( 1.254789639631331388, -0.3704945895121533050, 0.4822769824910828618 ) ) ;
#4076=CARTESIAN_POINT ( 'NONE',  ( 0.8318304347846213753, -0.4310575137535593848, -0.3436027928218019500 ) ) ;
#4082=ORIENTED_EDGE ( 'NONE', *, *, #11770, .F. ) ;
#4087=CARTESIAN_POINT ( 'NONE',  ( 8.840280274186273601, 0.9396554517976997145, -0.09865722066565443815 ) ) ;
#4092=CARTESIAN_POINT ( 'NONE',  ( 0.007386697474241961034, -0.2214999999999999469, -0.5229781811763313248 ) ) ;
#4094=EDGE_CURVE ( 'NONE', #1606, #9348, #8431, .T. ) ;
#4106=CARTESIAN_POINT ( 'NONE',  ( 2.977166378292719351, 0.8979166429007084949, 0.4579496274252440879 ) ) ;
#4115=AXIS2_PLACEMENT_3D ( 'NONE', #12735, #2260, #4644 ) ;
#4116=CARTESIAN_POINT ( 'NONE',  ( 8.705855184453634266, 0.9357017671275056347, 0.3021636316006244272 ) ) ;
#4122=CARTESIAN_POINT ( 'NONE',  ( -0.3725000000000002198, 0.1859999999999983611, -0.4125000000000000333 ) ) ;
#4124=ORIENTED_EDGE ( 'NONE', *, *, #13636, .T. ) ;
#4127=ORIENTED_EDGE ( 'NONE', *, *, #12315, .F. ) ;
#4137=DIRECTION ( 'NONE',  ( -1.000000000000000000, 0.000000000000000000, 0.000000000000000000 ) ) ;
#4140=CIRCLE ( 'NONE', #202, 0.8083085967350902568 ) ;
#4142=CARTESIAN_POINT ( 'NONE',  ( 0.7007173259569011714, -0.03973197056396925858, 0.4867265490097323344 ) ) ;
#4143=( BOUNDED_CURVE ( )  B_SPLINE_CURVE ( 3, ( #8600, #528, #4074, #7516 ),
 .UNSPECIFIED., .F., .F. ) 
 B_SPLINE_CURVE_WITH_KNOTS ( ( 4, 4 ),
 ( 3.926990816987240063, 4.712388980384689674 ),
 .UNSPECIFIED. ) 
 CURVE ( )  GEOMETRIC_REPRESENTATION_ITEM ( )  RATIONAL_B_SPLINE_CURVE ( ( 1.000000000000000000, 0.9492530216741910110, 0.9492530216741910110, 1.000000000000000000 ) ) 
 REPRESENTATION_ITEM ( '' )  );
#4144=CARTESIAN_POINT ( 'NONE',  ( 0.9738596046707562737, -0.4829585099714701069, -0.3606225395865768069 ) ) ;
#4145=EDGE_CURVE ( 'NONE', #2489, #13460, #4846, .T. ) ;
#4146=ORIENTED_EDGE ( 'NONE', *, *, #5910, .F. ) ;
#4151=( NAMED_UNIT ( * ) SI_UNIT ( $, .STERADIAN. ) SOLID_ANGLE_UNIT ( ) );
#4161=CARTESIAN_POINT ( 'NONE',  ( 0.8418300605894717403, -0.4429999999999996163, -0.3276580719765712635 ) ) ;
#4162=CARTESIAN_POINT ( 'NONE',  ( 3.268630585053793405E-17, -0.5030000000000000027, 0.000000000000000000 ) ) ;
#4168=DIRECTION ( 'NONE',  ( 0.000000000000000000, -0.7071067811865600072, -0.7071067811865350272 ) ) ;
#4169=VERTEX_POINT ( 'NONE', #2687 ) ;
#4173=ORIENTED_EDGE ( 'NONE', *, *, #4094, .T. ) ;
#4179=ORIENTED_EDGE ( 'NONE', *, *, #4555, .T. ) ;
#4180=EDGE_CURVE ( 'NONE', #2273, #13657, #9543, .T. ) ;
#4184=EDGE_LOOP ( 'NONE', ( #4434, #2987, #5808, #7121 ) ) ;
#4185=FACE_OUTER_BOUND ( 'NONE', #10949, .T. ) ;
#4192=CARTESIAN_POINT ( 'NONE',  ( 2.088768908813758873, 0.2870784642939425146, -0.4704976142822915319 ) ) ;
#4195=EDGE_CURVE ( 'NONE', #9577, #184, #10909, .T. ) ;
#4198=CARTESIAN_POINT ( 'NONE',  ( 0.9483256016623491380, -0.4339531631712009174, -0.4584628122268601946 ) ) ;
#4207=DIRECTION ( 'NONE',  ( 1.000000000000000000, 0.000000000000000000, 0.000000000000000000 ) ) ;
#4209=DIRECTION ( 'NONE',  ( 0.01412288512831583534, 0.000000000000000000, 0.9999002670844989726 ) ) ;
#4215=CARTESIAN_POINT ( 'NONE',  ( 2.381437798646418358, 0.6472152511677208286, -0.4058409478271036708 ) ) ;
#4216=LINE ( 'NONE', #14526, #442 ) ;
#4223=CARTESIAN_POINT ( 'NONE',  ( 0.7020471549603384265, -0.4140285412429734468, 0.4816513823572639574 ) ) ;
#4229=ADVANCED_FACE ( 'NONE', ( #12158 ), #8799, .F. ) ;
#4231=FACE_OUTER_BOUND ( 'NONE', #7636, .T. ) ;
#4232=( BOUNDED_CURVE ( )  B_SPLINE_CURVE ( 3, ( #12441, #6638, #10155, #14813 ),
 .UNSPECIFIED., .F., .F. ) 
 B_SPLINE_CURVE_WITH_KNOTS ( ( 4, 4 ),
 ( 1.605702911834775870, 2.356194490192339064 ),
 .UNSPECIFIED. ) 
 CURVE ( )  GEOMETRIC_REPRESENTATION_ITEM ( )  RATIONAL_B_SPLINE_CURVE ( ( 1.000000000000000000, 0.9536117119880161974, 0.9536117119880161974, 1.000000000000000000 ) ) 
 REPRESENTATION_ITEM ( '' )  );
#4247=CARTESIAN_POINT ( 'NONE',  ( 0.6821548861275755771, -0.4360442393940396344, -0.4605830663053250285 ) ) ;
#4248=EDGE_CURVE ( 'NONE', #10100, #1606, #3867, .T. ) ;
#4252=FACE_OUTER_BOUND ( 'NONE', #4617, .T. ) ;
#4260=DIRECTION ( 'NONE',  ( 1.365923996832131609E-16, -1.000000000000000000, -0.000000000000000000 ) ) ;
#4268=CARTESIAN_POINT ( 'NONE',  ( 8.474190026735612946, 0.9969999999999998863, -0.3203020658980470503 ) ) ;
#4269=CARTESIAN_POINT ( 'NONE',  ( 8.635695252271263556, 0.8745163133035790404, 0.2783269381325281788 ) ) ;
#4270=CARTESIAN_POINT ( 'NONE',  ( 0.9652705920801475381, -0.4828330467331340969, -0.4119425203458967344 ) ) ;
#4276=ORIENTED_EDGE ( 'NONE', *, *, #706, .T. ) ;
#4280=EDGE_CURVE ( 'NONE', #15092, #5075, #6064, .T. ) ;
#4286=CARTESIAN_POINT ( 'NONE',  ( -0.4125000000000001998, 0.1859999999999983611, -0.4125000000000000333 ) ) ;
#4291=CARTESIAN_POINT ( 'NONE',  ( 3.601417382415922130, 1.056999999999999718, -0.3891265382754439117 ) ) ;
#4292=CARTESIAN_POINT ( 'NONE',  ( 0.9652173913043479159, -0.4829999999999998739, -0.3379636412230419551 ) ) ;
#4308=DIRECTION ( 'NONE',  ( 0.000000000000000000, 0.000000000000000000, -1.000000000000000000 ) ) ;
#4309=FACE_OUTER_BOUND ( 'NONE', #2630, .T. ) ;
#4316=EDGE_CURVE ( 'NONE', #2489, #8413, #10704, .T. ) ;
#4318=VERTEX_POINT ( 'NONE', #12453 ) ;
#4322=ORIENTED_EDGE ( 'NONE', *, *, #9251, .F. ) ;
#4323=LINE ( 'NONE', #3178, #5240 ) ;
#4324=CARTESIAN_POINT ( 'NONE',  ( 0.6601485485260571995, -0.3723516483516484121, -0.5137583810202325241 ) ) ;
#4328=ORIENTED_EDGE ( 'NONE', *, *, #8650, .T. ) ;
#4330=VECTOR ( 'NONE', #6785, 39.37007874015748854 ) ;
#4334=ORIENTED_EDGE ( 'NONE', *, *, #7082, .F. ) ;
#4339=PLANE ( 'NONE',  #11443 ) ;
#4342=CARTESIAN_POINT ( 'NONE',  ( 1.003096136995459631, -0.4429976034824900655, -0.4258273028168327867 ) ) ;
#4343=DIRECTION ( 'NONE',  ( -0.9992912762382415437, -0.03489602031261518356, 0.01411428356269074126 ) ) ;
#4345=CARTESIAN_POINT ( 'NONE',  ( 0.9740510491226479495, -0.4388824337986295676, -0.4485312320239642769 ) ) ;
#4350=AXIS2_PLACEMENT_3D ( 'NONE', #10590, #9535, #2483 ) ;
#4360=CARTESIAN_POINT ( 'NONE',  ( 0.6653056208004449745, -0.4594276363813551423, -0.4725671546919800181 ) ) ;
#4364=AXIS2_PLACEMENT_3D ( 'NONE', #8581, #6138, #3763 ) ;
#4367=CARTESIAN_POINT ( 'NONE',  ( 0.9751458587006417433, -0.4432411459049188096, -0.3788907315698128997 ) ) ;
#4368=ADVANCED_FACE ( 'NONE', ( #13740 ), #2038, .T. ) ;
#4369=EDGE_LOOP ( 'NONE', ( #2614, #7241, #13987, #7799 ) ) ;
#4374=AXIS2_PLACEMENT_3D ( 'NONE', #12841, #8121, #14991 ) ;
#4377=CARTESIAN_POINT ( 'NONE',  ( 3.601417382415921686, 1.056999999999999718, 0.3891265382754439117 ) ) ;
#4382=FACE_OUTER_BOUND ( 'NONE', #14823, .T. ) ;
#4386=CARTESIAN_POINT ( 'NONE',  ( 0.7206835787589728204, -0.4360447880780422003, -0.4581197915133099485 ) ) ;
#4392=DIRECTION ( 'NONE',  ( 0.7071067811865414665, -0.7071067811865535679, 0.000000000000000000 ) ) ;
#4399=ORIENTED_EDGE ( 'NONE', *, *, #9944, .T. ) ;
#4402=CARTESIAN_POINT ( 'NONE',  ( 0.6566194192392912354, -0.4311570606644820614, -0.4974488347804309485 ) ) ;
#4407=ORIENTED_EDGE ( 'NONE', *, *, #9714, .F. ) ;
#4410=ORIENTED_EDGE ( 'NONE', *, *, #3269, .T. ) ;
#4413=ORIENTED_EDGE ( 'NONE', *, *, #697, .F. ) ;
#4415=CARTESIAN_POINT ( 'NONE',  ( 2.633946444925666874, 0.3625193201794746356, 0.4033906250602100618 ) ) ;
#4417=CARTESIAN_POINT ( 'NONE',  ( 2.187631780374527324, 0.4716415227047960901, 0.4691012460399078821 ) ) ;
#4418=ORIENTED_EDGE ( 'NONE', *, *, #8804, .F. ) ;
#4422=CARTESIAN_POINT ( 'NONE',  ( 0.6570965961311068249, -0.05543357626841138863, -0.5130374278108783548 ) ) ;
#4428=CARTESIAN_POINT ( 'NONE',  ( 1.000000000000000000, -0.4429999999999998939, 0.5000000000000000000 ) ) ;
#4430=ORIENTED_EDGE ( 'NONE', *, *, #4842, .F. ) ;
#4431=CARTESIAN_POINT ( 'NONE',  ( -0.0008473731076987391477, -0.05999999999999997696, -0.4400059839749300150 ) ) ;
#4434=ORIENTED_EDGE ( 'NONE', *, *, #6727, .T. ) ;
#4436=CARTESIAN_POINT ( 'NONE',  ( 0.6766651500320096657, -0.4745799178806336949, -0.4479228816209578357 ) ) ;
#4440=CARTESIAN_POINT ( 'NONE',  ( 3.083590687937563857, 0.9932358216848905519, -0.4564464592101518114 ) ) ;
#4448=DIRECTION ( 'NONE',  ( 1.000000000000000000, 0.000000000000000000, -1.655665450705613915E-16 ) ) ;
#4460=CARTESIAN_POINT ( 'NONE',  ( -0.3725000000000002198, 0.1859999999999983611, -0.3725000000000000533 ) ) ;
#4461=CARTESIAN_POINT ( 'NONE',  ( 0.8254245316410396827, -0.4829999999999998739, -0.3670313414528085239 ) ) ;
#4469=CARTESIAN_POINT ( 'NONE',  ( 0.6732025385091796599, -0.3978263200806930744, -0.4888865340280575400 ) ) ;
#4471=CARTESIAN_POINT ( 'NONE',  ( 0.8999999999999999112, -0.6429999999999999050, -0.3750000000000000555 ) ) ;
#4473=AXIS2_PLACEMENT_3D ( 'NONE', #10459, #13731, #4495 ) ;
#4476=EDGE_CURVE ( 'NONE', #13120, #10897, #11698, .T. ) ;
#4483=DIRECTION ( 'NONE',  ( 0.000000000000000000, 1.000000000000000000, 0.000000000000000000 ) ) ;
#4488=DIRECTION ( 'NONE',  ( 0.000000000000000000, 0.7071067811865603403, 0.7071067811865345831 ) ) ;
#4489=CARTESIAN_POINT ( 'NONE',  ( 0.6558154374103656314, -0.01854616410104658816, -0.5012742423172328321 ) ) ;
#4493=CIRCLE ( 'NONE', #9863, 0.06999999999999836908 ) ;
#4495=DIRECTION ( 'NONE',  ( -1.000000000000000000, -1.365923996832131609E-16, 0.000000000000000000 ) ) ;
#4514=CARTESIAN_POINT ( 'NONE',  ( 0.7058998964907862161, -0.3830000000000000071, -0.4900296624789436950 ) ) ;
#4530=CARTESIAN_POINT ( 'NONE',  ( 3.250637184708968785, 0.6799532182389171897, -0.4540870454137406198 ) ) ;
#4531=CARTESIAN_POINT ( 'NONE',  ( 2.220468100499050745, -0.03283382702752232762, 0.4686374562078457484 ) ) ;
#4533=DIRECTION ( 'NONE',  ( -1.000000000000000000, 0.000000000000000000, 0.000000000000000000 ) ) ;
#4534=EDGE_LOOP ( 'NONE', ( #3410, #2278, #12350, #9540 ) ) ;
#4536=CARTESIAN_POINT ( 'NONE',  ( 0.6555160077358691550, -0.4028346421833865487, 0.5098802871450707208 ) ) ;
#4537=FACE_OUTER_BOUND ( 'NONE', #1467, .T. ) ;
#4547=CARTESIAN_POINT ( 'NONE',  ( 3.113342878570761307, 0.6489923502455474669, 0.4560262305287002826 ) ) ;
#4550=DIRECTION ( 'NONE',  ( 0.000000000000000000, 1.000000000000000000, 0.000000000000000000 ) ) ;
#4555=EDGE_CURVE ( 'NONE', #5428, #12577, #7366, .T. ) ;
#4557=ADVANCED_FACE ( 'NONE', ( #633 ), #14086, .F. ) ;
#4561=DIRECTION ( 'NONE',  ( -0.9992912762382413216, -0.03489602031262311471, 0.01411428356268702201 ) ) ;
#4567=DIRECTION ( 'NONE',  ( 1.365923996832131609E-16, -1.000000000000000000, 0.000000000000000000 ) ) ;
#4568=ORIENTED_EDGE ( 'NONE', *, *, #2413, .T. ) ;
#4571=CARTESIAN_POINT ( 'NONE',  ( 0.7070627455984020981, -0.01874658262850352822, -0.4737642524341751926 ) ) ;
#4572=CARTESIAN_POINT ( 'NONE',  ( 1.250847373107698779, -0.05999999999999997696, -0.4823326642216426707 ) ) ;
#4579=ORIENTED_EDGE ( 'NONE', *, *, #14681, .F. ) ;
#4580=FACE_OUTER_BOUND ( 'NONE', #10386, .T. ) ;
#4582=ORIENTED_EDGE ( 'NONE', *, *, #1324, .T. ) ;
#4587=DIRECTION ( 'NONE',  ( 0.9999002670844989726, -2.665865973017557838E-15, -0.01412288512831216640 ) ) ;
#4589=AXIS2_PLACEMENT_3D ( 'NONE', #8952, #6890, #4587 ) ;
#4591=PLANE ( 'NONE',  #9041 ) ;
#4593=CARTESIAN_POINT ( 'NONE',  ( 3.601417382415921686, 1.056999999999999718, 0.3891265382754439117 ) ) ;
#4594=CONICAL_SURFACE ( 'NONE', #5821, 0.07000000000000047851, 0.7853981633974297383 ) ;
#4597=CARTESIAN_POINT ( 'NONE',  ( 8.792093969802149189, 0.8799778768672790186, 6.829619984160658046E-17 ) ) ;
#4603=ORIENTED_EDGE ( 'NONE', *, *, #9379, .T. ) ;
#4604=CARTESIAN_POINT ( 'NONE',  ( 0.6592591305498912702, 0.0007908075296091682943, -0.4883895785410080626 ) ) ;
#4605=VERTEX_POINT ( 'NONE', #1568 ) ;
#4608=AXIS2_PLACEMENT_3D ( 'NONE', #8649, #6587, #11245 ) ;
#4609=CARTESIAN_POINT ( 'NONE',  ( 2.916325821605861623, 0.5706613545855859781, -0.3991895006237661803 ) ) ;
#4611=EDGE_CURVE ( 'NONE', #2093, #8372, #14816, .T. ) ;
#4614=CIRCLE ( 'NONE', #13375, 0.7173254825712085392 ) ;
#4617=EDGE_LOOP ( 'NONE', ( #14075, #1003, #3044, #10467, #3253, #11896, #5625, #5414, #3926, #9448, #12228 ) ) ;
#4619=CARTESIAN_POINT ( 'NONE',  ( 0.7073375012244004223, -0.4456044010854968151, 0.4168187156545198335 ) ) ;
#4620=DIRECTION ( 'NONE',  ( 0.000000000000000000, 0.000000000000000000, -1.000000000000000000 ) ) ;
#4623=CARTESIAN_POINT ( 'NONE',  ( 0.7513246802501661881, -0.4429999999999998939, -0.4293820849162031661 ) ) ;
#4626=VERTEX_POINT ( 'NONE', #8483 ) ;
#4627=AXIS2_PLACEMENT_3D ( 'NONE', #2618, #291, #8371 ) ;
#4630=DIRECTION ( 'NONE',  ( 1.000000000000000000, -2.602462600580852055E-17, 0.000000000000000000 ) ) ;
#4644=DIRECTION ( 'NONE',  ( 0.000000000000000000, 0.000000000000000000, -1.000000000000000000 ) ) ;
#4648=CARTESIAN_POINT ( 'NONE',  ( 0.6742552310713034736, -0.02516590133966824933, -0.4797493044159580888 ) ) ;
#4653=ORIENTED_EDGE ( 'NONE', *, *, #2180, .F. ) ;
#4663=( BOUNDED_SURFACE ( )  B_SPLINE_SURFACE ( 3, 2, ( 
 ( #393, #5233, #12263 ),
 ( #8609, #9757, #538 ),
 ( #11116, #11042, #4087 ),
 ( #1482, #4011, #13404 ),
 ( #8676, #2941, #619 ),
 ( #6389, #2790, #7390 ),
 ( #2861, #9685, #9902 ),
 ( #13322, #7602, #7528 ),
 ( #9985, #6165, #14333 ),
 ( #3790, #10824, #8466 ) ),
 .UNSPECIFIED., .F., .F., .F. ) 
 B_SPLINE_SURFACE_WITH_KNOTS ( ( 4, 2, 2, 2, 4 ),
 ( 3, 3 ),
 ( 0.000000000000000000, 0.3891682430355878353, 0.7783364860711756705, 1.167504729106763506, 1.556672972142351341 ),
 ( 0.000000000000000000, 1.000000000000000000 ),
 .UNSPECIFIED. ) 
 GEOMETRIC_REPRESENTATION_ITEM ( )  RATIONAL_B_SPLINE_SURFACE ( (
 ( 1.000000000000000000, 0.7193398003386451967, 1.000000000000000000),
 ( 1.000000000000000000, 0.7193411551263428905, 1.000000000000000000),
 ( 1.000000000000000000, 0.7190300160696043719, 1.000000000000000000),
 ( 1.000000000000000000, 0.7178345465032389683, 1.000000000000000000),
 ( 1.000000000000000000, 0.7169492149876324216, 1.000000000000000000),
 ( 1.000000000000000000, 0.7147290448015459763, 1.000000000000000000),
 ( 1.000000000000000000, 0.7133949008891797838, 1.000000000000000000),
 ( 1.000000000000000000, 0.7104704279355633645, 1.000000000000000000),
 ( 1.000000000000000000, 0.7088814831338368094, 1.000000000000000000),
 ( 1.000000000000000000, 0.7072810196742753686, 1.000000000000000000) ) ) 
 REPRESENTATION_ITEM ( '' )  SURFACE ( )  );
#4665=DIRECTION ( 'NONE',  ( 1.000000000000000000, -2.602462600580852055E-17, 0.000000000000000000 ) ) ;
#4672=DIRECTION ( 'NONE',  ( -1.000000000000000000, -1.874307916738609066E-16, 0.000000000000000000 ) ) ;
#4683=CARTESIAN_POINT ( 'NONE',  ( 0.7067472695984847730, -0.3830000000000000071, -0.5500236785040135690 ) ) ;
#4692=ORIENTED_EDGE ( 'NONE', *, *, #9251, .T. ) ;
#4693=CARTESIAN_POINT ( 'NONE',  ( 0.6746175797782828498, -0.3871287346720767020, 0.4907030699472766377 ) ) ;
#4694=CIRCLE ( 'NONE', #2246, 0.6700292969071726112 ) ;
#4700=EDGE_CURVE ( 'NONE', #8801, #8372, #10191, .T. ) ;
#4704=CARTESIAN_POINT ( 'NONE',  ( 2.002892399651176714, -0.1783233198227758276, -0.4717105593270736752 ) ) ;
#4713=ORIENTED_EDGE ( 'NONE', *, *, #4316, .T. ) ;
#4717=CARTESIAN_POINT ( 'NONE',  ( 2.372634528609593563, 0.1852128444980908617, 0.4664882128727458888 ) ) ;
#4718=CARTESIAN_POINT ( 'NONE',  ( 0.7038870757886633855, -0.05564421503643584427, -0.4900580921498777776 ) ) ;
#4722=CARTESIAN_POINT ( 'NONE',  ( 1.249999999999999778, 9.390727478220904197E-17, 0.4223386481965726857 ) ) ;
#4748=CARTESIAN_POINT ( 'NONE',  ( 2.229630226914017133, 0.4287871555018993308, 0.4085020630706684974 ) ) ;
#4751=EDGE_LOOP ( 'NONE', ( #5895, #907, #9609, #13567, #5106, #2059, #10614, #11638, #5017, #2949, #6472, #9626 ) ) ;
#4755=EDGE_LOOP ( 'NONE', ( #431, #14640, #12547, #13584 ) ) ;
#4756=VERTEX_POINT ( 'NONE', #4415 ) ;
#4760=CARTESIAN_POINT ( 'NONE',  ( -0.3725000000000000533, -0.6590000000000000302, 0.4424999999999981726 ) ) ;
#4766=CARTESIAN_POINT ( 'NONE',  ( 0.7058998964907849949, -0.3829999999999992855, 0.4900296624789436950 ) ) ;
#4780=EDGE_CURVE ( 'NONE', #9554, #2583, #8249, .T. ) ;
#4790=VECTOR ( 'NONE', #1607, 39.37007874015748143 ) ;
#4800=CARTESIAN_POINT ( 'NONE',  ( 1.749262710669756693, 0.1141659463772449479, 0.4752928995668608270 ) ) ;
#4806=CARTESIAN_POINT ( 'NONE',  ( -5.764454660286586870E-18, 0.1956296296296295978, -0.7406097974541305806 ) ) ;
#4812=DIRECTION ( 'NONE',  ( 0.000000000000000000, -1.000000000000000000, 0.000000000000000000 ) ) ;
#4821=B_SPLINE_CURVE_WITH_KNOTS ( 'NONE', 3,
 ( #12753, #13822, #13745, #13974, #11622, #3285, #11704, #2281, #3510, #4360, #6891, #6964, #4436, #2124, #3360, #1046 ),
 .UNSPECIFIED., .F., .F.,
 ( 4, 2, 2, 2, 2, 2, 2, 4 ),
 ( 0.000000000000000000, 0.0005886476847306641811, 0.001177295369461328362, 0.001765943054191992543, 0.002354590738922656724, 0.002943238423653320689, 0.003531886108383985087, 0.004709181477845313449 ),
 .UNSPECIFIED. ) ;
#4825=FACE_OUTER_BOUND ( 'NONE', #13815, .T. ) ;
#4828=LINE ( 'NONE', #7052, #3399 ) ;
#4837=CARTESIAN_POINT ( 'NONE',  ( 0.8999999999999999112, -0.4829999999999998739, -0.3750000000000000555 ) ) ;
#4842=EDGE_CURVE ( 'NONE', #6905, #11355, #3258, .T. ) ;
#4844=EDGE_CURVE ( 'NONE', #5232, #6530, #6294, .T. ) ;
#4845=CARTESIAN_POINT ( 'NONE',  ( 0.9717435313913082018, -0.4829764291992613701, -0.3975967162296610846 ) ) ;
#4846=CIRCLE ( 'NONE', #6549, 0.06000000000000005329 ) ;
#4848=CARTESIAN_POINT ( 'NONE',  ( 0.7204397385173402224, -0.4363855711863642850, 0.4582225808237245790 ) ) ;
#4850=DIRECTION ( 'NONE',  ( 1.000000000000000000, 0.000000000000000000, 0.000000000000000000 ) ) ;
#4853=EDGE_CURVE ( 'NONE', #7795, #9366, #6557, .T. ) ;
#4859=VECTOR ( 'NONE', #9332, 39.37007874015748143 ) ;
#4861=CARTESIAN_POINT ( 'NONE',  ( 0.9999999999999964473, -0.4429999999999999494, -0.4258697216429006005 ) ) ;
#4865=FACE_OUTER_BOUND ( 'NONE', #11160, .T. ) ;
#4878=EDGE_CURVE ( 'NONE', #2583, #12064, #6628, .T. ) ;
#4881=AXIS2_PLACEMENT_3D ( 'NONE', #1722, #10156, #3036 ) ;
#4888=CARTESIAN_POINT ( 'NONE',  ( 2.088768908813758873, 0.2870784642939424591, -0.4704976142822916430 ) ) ;
#4891=CARTESIAN_POINT ( 'NONE',  ( 1.250847373107698779, -0.05999999999999997696, 0.4823326642216426707 ) ) ;
#4905=CARTESIAN_POINT ( 'NONE',  ( 8.524379033352621704, 0.9303642257649958891, 0.3795991661955845919 ) ) ;
#4910=CARTESIAN_POINT ( 'NONE',  ( 0.6555107925675723868, -0.4029228396118701983, 0.5098556521091195393 ) ) ;
#4917=CARTESIAN_POINT ( 'NONE',  ( 3.320735777595773541, 0.6889667851711056556, 0.4530969522938014249 ) ) ;
#4918=ORIENTED_EDGE ( 'NONE', *, *, #4476, .F. ) ;
#4919=CARTESIAN_POINT ( 'NONE',  ( 1.537522204129377457, -0.4429999999999995053, 0.4185053637614668531 ) ) ;
#4924=DIRECTION ( 'NONE',  ( 0.000000000000000000, -1.000000000000000000, 0.000000000000000000 ) ) ;
#4935=DIRECTION ( 'NONE',  ( -0.7070715176384863021, -0.7070715176384774203, 0.009986885842351498482 ) ) ;
#4936=CARTESIAN_POINT ( 'NONE',  ( 1.860560713452861892, -0.1867359432425545751, -0.4737208938777845435 ) ) ;
#4943=EDGE_CURVE ( 'NONE', #3132, #5891, #11080, .T. ) ;
#4949=CARTESIAN_POINT ( 'NONE',  ( 8.475037399843312613, 0.9969999999999998863, -0.3802960819231170908 ) ) ;
#4953=ORIENTED_EDGE ( 'NONE', *, *, #2397, .T. ) ;
#4956=DIRECTION ( 'NONE',  ( -0.7071067811865519026, -0.7071067811865430208, 0.000000000000000000 ) ) ;
#4962=ORIENTED_EDGE ( 'NONE', *, *, #4700, .F. ) ;
#4964=PLANE ( 'NONE',  #6776 ) ;
#4967=PRODUCT_CONTEXT ( 'NONE', #6078, 'mechanical' ) ;
#4976=CARTESIAN_POINT ( 'NONE',  ( 0.8310910854522474134, -0.4382321058747689624, -0.4519764243385314129 ) ) ;
#4983=CYLINDRICAL_SURFACE ( 'NONE', #2596, 0.07500000000000002498 ) ;
#4984=ORIENTED_EDGE ( 'NONE', *, *, #4280, .F. ) ;
#4988=CARTESIAN_POINT ( 'NONE',  ( 0.6601485485260571995, -0.07064835164835162051, -0.5137583810202324131 ) ) ;
#4990=ORIENTED_EDGE ( 'NONE', *, *, #14852, .F. ) ;
#4992=CARTESIAN_POINT ( 'NONE',  ( 0.6746193685512165139, -0.05586318815840191770, 0.4906972545532043428 ) ) ;
#4999=CARTESIAN_POINT ( 'NONE',  ( 1.539501593423603154, -0.4421672100983570219, -0.4184782450098369910 ) ) ;
#5004=CARTESIAN_POINT ( 'NONE',  ( 2.187203820042824542, 0.4712135623730921985, 0.4085020630706684974 ) ) ;
#5010=LINE ( 'NONE', #7444, #11732 ) ;
#5017=ORIENTED_EDGE ( 'NONE', *, *, #13478, .T. ) ;
#5019=FACE_OUTER_BOUND ( 'NONE', #11828, .T. ) ;
#5027=CARTESIAN_POINT ( 'NONE',  ( 1.405961592616383316, -0.05236138586009463081, 0.4801417854150228370 ) ) ;
#5037=ORIENTED_EDGE ( 'NONE', *, *, #10175, .T. ) ;
#5049=VECTOR ( 'NONE', #4561, 39.37007874015748854 ) ;
#5051=DIRECTION ( 'NONE',  ( 0.000000000000000000, 0.000000000000000000, -1.000000000000000000 ) ) ;
#5056=DIRECTION ( 'NONE',  ( -1.655665450705613915E-16, -3.103226861728128995E-32, -1.000000000000000000 ) ) ;
#5061=CARTESIAN_POINT ( 'NONE',  ( 0.6940366006580476199, 0.04143956043956066593, 0.4146323121508169729 ) ) ;
#5062=CARTESIAN_POINT ( 'NONE',  ( 0.000000000000000000, 0.000000000000000000, 0.000000000000000000 ) ) ;
#5066=EDGE_CURVE ( 'NONE', #1274, #13460, #4694, .T. ) ;
#5068=CARTESIAN_POINT ( 'NONE',  ( 0.7145271609291293791, -0.01099779881553469840, 0.4647412378891488394 ) ) ;
#5075=VERTEX_POINT ( 'NONE', #2722 ) ;
#5078=CARTESIAN_POINT ( 'NONE',  ( 2.045495128834867060, 0.3295048711651353268, 0.4105035982572216025 ) ) ;
#5084=CARTESIAN_POINT ( 'NONE',  ( 0.7893200925859867878, -0.4447764794942862809, -0.3170959440181289613 ) ) ;
#5090=VECTOR ( 'NONE', #13071, 39.37007874015748143 ) ;
#5091=ORIENTED_EDGE ( 'NONE', *, *, #10479, .F. ) ;
#5092=CARTESIAN_POINT ( 'NONE',  ( 2.230049639690012242, 0.4283591951701958278, -0.4685021237331919441 ) ) ;
#5106=ORIENTED_EDGE ( 'NONE', *, *, #14078, .T. ) ;
#5119=LINE ( 'NONE', #3961, #13846 ) ;
#5120=DIRECTION ( 'NONE',  ( -0.9992912762382412106, -0.03489602031262427351, -0.01411428356269072044 ) ) ;
#5122=VECTOR ( 'NONE', #13953, 39.37007874015748143 ) ;
#5138=ORIENTED_EDGE ( 'NONE', *, *, #7506, .T. ) ;
#5139=EDGE_CURVE ( 'NONE', #13964, #10623, #487, .T. ) ;
#5142=CARTESIAN_POINT ( 'NONE',  ( 0.7010312871322611494, 0.003350962741495644263, 0.4267273516602812511 ) ) ;
#5146=EDGE_LOOP ( 'NONE', ( #7681, #6214, #3788, #6655, #6802 ) ) ;
#5156=CARTESIAN_POINT ( 'NONE',  ( 0.8258103947154198377, -0.4830000013490253208, -0.3634202042301618585 ) ) ;
#5160=CARTESIAN_POINT ( 'NONE',  ( 1.936238515863220711, 0.2305039212133961901, -0.4121290732901491949 ) ) ;
#5163=ORIENTED_EDGE ( 'NONE', *, *, #2706, .F. ) ;
#5165=CARTESIAN_POINT ( 'NONE',  ( 0.3724999999999999423, -0.6590000000000000302, 0.3724999999999999423 ) ) ;
#5171=DIRECTION ( 'NONE',  ( 1.000000000000000000, 0.000000000000000000, 0.000000000000000000 ) ) ;
#5176=ORIENTED_EDGE ( 'NONE', *, *, #7782, .F. ) ;
#5178=CARTESIAN_POINT ( 'NONE',  ( 0.8999999999999999112, -0.4829999999999998739, -0.3750000000000000555 ) ) ;
#5180=CARTESIAN_POINT ( 'NONE',  ( 0.8254245316410396827, -0.4829999999999998739, -0.3670313414528085239 ) ) ;
#5183=FACE_OUTER_BOUND ( 'NONE', #12998, .T. ) ;
#5186=CARTESIAN_POINT ( 'NONE',  ( 8.752374375191447342, 0.8785908380595733869, 0.1599881670920847154 ) ) ;
#5187=CARTESIAN_POINT ( 'NONE',  ( 0.8482706842831971850, -0.4349723313396169910, -0.4582157225860795102 ) ) ;
#5193=ORIENTED_EDGE ( 'NONE', *, *, #6712, .T. ) ;
#5195=CARTESIAN_POINT ( 'NONE',  ( 3.602264755523620465, 0.9969999999999996643, -0.4491205543005138412 ) ) ;
#5196=ORIENTED_EDGE ( 'NONE', *, *, #7506, .F. ) ;
#5198=CARTESIAN_POINT ( 'NONE',  ( 0.6601485485260571995, -0.07064835164835162051, 0.5137583810202324131 ) ) ;
#5201=ORIENTED_EDGE ( 'NONE', *, *, #13440, .T. ) ;
#5206=CARTESIAN_POINT ( 'NONE',  ( 0.7022453151856735687, -0.02852180867591198182, 0.4813241942165198406 ) ) ;
#5207=( BOUNDED_SURFACE ( )  B_SPLINE_SURFACE ( 3, 2, ( 
 ( #4324, #848, #8910 ),
 ( #769, #622, #11201 ),
 ( #14719, #8995, #5628 ),
 ( #10212, #4469, #6543 ),
 ( #13475, #12421, #5469 ),
 ( #14947, #14871, #9141 ),
 ( #4402, #3017, #6622 ),
 ( #7683, #13554, #9066 ),
 ( #9990, #3243, #11276 ),
 ( #7909, #4247, #12559 ),
 ( #2082, #6770, #13779 ),
 ( #12266, #10341, #4386 ),
 ( #5613, #6676, #12544 ),
 ( #9051, #5683, #12471 ),
 ( #2067, #6757, #14853 ),
 ( #11333, #1989, #11411 ) ),
 .UNSPECIFIED., .F., .F., .F. ) 
 B_SPLINE_SURFACE_WITH_KNOTS ( ( 4, 2, 2, 2, 2, 2, 2, 4 ),
 ( 3, 3 ),
 ( 0.002083263661281769923, 0.002712596804664455137, 0.003341929948047140785, 0.003971263091429826433, 0.004600596234812511648, 0.005229929378195196862, 0.005859262521577882077, 0.007117928808343253373 ),
 ( 0.000000000000000000, 1.000000000000000000 ),
 .UNSPECIFIED. ) 
 GEOMETRIC_REPRESENTATION_ITEM ( )  RATIONAL_B_SPLINE_SURFACE ( (
 ( 1.000000000000000000, 0.8987017906623400165, 1.000000000000000000),
 ( 1.000000000000000000, 0.9020594141850755143, 1.000000000000000000),
 ( 1.000000000000000000, 0.9044651860914172392, 1.000000000000000000),
 ( 1.000000000000000000, 0.9073335834956595125, 1.000000000000000000),
 ( 1.000000000000000000, 0.9077660037303413310, 1.000000000000000000),
 ( 1.000000000000000000, 0.9065807100086308301, 1.000000000000000000),
 ( 1.000000000000000000, 0.9049576633627471889, 1.000000000000000000),
 ( 1.000000000000000000, 0.8998093858009208468, 1.000000000000000000),
 ( 1.000000000000000000, 0.8963317359659079830, 1.000000000000000000),
 ( 1.000000000000000000, 0.8876325024794819996, 1.000000000000000000),
 ( 1.000000000000000000, 0.8824894405370273809, 1.000000000000000000),
 ( 1.000000000000000000, 0.8708860455747078344, 1.000000000000000000),
 ( 1.000000000000000000, 0.8643359190950669069, 1.000000000000000000),
 ( 1.000000000000000000, 0.8432203508677428294, 1.000000000000000000),
 ( 1.000000000000000000, 0.8269334966166562717, 1.000000000000000000),
 ( 1.000000000000000000, 0.8091170061680378334, 1.000000000000000000) ) ) 
 REPRESENTATION_ITEM ( '' )  SURFACE ( )  );
#5211=ORIENTED_EDGE ( 'NONE', *, *, #12218, .F. ) ;
#5212=ADVANCED_FACE ( 'NONE', ( #13637 ), #5207, .F. ) ;
#5216=VERTEX_POINT ( 'NONE', #11495 ) ;
#5224=CARTESIAN_POINT ( 'NONE',  ( 0.8039452708728591634, -0.4429999999999999494, -0.3054822237058766876 ) ) ;
#5227=CARTESIAN_POINT ( 'NONE',  ( 1.324514161726550343, 5.548674798467436505E-05, -0.4812921728568291257 ) ) ;
#5232=VERTEX_POINT ( 'NONE', #10273 ) ;
#5233=CARTESIAN_POINT ( 'NONE',  ( 8.850000000000001421, 0.8819999999999995621, 6.829619984160658046E-17 ) ) ;
#5240=VECTOR ( 'NONE', #7835, 39.37007874015748854 ) ;
#5243=ORIENTED_EDGE ( 'NONE', *, *, #2043, .T. ) ;
#5245=ORIENTED_EDGE ( 'NONE', *, *, #13155, .F. ) ;
#5248=VECTOR ( 'NONE', #5614, 39.37007874015748143 ) ;
#5252=EDGE_LOOP ( 'NONE', ( #3776, #3223, #3735, #11103, #7118, #13802, #3624, #5243 ) ) ;
#5256=EDGE_CURVE ( 'NONE', #8543, #1080, #1009, .T. ) ;
#5262=CARTESIAN_POINT ( 'NONE',  ( 0.9658607511226641185, -0.4371914870459378544, -0.4523269952906700531 ) ) ;
#5264=DIRECTION ( 'NONE',  ( -0.2251194151855826497, -0.9743259920144012876, 0.003179652756858320634 ) ) ;
#5268=DIRECTION ( 'NONE',  ( -0.000000000000000000, 0.000000000000000000, 1.000000000000000000 ) ) ;
#5269=ORIENTED_EDGE ( 'NONE', *, *, #10500, .T. ) ;
#5271=CARTESIAN_POINT ( 'NONE',  ( 0.6566154142300545393, -0.01187121282287852304, 0.4974659767684405653 ) ) ;
#5276=CARTESIAN_POINT ( 'NONE',  ( 8.469665986256828205, 0.9969999999999998863, 6.829619984160658046E-17 ) ) ;
#5278=CIRCLE ( 'NONE', #10418, 0.03999999999999994532 ) ;
#5282=FACE_OUTER_BOUND ( 'NONE', #12594, .T. ) ;
#5287=EDGE_LOOP ( 'NONE', ( #12352, #9149, #13248, #1966 ) ) ;
#5293=EDGE_CURVE ( 'NONE', #14642, #1037, #2063, .T. ) ;
#5302=EDGE_CURVE ( 'NONE', #14113, #8835, #8127, .T. ) ;
#5309=EDGE_LOOP ( 'NONE', ( #2270, #4990, #7526, #4068 ) ) ;
#5310=B_SPLINE_CURVE_WITH_KNOTS ( 'NONE', 3,
 ( #13924, #8138, #4845, #3387, #8066, #9516 ),
 .UNSPECIFIED., .F., .F.,
 ( 4, 2, 4 ),
 ( 0.000000000000000000, 0.0004346861535602710444, 0.0008693723071205420889 ),
 .UNSPECIFIED. ) ;
#5334=CARTESIAN_POINT ( 'NONE',  ( 2.599715518929141211, 0.7930078835987426356, 0.4632808542523846329 ) ) ;
#5335=ORIENTED_EDGE ( 'NONE', *, *, #2088, .F. ) ;
#5340=AXIS2_PLACEMENT_3D ( 'NONE', #4162, #6679, #13622 ) ;
#5343=CARTESIAN_POINT ( 'NONE',  ( 0.6569077226922048762, 0.000000000000000000, -0.4307156577630670280 ) ) ;
#5350=EDGE_CURVE ( 'NONE', #8413, #1274, #13195, .T. ) ;
#5352=CARTESIAN_POINT ( 'NONE',  ( 2.230477600021715912, 0.4287871555018993308, -0.4684960790957384824 ) ) ;
#5367=DIRECTION ( 'NONE',  ( 1.655665450705613915E-16, 0.000000000000000000, 1.000000000000000000 ) ) ;
#5368=ORIENTED_EDGE ( 'NONE', *, *, #7219, .F. ) ;
#5374=EDGE_LOOP ( 'NONE', ( #2846, #2660, #11600, #7880, #14609 ) ) ;
#5378=ORIENTED_EDGE ( 'NONE', *, *, #5350, .F. ) ;
#5381=DIRECTION ( 'NONE',  ( 2.602462600580852055E-17, 1.000000000000000000, -4.814436796019480615E-35 ) ) ;
#5385=CARTESIAN_POINT ( 'NONE',  ( 0.9659751558686909823, -0.4829425875655894429, -0.4106976866094356193 ) ) ;
#5409=DIRECTION ( 'NONE',  ( -0.9992912762382413216, -0.03489602031262312859, -0.01411428356268701854 ) ) ;
#5414=ORIENTED_EDGE ( 'NONE', *, *, #5066, .T. ) ;
#5417=DIRECTION ( 'NONE',  ( 0.4961857140186716753, 0.000000000000000000, -0.8682164115033653706 ) ) ;
#5418=CARTESIAN_POINT ( 'NONE',  ( 0.7067472695984848841, -0.05999999999999994227, -0.5500236785040136800 ) ) ;
#5420=CARTESIAN_POINT ( 'NONE',  ( 8.802840746862891308, 0.9385542876807514423, 0.1899546695978080457 ) ) ;
#5421=CARTESIAN_POINT ( 'NONE',  ( 0.9999999999999993339, -0.4429999999999999494, 0.4258697216429003785 ) ) ;
#5422=CARTESIAN_POINT ( 'NONE',  ( 1.000048944713735732, -0.4428998280398805387, -0.4293350073753851581 ) ) ;
#5428=VERTEX_POINT ( 'NONE', #4572 ) ;
#5438=CARTESIAN_POINT ( 'NONE',  ( 3.470516203624053997, 1.056999999999999718, -0.3909199583802889233 ) ) ;
#5439=CARTESIAN_POINT ( 'NONE',  ( 0.9682282713927263806, -0.4430792971874000230, -0.3432655056157467022 ) ) ;
#5452=VERTEX_POINT ( 'NONE', #9550 ) ;
#5456=EDGE_CURVE ( 'NONE', #8139, #3117, #13958, .T. ) ;
#5458=CARTESIAN_POINT ( 'NONE',  ( 0.9662251482428009242, -0.4440312122665853733, -0.4102559963803746323 ) ) ;
#5461=DIRECTION ( 'NONE',  ( 1.655665450705613915E-16, 3.103226861728128995E-32, 1.000000000000000000 ) ) ;
#5465=CARTESIAN_POINT ( 'NONE',  ( 1.000081574522892591, -0.4828330467331338194, -0.4316451978637083631 ) ) ;
#5469=CARTESIAN_POINT ( 'NONE',  ( 0.7007173259568594270, -0.4032680294360234674, -0.4867265490097360536 ) ) ;
#5473=EDGE_CURVE ( 'NONE', #9898, #15127, #10608, .T. ) ;
#5482=CARTESIAN_POINT ( 'NONE',  ( -0.4424999999999983946, -0.6590000000000000302, -0.3725000000000000533 ) ) ;
#5484=ORIENTED_EDGE ( 'NONE', *, *, #4145, .T. ) ;
#5487=EDGE_CURVE ( 'NONE', #3922, #9279, #3744, .T. ) ;
#5488=ADVANCED_FACE ( 'NONE', ( #2264 ), #479, .T. ) ;
#5496=AXIS2_PLACEMENT_3D ( 'NONE', #4460, #11337, #9127 ) ;
#5501=FACE_OUTER_BOUND ( 'NONE', #6798, .T. ) ;
#5503=ORIENTED_EDGE ( 'NONE', *, *, #6712, .F. ) ;
#5509=AXIS2_PLACEMENT_3D ( 'NONE', #12682, #5735, #12599 ) ;
#5526=CARTESIAN_POINT ( 'NONE',  ( 7.144847001653046861E-17, -0.6334543218446814228, 0.000000000000000000 ) ) ;
#5528=DIRECTION ( 'NONE',  ( 0.000000000000000000, -1.000000000000000000, 0.000000000000000000 ) ) ;
#5539=ORIENTED_EDGE ( 'NONE', *, *, #10356, .F. ) ;
#5540=ORIENTED_EDGE ( 'NONE', *, *, #10810, .F. ) ;
#5541=CARTESIAN_POINT ( 'NONE',  ( 0.3724999999999999423, -0.6290000000000003366, 0.4124999999999999223 ) ) ;
#5557=CARTESIAN_POINT ( 'NONE',  ( 3.601417382415921686, 1.057000000000000162, 0.5000000000000000000 ) ) ;
#5559=DIRECTION ( 'NONE',  ( 0.000000000000000000, 0.000000000000000000, 1.000000000000000000 ) ) ;
#5576=CARTESIAN_POINT ( 'NONE',  ( 2.633526947634466708, 0.3620998228882749692, -0.4033965501631930906 ) ) ;
#5578=ORIENTED_EDGE ( 'NONE', *, *, #9575, .F. ) ;
#5579=VECTOR ( 'NONE', #7287, 39.37007874015748143 ) ;
#5581=( LENGTH_UNIT ( ) NAMED_UNIT ( * ) SI_UNIT ( $, .METRE. ) );
#5592=CARTESIAN_POINT ( 'NONE',  ( 2.230477600021715023, 0.4287871555018993308, -0.4684960790957384824 ) ) ;
#5596=DIRECTION ( 'NONE',  ( 0.03489949670248613384, -0.9993908270190963172, 0.000000000000000000 ) ) ;
#5603=FACE_OUTER_BOUND ( 'NONE', #4755, .T. ) ;
#5608=AXIS2_PLACEMENT_3D ( 'NONE', #5793, #9318, #8172 ) ;
#5613=CARTESIAN_POINT ( 'NONE',  ( 0.6766938413712969558, -0.4746063864208611704, -0.4478646436804322173 ) ) ;
#5614=DIRECTION ( 'NONE',  ( -0.7071067811865342501, -0.7071067811865607844, 0.000000000000000000 ) ) ;
#5625=ORIENTED_EDGE ( 'NONE', *, *, #9407, .T. ) ;
#5628=CARTESIAN_POINT ( 'NONE',  ( 0.7026404547606078799, -0.3911504053871472375, -0.4896627279036659397 ) ) ;
#5630=CARTESIAN_POINT ( 'NONE',  ( 0.8896579858124370466, -0.4298343112707130875, -0.4649362184193211456 ) ) ;
#5640=CARTESIAN_POINT ( 'NONE',  ( 0.8999999999999999112, -0.6429999999999999050, -0.3750000000000000555 ) ) ;
#5647=CARTESIAN_POINT ( 'NONE',  ( 0.7007157546338746990, -0.03969898687429768841, -0.4867155808989070409 ) ) ;
#5648=CARTESIAN_POINT ( 'NONE',  ( 8.661818191809109280, 0.8754285464536269989, -0.3176815264168135200 ) ) ;
#5650=DIRECTION ( 'NONE',  ( -0.9999002670844989726, 0.000000000000000000, -0.01412288512831212997 ) ) ;
#5656=ORIENTED_EDGE ( 'NONE', *, *, #2507, .T. ) ;
#5660=DIRECTION ( 'NONE',  ( 1.000000000000000000, 1.874307916738609066E-16, 0.000000000000000000 ) ) ;
#5665=PLANE ( 'NONE',  #14486 ) ;
#5667=CARTESIAN_POINT ( 'NONE',  ( 3.429441573760528161, -0.4329758086553958107, 0.5000000000000000000 ) ) ;
#5677=DIRECTION ( 'NONE',  ( 0.000000000000000000, -1.000000000000000000, 0.000000000000000000 ) ) ;
#5680=CARTESIAN_POINT ( 'NONE',  ( 3.025735579118526974, 0.6832920890234898126, -0.4572636217638627043 ) ) ;
#5683=CARTESIAN_POINT ( 'NONE',  ( 0.7010312871322603723, -0.4463509627415067071, -0.4267273516602834160 ) ) ;
#5686=CARTESIAN_POINT ( 'NONE',  ( 0.9672769954795885639, -0.4829975555521403008, -0.4081482409674996870 ) ) ;
#5687=ORIENTED_EDGE ( 'NONE', *, *, #9706, .F. ) ;
#5691=EDGE_CURVE ( 'NONE', #11839, #5850, #14010, .T. ) ;
#5692=CARTESIAN_POINT ( 'NONE',  ( 0.3724999999999999423, 0.1859999999999983611, 0.3724999999999999423 ) ) ;
#5695=AXIS2_PLACEMENT_3D ( 'NONE', #15089, #5991, #4620 ) ;
#5698=CARTESIAN_POINT ( 'NONE',  ( 3.319863249854034581, 0.6888833692903483241, 0.3931858364370117709 ) ) ;
#5700=CARTESIAN_POINT ( 'NONE',  ( 0.8359884731686543224, -0.4372643507807087992, -0.4540055247929744575 ) ) ;
#5703=( BOUNDED_SURFACE ( )  B_SPLINE_SURFACE ( 3, 2, ( 
 ( #13728, #6946, #11683 ),
 ( #10379, #6792, #5718 ),
 ( #13957, #12580, #2106 ),
 ( #13804, #3263, #12664 ),
 ( #3494, #7933, #10456 ),
 ( #15043, #14967, #4571 ),
 ( #3338, #8097, #13878 ),
 ( #2025, #4648, #11451 ),
 ( #4489, #9160, #6874 ),
 ( #15117, #3421, #5647 ),
 ( #2190, #9238, #3196 ),
 ( #4422, #14815, #1106 ),
 ( #10306, #8014, #12738 ),
 ( #13661, #11527, #2263 ) ),
 .UNSPECIFIED., .F., .F., .T. ) 
 B_SPLINE_SURFACE_WITH_KNOTS ( ( 4, 2, 2, 2, 2, 2, 4 ),
 ( 3, 3 ),
 ( 0.001551397270042531020, 0.002805300020215382474, 0.004059202770388233711, 0.004686154145474659763, 0.005313105520561085815, 0.005940056895647511867, 0.006567008270733937052 ),
 ( 0.000000000000000000, 1.000000000000000000 ),
 .UNSPECIFIED. ) 
 GEOMETRIC_REPRESENTATION_ITEM ( )  RATIONAL_B_SPLINE_SURFACE ( (
 ( 1.000000000000000000, 0.8091170061680381664, 1.000000000000000000),
 ( 1.000000000000000000, 0.8270513381945645559, 1.000000000000000000),
 ( 1.000000000000000000, 0.8430705034768221084, 1.000000000000000000),
 ( 1.000000000000000000, 0.8715016528490074910, 1.000000000000000000),
 ( 1.000000000000000000, 0.8830758126916298245, 1.000000000000000000),
 ( 1.000000000000000000, 0.8962350306362059094, 1.000000000000000000),
 ( 1.000000000000000000, 0.8997443014200150468, 1.000000000000000000),
 ( 1.000000000000000000, 0.9049100909109204505, 1.000000000000000000),
 ( 1.000000000000000000, 0.9065649576647841767, 1.000000000000000000),
 ( 1.000000000000000000, 0.9077684922225311981, 1.000000000000000000),
 ( 1.000000000000000000, 0.9073563424325319371, 1.000000000000000000),
 ( 1.000000000000000000, 0.9044691270900298008, 1.000000000000000000),
 ( 1.000000000000000000, 0.9020443801113525728, 1.000000000000000000),
 ( 1.000000000000000000, 0.8987017906623396835, 1.000000000000000000) ) ) 
 REPRESENTATION_ITEM ( '' )  SURFACE ( )  );
#5709=CARTESIAN_POINT ( 'NONE',  ( 3.389333715882079101, 0.6913093314209972640, 0.3921516461332968939 ) ) ;
#5710=VERTEX_POINT ( 'NONE', #12787 ) ;
#5711=DIRECTION ( 'NONE',  ( -0.000000000000000000, 1.000000000000000000, 0.000000000000000000 ) ) ;
#5713=CARTESIAN_POINT ( 'NONE',  ( 0.8051298376193415374, -0.4429999999999779670, -0.3049516186061956291 ) ) ;
#5718=CARTESIAN_POINT ( 'NONE',  ( 0.7429169091363049260, -3.303005800603283850E-18, -0.4367090053325354271 ) ) ;
#5721=AXIS2_PLACEMENT_3D ( 'NONE', #5526, #14924, #2058 ) ;
#5726=ORIENTED_EDGE ( 'NONE', *, *, #12761, .T. ) ;
#5731=ORIENTED_EDGE ( 'NONE', *, *, #14562, .T. ) ;
#5735=DIRECTION ( 'NONE',  ( -1.874307916738608820E-16, 1.000000000000000000, 0.000000000000000000 ) ) ;
#5740=LINE ( 'NONE', #12526, #9395 ) ;
#5741=CARTESIAN_POINT ( 'NONE',  ( 8.476283996537762988, 0.8689495495877206377, 0.3203020658980471613 ) ) ;
#5747=PLANE ( 'NONE',  #9929 ) ;
#5750=CARTESIAN_POINT ( 'NONE',  ( 1.000847373107698779, -0.3829999999999998961, -0.4858637376679703634 ) ) ;
#5753=CIRCLE ( 'NONE', #12085, 0.05999999999999995615 ) ;
#5756=CARTESIAN_POINT ( 'NONE',  ( 1.645138957953503622, -0.3406142803323702895, 0.4767635740404712053 ) ) ;
#5760=CARTESIAN_POINT ( 'NONE',  ( 0.6729652567417304665, -0.4032054944085891601, 0.4872362964973896982 ) ) ;
#5761=DIRECTION ( 'NONE',  ( 0.01412288512831583534, 0.000000000000000000, 0.9999002670844989726 ) ) ;
#5763=AXIS2_PLACEMENT_3D ( 'NONE', #6277, #13067, #13143 ) ;
#5764=ORIENTED_EDGE ( 'NONE', *, *, #7399, .F. ) ;
#5765=LINE ( 'NONE', #2075, #9912 ) ;
#5766=EDGE_LOOP ( 'NONE', ( #13849, #486, #5, #9361 ) ) ;
#5773=CARTESIAN_POINT ( 'NONE',  ( 1.645138957954975778, -0.3406142803326386859, -0.4767635740401386935 ) ) ;
#5780=ORIENTED_EDGE ( 'NONE', *, *, #1553, .T. ) ;
#5782=ORIENTED_EDGE ( 'NONE', *, *, #4248, .F. ) ;
#5785=EDGE_CURVE ( 'NONE', #6053, #10522, #2965, .T. ) ;
#5786=DIRECTION ( 'NONE',  ( 0.000000000000000000, 0.000000000000000000, 1.000000000000000000 ) ) ;
#5788=CARTESIAN_POINT ( 'NONE',  ( -0.3725000000000000533, 0.2159999999999999420, 0.4425000000000003930 ) ) ;
#5792=AXIS2_PLACEMENT_3D ( 'NONE', #173, #11594, #10450 ) ;
#5793=CARTESIAN_POINT ( 'NONE',  ( 2.591520038054473840, 0.4049457270506677253, 0.4033906250602100618 ) ) ;
#5794=( BOUNDED_CURVE ( )  B_SPLINE_CURVE ( 3, ( #2699, #4999, #9803, #13225 ),
 .UNSPECIFIED., .F., .F. ) 
 B_SPLINE_CURVE_WITH_KNOTS ( ( 4, 4 ),
 ( 1.572344395910955761, 2.356194490192339952 ),
 .UNSPECIFIED. ) 
 CURVE ( )  GEOMETRIC_REPRESENTATION_ITEM ( )  RATIONAL_B_SPLINE_CURVE ( ( 1.000000000000000000, 0.9494503106142797577, 0.9494503106142797577, 1.000000000000000000 ) ) 
 REPRESENTATION_ITEM ( '' )  );
#5796=EDGE_CURVE ( 'NONE', #8103, #15092, #574, .T. ) ;
#5801=ORIENTED_EDGE ( 'NONE', *, *, #4700, .T. ) ;
#5808=ORIENTED_EDGE ( 'NONE', *, *, #7281, .F. ) ;
#5814=CARTESIAN_POINT ( 'NONE',  ( 2.045495128834867504, 0.3295048711651357154, 0.5000000000000000000 ) ) ;
#5817=CARTESIAN_POINT ( 'NONE',  ( 8.849999999999999645, -0.4430000000000001714, 0.3750000000000000555 ) ) ;
#5821=AXIS2_PLACEMENT_3D ( 'NONE', #7091, #6084, #86 ) ;
#5823=ADVANCED_FACE ( 'NONE', ( #1414 ), #2433, .F. ) ;
#5824=LINE ( 'NONE', #9187, #6083 ) ;
#5826=CIRCLE ( 'NONE', #9489, 0.07500000000000002498 ) ;
#5830=DIRECTION ( 'NONE',  ( -1.000000000000000000, 0.000000000000000000, 0.000000000000000000 ) ) ;
#5834=CARTESIAN_POINT ( 'NONE',  ( 0.6566521509169384041, -0.01162981109769697236, -0.4973154343666586485 ) ) ;
#5838=CIRCLE ( 'NONE', #9749, 0.8083085967350902568 ) ;
#5847=CARTESIAN_POINT ( 'NONE',  ( 0.6610203958102930377, -0.4494184719130550065, 0.4833908188384043458 ) ) ;
#5848=DIRECTION ( 'NONE',  ( 0.9999002670844991947, 0.000000000000000000, -0.01412288512831213171 ) ) ;
#5850=VERTEX_POINT ( 'NONE', #1335 ) ;
#5859=CARTESIAN_POINT ( 'NONE',  ( 1.000847373107695226, -0.3830000000000000071, -0.4858637376679705855 ) ) ;
#5862=DIRECTION ( 'NONE',  ( -1.874307916738606601E-16, 1.000000000000000000, 0.000000000000000000 ) ) ;
#5866=EDGE_LOOP ( 'NONE', ( #11344, #10974, #8620, #14954 ) ) ;
#5871=CARTESIAN_POINT ( 'NONE',  ( 1.522243911113194015, -0.3830000000000001181, 0.4784993797865367826 ) ) ;
#5875=CARTESIAN_POINT ( 'NONE',  ( 0.8083085967350902568, 0.04143956043956045082, 0.000000000000000000 ) ) ;
#5876=DIRECTION ( 'NONE',  ( -0.000000000000000000, -1.000000000000000000, -0.000000000000000000 ) ) ;
#5877=CARTESIAN_POINT ( 'NONE',  ( -0.3725000000000000533, 0.2159999999999999698, 0.4124999999999999223 ) ) ;
#5887=ADVANCED_FACE ( 'NONE', ( #4252 ), #12272, .T. ) ;
#5891=VERTEX_POINT ( 'NONE', #7468 ) ;
#5895=ORIENTED_EDGE ( 'NONE', *, *, #4844, .F. ) ;
#5898=DIRECTION ( 'NONE',  ( 0.7071067811865336949, 0.7071067811865612285, 0.000000000000000000 ) ) ;
#5907=CARTESIAN_POINT ( 'NONE',  ( 0.6569077226922027668, -0.4429999999999999494, 0.4307156577630670280 ) ) ;
#5910=EDGE_CURVE ( 'NONE', #7869, #251, #13415, .T. ) ;
#5914=ADVANCED_FACE ( 'NONE', ( #10984 ), #6396, .F. ) ;
#5916=CARTESIAN_POINT ( 'NONE',  ( 8.475037399843312613, 0.8689060174719044349, -0.3802960819231170908 ) ) ;
#5925=CARTESIAN_POINT ( 'NONE',  ( 0.7513246802501660770, 0.000000000000000000, 0.4293820849162031661 ) ) ;
#5927=CARTESIAN_POINT ( 'NONE',  ( 0.6412116890856961460, -0.6589999999999996971, 7.852578426146655751E-17 ) ) ;
#5929=FACE_OUTER_BOUND ( 'NONE', #3868, .T. ) ;
#5933=EDGE_LOOP ( 'NONE', ( #4127, #11096, #10229, #5335, #12747, #3054 ) ) ;
#5938=CARTESIAN_POINT ( 'NONE',  ( 0.8553300727722267238, -0.4749930492489788381, -0.4355902931210492435 ) ) ;
#5949=ORIENTED_EDGE ( 'NONE', *, *, #12761, .F. ) ;
#5960=ORIENTED_EDGE ( 'NONE', *, *, #13414, .F. ) ;
#5970=DIRECTION ( 'NONE',  ( 0.000000000000000000, -1.000000000000000000, 0.000000000000000000 ) ) ;
#5974=CARTESIAN_POINT ( 'NONE',  ( 2.045495128834867060, 0.3295048711651353268, -0.4105035982572215469 ) ) ;
#5975=DIRECTION ( 'NONE',  ( -0.9999002670844989726, -1.365787769249574676E-16, 0.01412288512831212997 ) ) ;
#5981=CARTESIAN_POINT ( 'NONE',  ( 2.644772327657329836, 0.4573506435455682584, 0.4626444586489077415 ) ) ;
#5982=VERTEX_POINT ( 'NONE', #224 ) ;
#5991=DIRECTION ( 'NONE',  ( -5.190764794801482736E-21, -1.000000000000000000, -3.675061474719450755E-19 ) ) ;
#6003=CARTESIAN_POINT ( 'NONE',  ( 1.886302412727347999, -0.2406659208691243612, -0.4137268778527457558 ) ) ;
#6008=EDGE_CURVE ( 'NONE', #7355, #13657, #5740, .T. ) ;
#6009=ADVANCED_FACE ( 'NONE', ( #9415 ), #13824, .T. ) ;
#6014=AXIS2_PLACEMENT_3D ( 'NONE', #6998, #10130, #14784 ) ;
#6015=DIRECTION ( 'NONE',  ( -1.000000000000000000, -1.874307916738609066E-16, 0.000000000000000000 ) ) ;
#6019=CARTESIAN_POINT ( 'NONE',  ( 0.7023896125859220296, -0.05117280967830968585, -0.4896155492289063216 ) ) ;
#6024=B_SPLINE_CURVE_WITH_KNOTS ( 'NONE', 3,
 ( #11642, #13837, #3377, #11560, #1144, #15078, #4604, #5834, #6709, #3914, #8507, #8578, #8367, #4988 ),
 .UNSPECIFIED., .F., .F.,
 ( 4, 2, 2, 2, 2, 2, 4 ),
 ( 0.000000000000000000, 0.001176052134299114061, 0.002352104268598228121, 0.002940130335747782441, 0.003528156402897335894, 0.004116182470046890647, 0.004704208537196444967 ),
 .UNSPECIFIED. ) ;
#6026=CARTESIAN_POINT ( 'NONE',  ( 1.541692889559683088, 0.03598127022577170264, -0.4179989611390685922 ) ) ;
#6027=ADVANCED_FACE ( 'NONE', ( #14056, #1129 ), #5665, .F. ) ;
#6039=CARTESIAN_POINT ( 'NONE',  ( 0.9991526268923013321, -0.4429999999999998939, -0.4258816901896192997 ) ) ;
#6040=CARTESIAN_POINT ( 'NONE',  ( -0.7287617923574205570, 0.2159999999999999420, -0.8499999999999999778 ) ) ;
#6041=CARTESIAN_POINT ( 'NONE',  ( 0.3724999999999997757, 0.2159999999999999420, -0.4425000000000005596 ) ) ;
#6045=CARTESIAN_POINT ( 'NONE',  ( 8.526344538924147898, 0.8706977022493568308, 0.3793004607997266797 ) ) ;
#6052=FACE_OUTER_BOUND ( 'NONE', #5252, .T. ) ;
#6053=VERTEX_POINT ( 'NONE', #9180 ) ;
#6057=CARTESIAN_POINT ( 'NONE',  ( 2.855088541747415221, 0.5369222675350757701, 0.4596738906534074132 ) ) ;
#6064=CIRCLE ( 'NONE', #12166, 0.06000000000000001166 ) ;
#6069=CARTESIAN_POINT ( 'NONE',  ( 0.6766392826275051675, -0.4261666590922867370, 0.4729147972023082236 ) ) ;
#6072=ORIENTED_EDGE ( 'NONE', *, *, #1676, .F. ) ;
#6078=APPLICATION_CONTEXT ( 'automotive_design' ) ;
#6083=VECTOR ( 'NONE', #10409, 39.37007874015748143 ) ;
#6084=DIRECTION ( 'NONE',  ( -0.000000000000000000, 1.000000000000000000, -0.000000000000000000 ) ) ;
#6088=FACE_OUTER_BOUND ( 'NONE', #12976, .T. ) ;
#6092=AXIS2_PLACEMENT_3D ( 'NONE', #10803, #4924, #8443 ) ;
#6095=CARTESIAN_POINT ( 'NONE',  ( 1.004574810408579433, -0.4429999999999998384, -0.3264278243218214359 ) ) ;
#6105=ADVANCED_FACE ( 'NONE', ( #9340 ), #13977, .T. ) ;
#6106=CARTESIAN_POINT ( 'NONE',  ( 1.814459835756555783, 0.1490781312163585171, 0.4743720362179413286 ) ) ;
#6112=CARTESIAN_POINT ( 'NONE',  ( 0.7007556580885034858, -0.4010748535711006202, -0.4875099722676211056 ) ) ;
#6114=EDGE_LOOP ( 'NONE', ( #9028, #8404, #4582, #4918, #7456 ) ) ;
#6128=CARTESIAN_POINT ( 'NONE',  ( 0.8232171895119964056, -0.4398285061085906444, -0.4481849241520746152 ) ) ;
#6132=CARTESIAN_POINT ( 'NONE',  ( 0.6733268703976357239, -0.4720969008048874760, 0.4545075337565439577 ) ) ;
#6138=DIRECTION ( 'NONE',  ( -1.000000000000000000, -0.000000000000000000, -0.000000000000000000 ) ) ;
#6162=ORIENTED_EDGE ( 'NONE', *, *, #9430, .F. ) ;
#6165=CARTESIAN_POINT ( 'NONE',  ( 8.526344538923749994, 0.8706977022493430640, -0.3793004607997343958 ) ) ;
#6167=CARTESIAN_POINT ( 'NONE',  ( 0.8108060929038570785, -0.4429999999999998939, -0.3024090436974096185 ) ) ;
#6174=CARTESIAN_POINT ( 'NONE',  ( -0.7287617923574205570, 0.2159999999999999420, 0.4425000000000005596 ) ) ;
#6176=ORIENTED_EDGE ( 'NONE', *, *, #8011, .T. ) ;
#6178=CARTESIAN_POINT ( 'NONE',  ( 0.7006934119264053296, -0.4055938261068608996, -0.4858827016952778632 ) ) ;
#6187=ORIENTED_EDGE ( 'NONE', *, *, #3326, .T. ) ;
#6188=CARTESIAN_POINT ( 'NONE',  ( -0.4125000000000001998, 0.2159999999999999698, -0.3725000000000000533 ) ) ;
#6193=CARTESIAN_POINT ( 'NONE',  ( 0.8575369771065451951, -0.4333177464522090516, -0.4606414905107603652 ) ) ;
#6203=VERTEX_POINT ( 'NONE', #1917 ) ;
#6204=TOROIDAL_SURFACE ( 'NONE', #14741, 0.1150000000000000050, 0.04000000000000000083 ) ;
#6205=DIRECTION ( 'NONE',  ( 1.655665450705613915E-16, 3.103226861728128995E-32, 1.000000000000000000 ) ) ;
#6211=CARTESIAN_POINT ( 'NONE',  ( 0.6782188896242594689, -0.01324371508926007121, 0.4691064452754763470 ) ) ;
#6214=ORIENTED_EDGE ( 'NONE', *, *, #11883, .F. ) ;
#6221=CARTESIAN_POINT ( 'NONE',  ( 0.7238317330277964645, -0.005069019069653440263, 0.4548041668469371412 ) ) ;
#6226=CARTESIAN_POINT ( 'NONE',  ( 0.8254245316410399047, -0.4429999999999996163, -0.3670313414528083573 ) ) ;
#6230=ADVANCED_FACE ( 'NONE', ( #4231 ), #2166, .T. ) ;
#6253=ORIENTED_EDGE ( 'NONE', *, *, #12679, .T. ) ;
#6261=CARTESIAN_POINT ( 'NONE',  ( 2.715751415184836315, 0.8549853309850858896, 0.4616419291641825073 ) ) ;
#6270=ADVANCED_FACE ( 'NONE', ( #2028 ), #11553, .T. ) ;
#6271=CARTESIAN_POINT ( 'NONE',  ( 0.8336852985356731915, -0.4829999999999998739, -0.4100337033397443709 ) ) ;
#6276=ORIENTED_EDGE ( 'NONE', *, *, #364, .F. ) ;
#6277=CARTESIAN_POINT ( 'NONE',  ( 1.000000000000000222, -0.4829999999999998739, -0.3182109165419976238 ) ) ;
#6286=CARTESIAN_POINT ( 'NONE',  ( 0.8999999999999999112, -0.6230000000000016636, -0.4500000000000000666 ) ) ;
#6290=CARTESIAN_POINT ( 'NONE',  ( 0.7117500205948168457, -0.01337125625712030051, 0.4679153652930429508 ) ) ;
#6292=ORIENTED_EDGE ( 'NONE', *, *, #3534, .T. ) ;
#6294=CIRCLE ( 'NONE', #14830, 0.8499999999999999778 ) ;
#6295=CARTESIAN_POINT ( 'NONE',  ( -0.4425000000000007261, 0.2159999999999999420, -0.8499999999999999778 ) ) ;
#6302=CARTESIAN_POINT ( 'NONE',  ( 0.3724999999999999423, 0.2159999999999999698, 0.3724999999999999423 ) ) ;
#6308=CIRCLE ( 'NONE', #9969, 0.3203340137431719414 ) ;
#6312=ORIENTED_EDGE ( 'NONE', *, *, #7399, .T. ) ;
#6323=CARTESIAN_POINT ( 'NONE',  ( 0.4124999999999997558, 0.1859999999999983611, -0.4125000000000000333 ) ) ;
#6331=AXIS2_PLACEMENT_3D ( 'NONE', #6040, #1350, #11778 ) ;
#6349=CARTESIAN_POINT ( 'NONE',  ( 0.8336852985356729695, -0.4430000000000001714, -0.4100337033397444264 ) ) ;
#6354=ORIENTED_EDGE ( 'NONE', *, *, #14567, .T. ) ;
#6355=DIRECTION ( 'NONE',  ( 1.000000000000000000, -2.602462600580851747E-17, 0.000000000000000000 ) ) ;
#6360=CARTESIAN_POINT ( 'NONE',  ( 2.187203820042824542, 0.4712135623730921985, -0.4085020630706684974 ) ) ;
#6366=CARTESIAN_POINT ( 'NONE',  ( 0.7241094260644624914, -0.005263640177536527999, 0.4546250289485997964 ) ) ;
#6369=CARTESIAN_POINT ( 'NONE',  ( 0.6601485485260571995, -0.07064835164835162051, -0.5137583810202324131 ) ) ;
#6373=ORIENTED_EDGE ( 'NONE', *, *, #1065, .F. ) ;
#6379=CARTESIAN_POINT ( 'NONE',  ( 0.7982897726210904654, -0.4436723967305212235, -0.3090191557806227785 ) ) ;
#6389=CARTESIAN_POINT ( 'NONE',  ( 8.670688874134334867, 0.8757383175063406799, -0.2544954840226750781 ) ) ;
#6396=PLANE ( 'NONE',  #10538 ) ;
#6400=ORIENTED_EDGE ( 'NONE', *, *, #6008, .T. ) ;
#6406=CARTESIAN_POINT ( 'NONE',  ( 0.3724999999999997757, -0.6290000000000003366, -0.3725000000000000533 ) ) ;
#6412=CARTESIAN_POINT ( 'NONE',  ( 0.9254934464156098217, -0.4652881421103379767, -0.4458518134710270919 ) ) ;
#6425=CARTESIAN_POINT ( 'NONE',  ( 0.6653056208004448635, 0.01642763638135510268, 0.4725671546919802957 ) ) ;
#6426=( NAMED_UNIT ( * ) SI_UNIT ( $, .STERADIAN. ) SOLID_ANGLE_UNIT ( ) );
#6430=LINE ( 'NONE', #6657, #13627 ) ;
#6433=CARTESIAN_POINT ( 'NONE',  ( 0.6732025385091793268, -0.04517367991929972099, 0.4888865340280583727 ) ) ;
#6434=CARTESIAN_POINT ( 'NONE',  ( 0.9705801008103163152, -0.4829849771478168519, -0.3489154846764306872 ) ) ;
#6436=CARTESIAN_POINT ( 'NONE',  ( 2.807059454666800402, 0.6196377705552925663, 0.4603522675894519689 ) ) ;
#6451=CARTESIAN_POINT ( 'NONE',  ( 0.8337711728933204780, -0.4835921594977613536, -0.3396201722514596288 ) ) ;
#6460=CIRCLE ( 'NONE', #9146, 0.07500000000000002498 ) ;
#6461=DIRECTION ( 'NONE',  ( 0.000000000000000000, 0.000000000000000000, -1.000000000000000000 ) ) ;
#6463=CARTESIAN_POINT ( 'NONE',  ( 0.6412116890856961460, -0.6589999999999996971, 8.478919399169820819E-17 ) ) ;
#6464=CARTESIAN_POINT ( 'NONE',  ( 2.599160627732593376, 0.7974701832127791823, 0.4632886916986920789 ) ) ;
#6472=ORIENTED_EDGE ( 'NONE', *, *, #236, .T. ) ;
#6483=DIRECTION ( 'NONE',  ( 0.03489949670249522379, -0.9993908270190959842, 0.000000000000000000 ) ) ;
#6488=CARTESIAN_POINT ( 'NONE',  ( 8.849999999999999645, 0.9399413264884247665, 6.829619984160658046E-17 ) ) ;
#6489=AXIS2_PLACEMENT_3D ( 'NONE', #5276, #1740, #10101 ) ;
#6491=CARTESIAN_POINT ( 'NONE',  ( 0.9618623841134203989, -0.4823031615770373981, -0.4179641926583888001 ) ) ;
#6495=ORIENTED_EDGE ( 'NONE', *, *, #10574, .F. ) ;
#6496=CARTESIAN_POINT ( 'NONE',  ( 0.3724999999999999423, -0.6590000000000000302, 0.4124999999999999223 ) ) ;
#6499=CARTESIAN_POINT ( 'NONE',  ( 0.8999999999999999112, -0.6429999999999999050, -0.3750000000000000555 ) ) ;
#6503=FACE_OUTER_BOUND ( 'NONE', #3409, .T. ) ;
#6506=VECTOR ( 'NONE', #12653, 39.37007874015748143 ) ;
#6509=CARTESIAN_POINT ( 'NONE',  ( 2.187631780374527324, 0.4716415227047954795, -0.4691012460399074380 ) ) ;
#6510=CARTESIAN_POINT ( 'NONE',  ( 1.003096136995459631, -0.4429976034824906761, -0.4258273028168332863 ) ) ;
#6511=ORIENTED_EDGE ( 'NONE', *, *, #11090, .T. ) ;
#6516=CARTESIAN_POINT ( 'NONE',  ( 0.7176122613104018999, -0.4347745074854311165, 0.4611624156322181034 ) ) ;
#6522=CONICAL_SURFACE ( 'NONE', #10432, 0.6412116890856960350, 1.326062729686469988 ) ;
#6524=EDGE_CURVE ( 'NONE', #3025, #3922, #6955, .T. ) ;
#6527=CARTESIAN_POINT ( 'NONE',  ( 0.7859940414473148840, -0.4452037809602719665, -0.3216753057612609656 ) ) ;
#6529=CARTESIAN_POINT ( 'NONE',  ( 0.9666439951188899871, -0.4829990579840729437, -0.4094329656214278912 ) ) ;
#6530=VERTEX_POINT ( 'NONE', #7962 ) ;
#6539=DIRECTION ( 'NONE',  ( 0.000000000000000000, 0.000000000000000000, -1.000000000000000000 ) ) ;
#6543=CARTESIAN_POINT ( 'NONE',  ( 0.7009834207394823880, -0.3992359203334029383, -0.4880078140243664930 ) ) ;
#6547=VECTOR ( 'NONE', #14405, 39.37007874015748854 ) ;
#6549=AXIS2_PLACEMENT_3D ( 'NONE', #4683, #10794, #3836 ) ;
#6557=LINE ( 'NONE', #11217, #11530 ) ;
#6559=CIRCLE ( 'NONE', #10226, 0.03999999999999998695 ) ;
#6560=EDGE_CURVE ( 'NONE', #10623, #7355, #13763, .T. ) ;
#6563=CARTESIAN_POINT ( 'NONE',  ( 0.7067472695984847730, -0.05999999999999996309, 0.5500236785040135690 ) ) ;
#6564=CARTESIAN_POINT ( 'NONE',  ( 8.849152626892301754, -0.3829999999999988414, 0.3150059839749300705 ) ) ;
#6569=MECHANICAL_DESIGN_GEOMETRIC_PRESENTATION_REPRESENTATION('',(#10969),#12668);
#6570=DIRECTION ( 'NONE',  ( -0.9999002670844989726, -0.000000000000000000, -0.01412288512831212997 ) ) ;
#6572=CARTESIAN_POINT ( 'NONE',  ( 0.8920597045391224222, -0.4611706669540619474, -0.4498866585187662470 ) ) ;
#6576=ORIENTED_EDGE ( 'NONE', *, *, #12725, .F. ) ;
#6578=ORIENTED_EDGE ( 'NONE', *, *, #12613, .F. ) ;
#6587=DIRECTION ( 'NONE',  ( -0.000000000000000000, -0.000000000000000000, -1.000000000000000000 ) ) ;
#6588=VECTOR ( 'NONE', #7252, 39.37007874015748143 ) ;
#6592=CARTESIAN_POINT ( 'NONE',  ( 3.388933043275772494, 0.7513023213622327390, 0.4521337140780258279 ) ) ;
#6606=CARTESIAN_POINT ( 'NONE',  ( 2.219979583768778131, -0.03321525116820610996, 0.4091553120912245212 ) ) ;
#6613=CARTESIAN_POINT ( 'NONE',  ( 0.7020310496751531737, -0.4139656494879343507, -0.4816878228448813193 ) ) ;
#6622=CARTESIAN_POINT ( 'NONE',  ( 0.7022453151856608011, -0.4144781913240899729, -0.4813241942165185638 ) ) ;
#6628=B_SPLINE_CURVE_WITH_KNOTS ( 'NONE', 3,
 ( #11676, #13030, #1101, #1252, #5938, #8092, #1179, #175, #7021, #12733, #2258, #3722, #25, #3488, #14187, #8167, #11595, #2340, #2494, #10601 ),
 .UNSPECIFIED., .F., .F.,
 ( 4, 2, 2, 2, 2, 2, 2, 2, 2, 4 ),
 ( 0.000000000000000000, 0.0005275929577467031390, 0.001055185915493406278, 0.001582778873240109525, 0.002110371830986812556, 0.002374168309860159084, 0.002637964788733505178, 0.003165557746480196499, 0.003693150704226888254, 0.004220743661973579142 ),
 .UNSPECIFIED. ) ;
#6630=ORIENTED_EDGE ( 'NONE', *, *, #11883, .T. ) ;
#6635=LINE ( 'NONE', #13570, #3408 ) ;
#6638=CARTESIAN_POINT ( 'NONE',  ( 3.102108017520303740, 0.6812791890164018316, 0.3964255093850733713 ) ) ;
#6643=CARTESIAN_POINT ( 'NONE',  ( 0.9056315879401858338, -0.4606766705580153110, -0.4500955733274891180 ) ) ;
#6651=EDGE_LOOP ( 'NONE', ( #14747, #11543, #9126, #732 ) ) ;
#6655=ORIENTED_EDGE ( 'NONE', *, *, #1283, .F. ) ;
#6657=CARTESIAN_POINT ( 'NONE',  ( 2.088340948482054316, 0.2866505039622389006, 0.4705036589197449937 ) ) ;
#6658=LINE ( 'NONE', #13519, #1089 ) ;
#6659=CARTESIAN_POINT ( 'NONE',  ( 0.9719779994246295907, -0.4829746353139036663, -0.3969404040289119528 ) ) ;
#6667=CARTESIAN_POINT ( 'NONE',  ( 0.7096982392392976458, -0.4275148688008855724, 0.4703908291968755262 ) ) ;
#6671=CARTESIAN_POINT ( 'NONE',  ( 0.9708583742000757022, -0.4829832308505582206, -0.3495890805477908647 ) ) ;
#6675=CARTESIAN_POINT ( 'NONE',  ( 2.702105678820072132, 0.5048229836667897930, -0.4618346655533888123 ) ) ;
#6676=CARTESIAN_POINT ( 'NONE',  ( 0.6922886459387327385, -0.4439147467600604857, -0.4416098182902895575 ) ) ;
#6679=DIRECTION ( 'NONE',  ( -1.365923996832131609E-16, 1.000000000000000000, 0.000000000000000000 ) ) ;
#6683=CARTESIAN_POINT ( 'NONE',  ( 0.7174986153957904067, -0.4347107752510870893, -0.4612806347796395978 ) ) ;
#6704=CARTESIAN_POINT ( 'NONE',  ( 0.7827579871403669287, -0.4452001257954049107, -0.3294746359414947312 ) ) ;
#6706=EDGE_LOOP ( 'NONE', ( #11027, #10793, #11863, #6725, #10569 ) ) ;
#6709=CARTESIAN_POINT ( 'NONE',  ( 0.6558215032554000068, -0.01848230360567671218, -0.5012403847680007019 ) ) ;
#6712=EDGE_CURVE ( 'NONE', #2844, #10000, #14020, .T. ) ;
#6714=CARTESIAN_POINT ( 'NONE',  ( 0.8874725658679039064, -0.4299024001883317569, -0.4648823484497104364 ) ) ;
#6721=B_SPLINE_CURVE_WITH_KNOTS ( 'NONE', 3,
 ( #4342, #2345, #7026, #9014 ),
 .UNSPECIFIED., .F., .F.,
 ( 4, 4 ),
 ( 0.000000000000000000, 0.0001180456142323141122 ),
 .UNSPECIFIED. ) ;
#6725=ORIENTED_EDGE ( 'NONE', *, *, #9608, .F. ) ;
#6727=EDGE_CURVE ( 'NONE', #14371, #13066, #9935, .T. ) ;
#6737=CARTESIAN_POINT ( 'NONE',  ( 2.280218097288460033, 0.5641718375784713357, -0.4677935297007478344 ) ) ;
#6738=CARTESIAN_POINT ( 'NONE',  ( 0.9672769954795883418, -0.4829975555521405228, -0.4081482409675000200 ) ) ;
#6742=CARTESIAN_POINT ( 'NONE',  ( 2.591520038054473840, 0.4049457270506677808, -0.4033906250602100618 ) ) ;
#6748=ORIENTED_EDGE ( 'NONE', *, *, #13237, .T. ) ;
#6749=CIRCLE ( 'NONE', #8954, 0.06999999999999836908 ) ;
#6753=FACE_OUTER_BOUND ( 'NONE', #4751, .T. ) ;
#6757=CARTESIAN_POINT ( 'NONE',  ( 0.7073825753665241578, -0.4455853224013471836, -0.4167523536742555601 ) ) ;
#6759=CARTESIAN_POINT ( 'NONE',  ( 0.7513246802501661881, 0.000000000000000000, -0.4293820849162031661 ) ) ;
#6764=DIRECTION ( 'NONE',  ( -0.7071067811865350272, 0.7071067811865600072, 0.000000000000000000 ) ) ;
#6770=CARTESIAN_POINT ( 'NONE',  ( 0.6844575745811062317, -0.4385969160104463138, -0.4560057122457037981 ) ) ;
#6774=CARTESIAN_POINT ( 'NONE',  ( 0.9618941676350062364, -0.4364129403843365895, -0.4539147763481607978 ) ) ;
#6776=AXIS2_PLACEMENT_3D ( 'NONE', #2876, #10919, #7337 ) ;
#6778=( BOUNDED_SURFACE ( )  B_SPLINE_SURFACE ( 3, 2, ( 
 ( #1656, #6349, #8421 ),
 ( #13136, #7348, #421 ),
 ( #8495, #2602, #1439 ),
 ( #8569, #11001, #6128 ),
 ( #10786, #273, #4976 ),
 ( #9642, #14289, #5187 ),
 ( #2677, #12002, #6193 ),
 ( #10852, #2029, #14743 ),
 ( #6572, #7709, #6714 ),
 ( #6643, #10161, #8705 ),
 ( #565, #1799, #2967 ),
 ( #6412, #1725, #7790 ),
 ( #11068, #7861, #4198 ),
 ( #3197, #7628, #5262 ),
 ( #10017, #12288, #4345 ),
 ( #12368, #12510, #11297 ),
 ( #6491, #11228, #2893 ),
 ( #4270, #724, #5422 ) ),
 .UNSPECIFIED., .F., .F., .F. ) 
 B_SPLINE_SURFACE_WITH_KNOTS ( ( 4, 2, 2, 2, 2, 2, 2, 2, 4 ),
 ( 3, 3 ),
 ( 1.626303258728256651E-18, 0.0007909791536113771216, 0.001581958307222752725, 0.002372937460834128112, 0.003163916614445503716, 0.003954895768056879320, 0.004745874921668254490, 0.005536854075279630527, 0.006327833228891005697 ),
 ( 0.000000000000000000, 1.000000000000000000 ),
 .UNSPECIFIED. ) 
 GEOMETRIC_REPRESENTATION_ITEM ( )  RATIONAL_B_SPLINE_SURFACE ( (
 ( 1.000000000000000000, 0.7071067811865485719, 1.000000000000000000),
 ( 1.000000000000000000, 0.7223000759815237926, 1.000000000000000000),
 ( 1.000000000000000000, 0.7432471854318939419, 1.000000000000000000),
 ( 1.000000000000000000, 0.7877081205363730687, 1.000000000000000000),
 ( 1.000000000000000000, 0.8105118531247716973, 1.000000000000000000),
 ( 1.000000000000000000, 0.8506981922268006535, 1.000000000000000000),
 ( 1.000000000000000000, 0.8680068107956325774, 1.000000000000000000),
 ( 1.000000000000000000, 0.8928257656524388741, 1.000000000000000000),
 ( 1.000000000000000000, 0.9004767918862143228, 1.000000000000000000),
 ( 1.000000000000000000, 0.9031067434151224260, 1.000000000000000000),
 ( 1.000000000000000000, 0.8981097434906895050, 1.000000000000000000),
 ( 1.000000000000000000, 0.8774757945656930236, 1.000000000000000000),
 ( 1.000000000000000000, 0.8617372505914389080, 1.000000000000000000),
 ( 1.000000000000000000, 0.8241150794756328946, 1.000000000000000000),
 ( 1.000000000000000000, 0.8017387543657485960, 1.000000000000000000),
 ( 1.000000000000000000, 0.7573703026982906428, 1.000000000000000000),
 ( 1.000000000000000000, 0.7351444931784540948, 1.000000000000000000),
 ( 1.000000000000000000, 0.7173416231802117737, 1.000000000000000000) ) ) 
 REPRESENTATION_ITEM ( '' )  SURFACE ( )  );
#6785=DIRECTION ( 'NONE',  ( -0.9999002670844989726, 0.000000000000000000, 0.01412288512831212997 ) ) ;
#6787=CARTESIAN_POINT ( 'NONE',  ( 2.230477600021715912, 0.4287871555018996084, 0.4684960790957384824 ) ) ;
#6792=CARTESIAN_POINT ( 'NONE',  ( 0.7073375012242669735, 0.002604401085336686614, -0.4168187156544767569 ) ) ;
#6798=EDGE_LOOP ( 'NONE', ( #2860, #6292, #5539, #9424 ) ) ;
#6802=ORIENTED_EDGE ( 'NONE', *, *, #3291, .F. ) ;
#6808=LINE ( 'NONE', #808, #581 ) ;
#6809=( BOUNDED_CURVE ( )  B_SPLINE_CURVE ( 3, ( #11195, #12637, #8990, #927 ),
 .UNSPECIFIED., .F., .F. ) 
 B_SPLINE_CURVE_WITH_KNOTS ( ( 4, 4 ),
 ( 0.7853981633974467247, 1.570796326794896780 ),
 .UNSPECIFIED. ) 
 CURVE ( )  GEOMETRIC_REPRESENTATION_ITEM ( )  RATIONAL_B_SPLINE_CURVE ( ( 1.000000000000000000, 0.9492530216741910110, 0.9492530216741910110, 1.000000000000000000 ) ) 
 REPRESENTATION_ITEM ( '' )  );
#6820=EDGE_CURVE ( 'NONE', #1866, #14657, #7653, .T. ) ;
#6823=VERTEX_POINT ( 'NONE', #10311 ) ;
#6835=DIRECTION ( 'NONE',  ( -0.9999002670844991947, 0.000000000000000000, -0.01412288512831586830 ) ) ;
#6837=CARTESIAN_POINT ( 'NONE',  ( 2.414213562373087374, 0.1427864376268978830, 0.4064941968476759038 ) ) ;
#6838=CARTESIAN_POINT ( 'NONE',  ( 2.738128344600899933, 0.4573395005112720901, -0.4018406495283275981 ) ) ;
#6844=ORIENTED_EDGE ( 'NONE', *, *, #10917, .T. ) ;
#6845=DIRECTION ( 'NONE',  ( 0.1062487806292201492, -7.256387954780240841E-16, 0.9943395781194692695 ) ) ;
#6856=CARTESIAN_POINT ( 'NONE',  ( 0.8803859122989420305, -0.4304857796780524049, -0.4642829517559106112 ) ) ;
#6865=LINE ( 'NONE', #9859, #6506 ) ;
#6874=CARTESIAN_POINT ( 'NONE',  ( 0.7013557507355751008, -0.03211000548724558118, -0.4833783981792019180 ) ) ;
#6875=DIRECTION ( 'NONE',  ( 0.03489949670248613384, -0.9993908270190963172, 0.000000000000000000 ) ) ;
#6880=EDGE_LOOP ( 'NONE', ( #10711, #6844, #10134, #14513 ) ) ;
#6890=DIRECTION ( 'NONE',  ( -0.01412288512831213171, 3.675428035873182550E-19, -0.9999002670844991947 ) ) ;
#6891=CARTESIAN_POINT ( 'NONE',  ( 0.6678556410416571776, -0.4638629127466907254, -0.4666787114416890425 ) ) ;
#6900=LINE ( 'NONE', #9346, #684 ) ;
#6905=VERTEX_POINT ( 'NONE', #4891 ) ;
#6908=DIRECTION ( 'NONE',  ( 0.000000000000000000, -1.000000000000000000, 0.000000000000000000 ) ) ;
#6917=CARTESIAN_POINT ( 'NONE',  ( 0.6782634401674774161, -0.4298497817134653287, 0.4690018541713363853 ) ) ;
#6920=DIRECTION ( 'NONE',  ( -0.9993908270190959842, -0.03489949670249406499, 0.000000000000000000 ) ) ;
#6922=AXIS2_PLACEMENT_3D ( 'NONE', #2841, #7582, #5596 ) ;
#6927=CARTESIAN_POINT ( 'NONE',  ( 0.9703582086188188294, -0.4381469060595838960, -0.4503728430570826391 ) ) ;
#6937=CARTESIAN_POINT ( 'NONE',  ( 1.007186596135057011, -0.4429912711639673040, -0.4173593519128859231 ) ) ;
#6938=ORIENTED_EDGE ( 'NONE', *, *, #8804, .T. ) ;
#6946=CARTESIAN_POINT ( 'NONE',  ( 0.7134904538003046248, -1.707404996040164512E-17, -0.4077598229816902231 ) ) ;
#6948=CARTESIAN_POINT ( 'NONE',  ( 2.633946444925666874, 0.3625193201794746356, -0.4033906250602100618 ) ) ;
#6949=AXIS2_PLACEMENT_3D ( 'NONE', #10336, #6835, #2225 ) ;
#6950=PLANE ( 'NONE',  #771 ) ;
#6955=CIRCLE ( 'NONE', #2553, 0.06000000000000008105 ) ;
#6957=ORIENTED_EDGE ( 'NONE', *, *, #12871, .F. ) ;
#6961=DIRECTION ( 'NONE',  ( 0.000000000000000000, 0.000000000000000000, -1.000000000000000000 ) ) ;
#6964=CARTESIAN_POINT ( 'NONE',  ( 0.6735138268600964206, -0.4714177217989499180, -0.4544009417003763152 ) ) ;
#6968=AXIS2_PLACEMENT_3D ( 'NONE', #3761, #3612, #8433 ) ;
#6969=DIRECTION ( 'NONE',  ( 0.01412288512831213171, -3.675428035873182550E-19, 0.9999002670844991947 ) ) ;
#6975=ORIENTED_EDGE ( 'NONE', *, *, #13478, .F. ) ;
#6987=CARTESIAN_POINT ( 'NONE',  ( 2.414213562373090927, 0.1427864376269009083, 0.4064941968476758483 ) ) ;
#6992=CARTESIAN_POINT ( 'NONE',  ( 0.6867276282385307296, -0.4820986824598040843, 0.4280639610650029403 ) ) ;
#6993=CARTESIAN_POINT ( 'NONE',  ( 3.601417382415921686, 0.9969999999999999973, 0.4491325228472327624 ) ) ;
#6997=ORIENTED_EDGE ( 'NONE', *, *, #13660, .T. ) ;
#6998=CARTESIAN_POINT ( 'NONE',  ( 7.623651669702752511E-17, -0.6589999999999998082, 0.000000000000000000 ) ) ;
#7008=CARTESIAN_POINT ( 'NONE',  ( 2.321652452206756756, 0.05022532746056743852, -0.4077623363510139431 ) ) ;
#7013=AXIS2_PLACEMENT_3D ( 'NONE', #4428, #9171, #13737 ) ;
#7021=CARTESIAN_POINT ( 'NONE',  ( 0.8917602750860615934, -0.4611956585980242496, -0.4498705880430254322 ) ) ;
#7026=CARTESIAN_POINT ( 'NONE',  ( 1.001102354577344311, -0.4429645722769263716, -0.4282009803966606576 ) ) ;
#7028=CARTESIAN_POINT ( 'NONE',  ( 2.003951500898716542, -0.1834701832127828836, -0.4716956002697923478 ) ) ;
#7042=CARTESIAN_POINT ( 'NONE',  ( -5.764454660286586870E-18, 0.1956296296296295978, 0.000000000000000000 ) ) ;
#7046=CARTESIAN_POINT ( 'NONE',  ( 0.9749999999999999778, -0.6230000000000016636, -0.3750000000000000555 ) ) ;
#7052=CARTESIAN_POINT ( 'NONE',  ( 2.591947913870973785, 0.4045262297594673373, 0.4633905661882630755 ) ) ;
#7060=B_SPLINE_CURVE_WITH_KNOTS ( 'NONE', 3,
 ( #8392, #6095, #10598, #247, #21, #12803, #9612, #12729, #6937, #2335 ),
 .UNSPECIFIED., .F., .F.,
 ( 4, 2, 2, 2, 4 ),
 ( 1.734723475976807094E-18, 0.0007067171527782007247, 0.001413434305556399715, 0.002120151458334598813, 0.002826868611112797695 ),
 .UNSPECIFIED. ) ;
#7062=DIRECTION ( 'NONE',  ( -1.000000000000000000, -1.365923996832131609E-16, 0.000000000000000000 ) ) ;
#7064=AXIS2_PLACEMENT_3D ( 'NONE', #11901, #4567, #13874 ) ;
#7068=DIRECTION ( 'NONE',  ( -0.000000000000000000, -0.000000000000000000, -1.000000000000000000 ) ) ;
#7072=ORIENTED_EDGE ( 'NONE', *, *, #706, .F. ) ;
#7074=CARTESIAN_POINT ( 'NONE',  ( 0.6583927779709454198, -0.3799506946983937650, 0.5137831800632561841 ) ) ;
#7082=EDGE_CURVE ( 'NONE', #13550, #14571, #9979, .T. ) ;
#7085=EDGE_LOOP ( 'NONE', ( #3910, #8344, #12743, #8425 ) ) ;
#7089=CARTESIAN_POINT ( 'NONE',  ( 2.220468100499630726, -0.03283382702689773003, -0.4686374562075200090 ) ) ;
#7090=AXIS2_PLACEMENT_3D ( 'NONE', #9142, #4550, #12720 ) ;
#7091=CARTESIAN_POINT ( 'NONE',  ( 0.3724999999999997757, 0.2159999999999999698, -0.3725000000000000533 ) ) ;
#7092=CARTESIAN_POINT ( 'NONE',  ( 0.4425000000000001155, 0.2159999999999999420, -0.8500000000000000888 ) ) ;
#7103=DIRECTION ( 'NONE',  ( -1.000000000000000000, -2.130223169792495565E-16, 0.000000000000000000 ) ) ;
#7107=CARTESIAN_POINT ( 'NONE',  ( 0.7441595030246632714, -3.474002255126643149E-17, -0.4356261515797149597 ) ) ;
#7108=ORIENTED_EDGE ( 'NONE', *, *, #14522, .F. ) ;
#7110=CARTESIAN_POINT ( 'NONE',  ( 1.250847373107698557, 9.390727478220904197E-17, 0.4823326642216427262 ) ) ;
#7118=ORIENTED_EDGE ( 'NONE', *, *, #4780, .T. ) ;
#7121=ORIENTED_EDGE ( 'NONE', *, *, #3123, .F. ) ;
#7122=LINE ( 'NONE', #11918, #14778 ) ;
#7137=CARTESIAN_POINT ( 'NONE',  ( -0.6412116890856959239, -0.6590000000000000302, 0.000000000000000000 ) ) ;
#7140=DIRECTION ( 'NONE',  ( 0.000000000000000000, 1.000000000000000000, 0.000000000000000000 ) ) ;
#7141=CARTESIAN_POINT ( 'NONE',  ( 0.8999999999999999112, -0.6230000000000016636, -0.3750000000000000555 ) ) ;
#7142=CARTESIAN_POINT ( 'NONE',  ( 2.702105678819866963, 0.5048229836667779136, 0.4618346655533916989 ) ) ;
#7147=EDGE_CURVE ( 'NONE', #2489, #5710, #12373, .T. ) ;
#7163=CARTESIAN_POINT ( 'NONE',  ( 0.007908111413600220699, -0.2214999999999999469, -0.5598942880828962076 ) ) ;
#7165=AXIS2_PLACEMENT_3D ( 'NONE', #1381, #5848, #13928 ) ;
#7173=LINE ( 'NONE', #1329, #1408 ) ;
#7184=ORIENTED_EDGE ( 'NONE', *, *, #7956, .T. ) ;
#7186=CARTESIAN_POINT ( 'NONE',  ( -5.764454660286586870E-18, 0.06000000000000001166, 0.000000000000000000 ) ) ;
#7198=EDGE_CURVE ( 'NONE', #6823, #9279, #12478, .T. ) ;
#7199=CARTESIAN_POINT ( 'NONE',  ( 8.517841687953398022, 0.8704007761502550178, 0.3197150928555234639 ) ) ;
#7203=CARTESIAN_POINT ( 'NONE',  ( 0.000000000000000000, 0.000000000000000000, 0.5000000000000000000 ) ) ;
#7207=EDGE_LOOP ( 'NONE', ( #10144, #12079, #14972, #2015 ) ) ;
#7210=ORIENTED_EDGE ( 'NONE', *, *, #5456, .T. ) ;
#7211=ORIENTED_EDGE ( 'NONE', *, *, #15069, .F. ) ;
#7213=CARTESIAN_POINT ( 'NONE',  ( 3.045371920833451096, 0.6267721954701777065, 0.3972696057388188096 ) ) ;
#7215=CARTESIAN_POINT ( 'NONE',  ( 1.000000000000000222, -0.4429999999999998939, 0.4258697216429003785 ) ) ;
#7218=DIRECTION ( 'NONE',  ( 0.000000000000000000, -1.000000000000000000, -0.000000000000000000 ) ) ;
#7219=EDGE_CURVE ( 'NONE', #14571, #7869, #11814, .T. ) ;
#7221=CARTESIAN_POINT ( 'NONE',  ( 0.6566433263007029897, -0.4313127572425527467, 0.4973513887421178725 ) ) ;
#7222=DIRECTION ( 'NONE',  ( -0.9999002670844989726, 2.602203049398214110E-17, 0.01412288512831212997 ) ) ;
#7236=CARTESIAN_POINT ( 'NONE',  ( 2.414213562373087374, 0.1427864376268978830, 0.4064941968476759038 ) ) ;
#7241=ORIENTED_EDGE ( 'NONE', *, *, #11203, .F. ) ;
#7245=FACE_OUTER_BOUND ( 'NONE', #4184, .T. ) ;
#7249=CARTESIAN_POINT ( 'NONE',  ( 1.000847373107698779, -0.3829999999999998961, 0.4858637376679703634 ) ) ;
#7251=EDGE_LOOP ( 'NONE', ( #10335, #752 ) ) ;
#7252=DIRECTION ( 'NONE',  ( -0.7071067811865350272, -0.7071067811865600072, 0.000000000000000000 ) ) ;
#7253=CARTESIAN_POINT ( 'NONE',  ( 1.612492615670230611, 0.05745813234176449374, 0.4169456318805255801 ) ) ;
#7260=VERTEX_POINT ( 'NONE', #12715 ) ;
#7261=CARTESIAN_POINT ( 'NONE',  ( 0.3724999999999999423, 0.2159999999999999420, 0.3724999999999999423 ) ) ;
#7262=ORIENTED_EDGE ( 'NONE', *, *, #11669, .F. ) ;
#7263=ADVANCED_FACE ( 'NONE', ( #1077 ), #9059, .F. ) ;
#7268=LINE ( 'NONE', #6039, #12629 ) ;
#7271=AXIS2_PLACEMENT_3D ( 'NONE', #1790, #14730, #11363 ) ;
#7273=CARTESIAN_POINT ( 'NONE',  ( 8.573547510565930452, 0.9318103594813683666, 0.3691840008912894988 ) ) ;
#7275=( BOUNDED_SURFACE ( )  B_SPLINE_SURFACE ( 3, 2, ( 
 ( #14193, #7110, #4722 ),
 ( #2429, #1411, #3576 ),
 ( #5027, #2575, #181 ),
 ( #11757, #13114, #8337 ),
 ( #14340, #319, #7253 ),
 ( #14116, #4800, #2651 ),
 ( #9472, #6106, #2498 ),
 ( #12891, #3876, #12969 ),
 ( #12049, #9549, #3655 ),
 ( #7397, #13187, #1333 ) ),
 .UNSPECIFIED., .F., .F., .F. ) 
 B_SPLINE_SURFACE_WITH_KNOTS ( ( 4, 2, 2, 2, 4 ),
 ( 3, 3 ),
 ( 4.712388980384689674, 4.908738521234051966, 5.105088062083414258, 5.301437602932777438, 5.497787143782139729 ),
 ( 0.000000000000000000, 1.000000000000000000 ),
 .UNSPECIFIED. ) 
 GEOMETRIC_REPRESENTATION_ITEM ( )  RATIONAL_B_SPLINE_SURFACE ( (
 ( 1.000000000000000000, 0.7071067811865475727, 1.000000000000000000),
 ( 1.000000000000000000, 0.7067799747774232699, 1.000000000000000000),
 ( 1.000000000000000000, 0.7064529522741163081, 1.000000000000000000),
 ( 1.000000000000000000, 0.7058110186552004617, 1.000000000000000000),
 ( 1.000000000000000000, 0.7054961263470524990, 1.000000000000000000),
 ( 1.000000000000000000, 0.7048906332647922879, 1.000000000000000000),
 ( 1.000000000000000000, 0.7046000480551916079, 1.000000000000000000),
 ( 1.000000000000000000, 0.7040544485608896119, 1.000000000000000000),
 ( 1.000000000000000000, 0.7037994241814393703, 1.000000000000000000),
 ( 1.000000000000000000, 0.7035672008258526677, 1.000000000000000000) ) ) 
 REPRESENTATION_ITEM ( '' )  SURFACE ( )  );
#7281=EDGE_CURVE ( 'NONE', #5452, #2763, #5765, .T. ) ;
#7287=DIRECTION ( 'NONE',  ( -0.7070715176384863021, -0.7070715176384774203, 0.009986885842351498482 ) ) ;
#7289=CARTESIAN_POINT ( 'NONE',  ( 2.633946444925666430, 0.3625193201794738584, 0.4033906250602100618 ) ) ;
#7292=ADVANCED_FACE ( 'NONE', ( #15091 ), #12583, .T. ) ;
#7296=AXIS2_PLACEMENT_3D ( 'NONE', #13895, #12520, #9174 ) ;
#7302=CIRCLE ( 'NONE', #8021, 0.06000000000000001166 ) ;
#7319=ORIENTED_EDGE ( 'NONE', *, *, #8373, .F. ) ;
#7337=DIRECTION ( 'NONE',  ( -1.000000000000000000, -1.365923996832131609E-16, 0.000000000000000000 ) ) ;
#7338=DIRECTION ( 'NONE',  ( 1.365923996832131609E-16, -1.000000000000000000, -0.000000000000000000 ) ) ;
#7340=CARTESIAN_POINT ( 'NONE',  ( 2.381934877626968206, 0.6476033094210934538, 0.4663568520109472870 ) ) ;
#7348=CARTESIAN_POINT ( 'NONE',  ( 0.8352936206970669186, -0.4446654365634041262, -0.4130780710220839369 ) ) ;
#7353=CARTESIAN_POINT ( 'NONE',  ( 0.4424999999999979505, -0.6589999999999996971, -0.8500000000000000888 ) ) ;
#7355=VERTEX_POINT ( 'NONE', #5004 ) ;
#7358=DIRECTION ( 'NONE',  ( 0.000000000000000000, 0.000000000000000000, 1.000000000000000000 ) ) ;
#7359=CARTESIAN_POINT ( 'NONE',  ( 2.738674485064839459, 0.4577639129046877642, 0.4613181569904871160 ) ) ;
#7362=AXIS2_PLACEMENT_3D ( 'NONE', #5418, #10082, #13578 ) ;
#7364=CARTESIAN_POINT ( 'NONE',  ( 0.7040121242107247879, -0.05591482235280140212, 0.4900563259292270990 ) ) ;
#7366=( BOUNDED_CURVE ( )  B_SPLINE_CURVE ( 3, ( #10920, #14277, #483, #9921 ),
 .UNSPECIFIED., .F., .F. ) 
 B_SPLINE_CURVE_WITH_KNOTS ( ( 4, 4 ),
 ( 1.570796326794896780, 2.356194490192346613 ),
 .UNSPECIFIED. ) 
 CURVE ( )  GEOMETRIC_REPRESENTATION_ITEM ( )  RATIONAL_B_SPLINE_CURVE ( ( 1.000000000000000000, 0.9492530216741910110, 0.9492530216741910110, 1.000000000000000000 ) ) 
 REPRESENTATION_ITEM ( '' )  );
#7367=DIRECTION ( 'NONE',  ( -0.9999002670844990837, 0.000000000000000000, 0.01412288512831215426 ) ) ;
#7371=CARTESIAN_POINT ( 'NONE',  ( 0.7243146799153700188, -0.2214999999999999469, 0.4897695666678619220 ) ) ;
#7376=CARTESIAN_POINT ( 'NONE',  ( 0.7020310496751535068, -0.02903435051206633769, 0.4816878228448820409 ) ) ;
#7381=CARTESIAN_POINT ( 'NONE',  ( 0.7856509485162607165, -0.4429999999999998939, -0.3627813902276395552 ) ) ;
#7390=CARTESIAN_POINT ( 'NONE',  ( 8.705855184453682227, 0.9357017671274362458, -0.3021636316005746892 ) ) ;
#7397=CARTESIAN_POINT ( 'NONE',  ( 2.088768908813761094, 0.2870784642939447906, 0.4704976142822914764 ) ) ;
#7399=EDGE_CURVE ( 'NONE', #9046, #7832, #2578, .T. ) ;
#7400=VECTOR ( 'NONE', #7935, 39.37007874015748143 ) ;
#7414=DIRECTION ( 'NONE',  ( 0.000000000000000000, -1.000000000000000000, 0.000000000000000000 ) ) ;
#7417=VERTEX_POINT ( 'NONE', #1309 ) ;
#7419=PLANE ( 'NONE',  #7969 ) ;
#7420=DIRECTION ( 'NONE',  ( 0.7071067811865354713, -0.7071067811865595631, 0.000000000000000000 ) ) ;
#7429=CARTESIAN_POINT ( 'NONE',  ( 0.6555286510801312527, -0.04031751147701368582, 0.5099168278768518858 ) ) ;
#7432=CIRCLE ( 'NONE', #6949, 0.06000000000000001860 ) ;
#7433=ORIENTED_EDGE ( 'NONE', *, *, #13123, .T. ) ;
#7436=LENGTH_MEASURE_WITH_UNIT ( LENGTH_MEASURE( 0.02539999999999999897 ), #4064 );
#7440=ORIENTED_EDGE ( 'NONE', *, *, #3326, .F. ) ;
#7444=CARTESIAN_POINT ( 'NONE',  ( 2.633946444925666874, 0.3625193201794746356, 0.5000000000000000000 ) ) ;
#7445=CARTESIAN_POINT ( 'NONE',  ( 0.8293604527229431200, -0.4837317850455687962, -0.3495425184068792768 ) ) ;
#7456=ORIENTED_EDGE ( 'NONE', *, *, #10810, .T. ) ;
#7462=DIRECTION ( 'NONE',  ( 0.000000000000000000, 0.000000000000000000, 1.000000000000000000 ) ) ;
#7468=CARTESIAN_POINT ( 'NONE',  ( 2.372634528609593563, 0.1852128444980908617, 0.4664882128727458888 ) ) ;
#7480=DIRECTION ( 'NONE',  ( -0.9999002670844991947, 0.000000000000000000, 0.01412288512831128343 ) ) ;
#7485=CIRCLE ( 'NONE', #12849, 0.03999999999999998695 ) ;
#7493=CARTESIAN_POINT ( 'NONE',  ( 0.6566521509169380710, -0.4313701889023026648, 0.4973154343666586485 ) ) ;
#7494=CARTESIAN_POINT ( 'NONE',  ( 0.4124999999999997558, -0.6290000000000003366, -0.3725000000000000533 ) ) ;
#7502=CONICAL_SURFACE ( 'NONE', #879, 0.07000000000000047851, 0.7853981633974297383 ) ;
#7506=EDGE_CURVE ( 'NONE', #13657, #14149, #11098, .T. ) ;
#7510=CARTESIAN_POINT ( 'NONE',  ( 1.000000000000000222, -0.4429999999999998939, 0.5000000000000000000 ) ) ;
#7514=ORIENTED_EDGE ( 'NONE', *, *, #2286, .F. ) ;
#7516=CARTESIAN_POINT ( 'NONE',  ( 1.250000000000000000, 0.000000000000000000, -0.4223386481965726302 ) ) ;
#7518=CARTESIAN_POINT ( 'NONE',  ( 0.7818165671723676935, -0.4451953551292709421, -0.3317768536406905944 ) ) ;
#7522=CARTESIAN_POINT ( 'NONE',  ( 1.323631913064688748, -9.281535253675872034E-17, -0.4212431828231353870 ) ) ;
#7526=ORIENTED_EDGE ( 'NONE', *, *, #9833, .F. ) ;
#7528=CARTESIAN_POINT ( 'NONE',  ( 8.573547510565946439, 0.9318103594814406421, -0.3691840008912834481 ) ) ;
#7539=CARTESIAN_POINT ( 'NONE',  ( -0.4125000000000001998, -0.6590000000000000302, -0.4125000000000000333 ) ) ;
#7540=CIRCLE ( 'NONE', #1189, 0.03999999999999998002 ) ;
#7550=LINE ( 'NONE', #8625, #14605 ) ;
#7558=CARTESIAN_POINT ( 'NONE',  ( 8.792093969802149189, 0.8799778768672790186, 6.829619984160658046E-17 ) ) ;
#7571=CARTESIAN_POINT ( 'NONE',  ( 3.063895178286539789, 1.056999999999999718, -0.3964908961568774926 ) ) ;
#7575=DIRECTION ( 'NONE',  ( -0.000000000000000000, -1.000000000000000000, -0.000000000000000000 ) ) ;
#7576=DIRECTION ( 'NONE',  ( 0.8970266063945135926, 0.000000000000000000, -0.4419765462333294370 ) ) ;
#7578=CARTESIAN_POINT ( 'NONE',  ( 0.6894988814560862878, -0.0004723380455460435431, 0.4465617225471406049 ) ) ;
#7579=CARTESIAN_POINT ( 'NONE',  ( 0.9699525753244386816, -0.4431216144847617833, -0.4027229741727945678 ) ) ;
#7582=DIRECTION ( 'NONE',  ( -0.9992912762382415437, -0.03489602031261516274, -0.01411428356269072565 ) ) ;
#7584=ORIENTED_EDGE ( 'NONE', *, *, #7198, .T. ) ;
#7593=DIRECTION ( 'NONE',  ( 0.9999002670844989726, 1.365787769249574676E-16, -0.01412288512831212997 ) ) ;
#7597=CARTESIAN_POINT ( 'NONE',  ( 1.558097216777239780, -0.02209972869556142000, -0.4779929771641632796 ) ) ;
#7600=ORIENTED_EDGE ( 'NONE', *, *, #9706, .T. ) ;
#7602=CARTESIAN_POINT ( 'NONE',  ( 8.575402687748473696, 0.8724108505558056947, -0.3686609533457590460 ) ) ;
#7607=VECTOR ( 'NONE', #13333, 39.37007874015748143 ) ;
#7615=DIRECTION ( 'NONE',  ( 0.01412288512831213171, -3.675428035873182550E-19, 0.9999002670844991947 ) ) ;
#7620=CARTESIAN_POINT ( 'NONE',  ( 2.599116034106475404, 0.7926631980420985046, 0.4028586330191923914 ) ) ;
#7627=CARTESIAN_POINT ( 'NONE',  ( 8.803302564019910292, 0.8803692896022998760, 0.1890918720381998541 ) ) ;
#7628=CARTESIAN_POINT ( 'NONE',  ( 0.9492541663682917408, -0.4468142390482141568, -0.4325038486745500510 ) ) ;
#7631=ORIENTED_EDGE ( 'NONE', *, *, #2413, .F. ) ;
#7633=EDGE_LOOP ( 'NONE', ( #8816, #1782, #6997, #311 ) ) ;
#7636=EDGE_LOOP ( 'NONE', ( #2271, #12801, #8181, #3988 ) ) ;
#7637=EDGE_LOOP ( 'NONE', ( #14103, #7433, #4328, #13016, #10860 ) ) ;
#7638=EDGE_CURVE ( 'NONE', #3117, #14571, #1910, .T. ) ;
#7642=CARTESIAN_POINT ( 'NONE',  ( 8.849999999999999645, 0.9399413264884247665, 6.829619984160658046E-17 ) ) ;
#7644=ADVANCED_FACE ( 'NONE', ( #13686 ), #5747, .F. ) ;
#7653=CIRCLE ( 'NONE', #12051, 0.8653656741516848605 ) ;
#7656=CIRCLE ( 'NONE', #5721, 0.7435009325572419225 ) ;
#7660=ORIENTED_EDGE ( 'NONE', *, *, #4943, .T. ) ;
#7661=FACE_OUTER_BOUND ( 'NONE', #4534, .T. ) ;
#7663=LINE ( 'NONE', #10889, #2192 ) ;
#7666=CARTESIAN_POINT ( 'NONE',  ( 1.519298119451261364, -0.3788322150377887443, 0.4785409870134300636 ) ) ;
#7669=ADVANCED_FACE ( 'NONE', ( #5603 ), #12115, .F. ) ;
#7672=CARTESIAN_POINT ( 'NONE',  ( 1.249999999999997335, 9.390727478220904197E-17, -0.4223386481965728523 ) ) ;
#7681=ORIENTED_EDGE ( 'NONE', *, *, #1437, .F. ) ;
#7683=CARTESIAN_POINT ( 'NONE',  ( 0.6592137334438913365, -0.4436300111355807596, -0.4885243083254872110 ) ) ;
#7690=VERTEX_POINT ( 'NONE', #11326 ) ;
#7694=CARTESIAN_POINT ( 'NONE',  ( 8.476283996537762988, 0.8689495495877206377, 0.3203020658980471613 ) ) ;
#7702=DIRECTION ( 'NONE',  ( 0.000000000000000000, 1.000000000000000000, 0.000000000000000000 ) ) ;
#7705=CARTESIAN_POINT ( 'NONE',  ( 8.476283996537762988, 0.8689495495877206377, -0.3203020658980470503 ) ) ;
#7706=CARTESIAN_POINT ( 'NONE',  ( 8.670688874134258484, 0.8757383175063380154, 0.2544954840226653636 ) ) ;
#7709=CARTESIAN_POINT ( 'NONE',  ( 0.8902005033493116670, -0.4418901924079376431, -0.4498168137707627690 ) ) ;
#7715=DIRECTION ( 'NONE',  ( -0.000000000000000000, -1.000000000000000000, -0.000000000000000000 ) ) ;
#7720=( NAMED_UNIT ( * ) PLANE_ANGLE_UNIT ( ) SI_UNIT ( $, .RADIAN. ) );
#7722=ORIENTED_EDGE ( 'NONE', *, *, #2045, .T. ) ;
#7723=DIRECTION ( 'NONE',  ( 0.7071067811865430208, -0.7071067811865520136, 0.000000000000000000 ) ) ;
#7724=CARTESIAN_POINT ( 'NONE',  ( 0.3724999999999997757, 0.2159999999999999420, -0.3725000000000000533 ) ) ;
#7726=CARTESIAN_POINT ( 'NONE',  ( 2.742551415177088003, 0.8007359432430825041, -0.4612633980907191456 ) ) ;
#7729=EDGE_CURVE ( 'NONE', #9809, #1024, #2090, .T. ) ;
#7737=CARTESIAN_POINT ( 'NONE',  ( 0.7007544714965477928, -0.4010719056816615113, 0.4875120335496959667 ) ) ;
#7744=LINE ( 'NONE', #1839, #13662 ) ;
#7750=CARTESIAN_POINT ( 'NONE',  ( 0.8321296539245407464, -0.4837347236987069587, -0.3428806532137185226 ) ) ;
#7752=VECTOR ( 'NONE', #5711, 39.37007874015748143 ) ;
#7776=CIRCLE ( 'NONE', #1166, 0.05999999999999990757 ) ;
#7779=ORIENTED_EDGE ( 'NONE', *, *, #2625, .F. ) ;
#7782=EDGE_CURVE ( 'NONE', #12826, #11117, #10791, .T. ) ;
#7787=CIRCLE ( 'NONE', #8039, 0.03999999999999998002 ) ;
#7789=AXIS2_PLACEMENT_3D ( 'NONE', #11222, #5120, #6483 ) ;
#7790=CARTESIAN_POINT ( 'NONE',  ( 0.9387684931985510461, -0.4323728853731128030, -0.4608802220936111804 ) ) ;
#7795=VERTEX_POINT ( 'NONE', #8427 ) ;
#7799=ORIENTED_EDGE ( 'NONE', *, *, #7147, .T. ) ;
#7804=DIRECTION ( 'NONE',  ( 0.4419764427789427685, 0.0006842106276663988736, 0.8970263964255951183 ) ) ;
#7807=CARTESIAN_POINT ( 'NONE',  ( 2.630032447663877893, 0.7405933021012496287, -0.4628526490442955166 ) ) ;
#7808=CARTESIAN_POINT ( 'NONE',  ( 1.014070859989637308, -0.4429514566285153720, -0.3903639285911673640 ) ) ;
#7817=ORIENTED_EDGE ( 'NONE', *, *, #2533, .F. ) ;
#7818=CARTESIAN_POINT ( 'NONE',  ( 0.9652173913043479159, -0.4829999999999998739, -0.3379636412230419551 ) ) ;
#7823=DIRECTION ( 'NONE',  ( -0.7071067811865474617, 0.7071067811865474617, 0.000000000000000000 ) ) ;
#7824=CARTESIAN_POINT ( 'NONE',  ( -0.4424999999999982836, -0.6590000000000000302, 0.3724999999999999423 ) ) ;
#7831=EDGE_LOOP ( 'NONE', ( #13152, #1828, #5780, #13233 ) ) ;
#7832=VERTEX_POINT ( 'NONE', #7137 ) ;
#7835=DIRECTION ( 'NONE',  ( 0.9999002670844989726, -0.000000000000000000, -0.01412288512831212997 ) ) ;
#7853=CARTESIAN_POINT ( 'NONE',  ( 0.7834577061006936516, -0.4429999999999997273, -0.3569559810110801146 ) ) ;
#7861=CARTESIAN_POINT ( 'NONE',  ( 0.9372784336483218626, -0.4451370293985828508, -0.4407327033732494348 ) ) ;
#7866=ORIENTED_EDGE ( 'NONE', *, *, #9316, .F. ) ;
#7869=VERTEX_POINT ( 'NONE', #10564 ) ;
#7876=DIRECTION ( 'NONE',  ( -0.000000000000000000, -0.000000000000000000, -1.000000000000000000 ) ) ;
#7877=CARTESIAN_POINT ( 'NONE',  ( 2.187203820042824542, 0.4712135623730921985, -0.4085020630706684974 ) ) ;
#7880=ORIENTED_EDGE ( 'NONE', *, *, #11100, .F. ) ;
#7881=CARTESIAN_POINT ( 'NONE',  ( 2.592367411162173507, 0.4049457270506671147, 0.4633846410852800468 ) ) ;
#7884=ADVANCED_FACE ( 'NONE', ( #6052 ), #4983, .T. ) ;
#7889=DIRECTION ( 'NONE',  ( 0.9992912762382414327, 0.03489602031262312859, 0.01411428356268702201 ) ) ;
#7909=CARTESIAN_POINT ( 'NONE',  ( 0.6653223438648755428, -0.4594602905154550054, -0.4725272431374125670 ) ) ;
#7910=CARTESIAN_POINT ( 'NONE',  ( 0.9081152184408426420, -0.4296495775394855721, -0.4649050791335925803 ) ) ;
#7915=ADVANCED_FACE ( 'NONE', ( #8205 ), #12845, .F. ) ;
#7916=EDGE_CURVE ( 'NONE', #13167, #14331, #9940, .T. ) ;
#7919=ORIENTED_EDGE ( 'NONE', *, *, #9606, .F. ) ;
#7923=CARTESIAN_POINT ( 'NONE',  ( -5.764454660286586870E-18, 0.2159999999999999420, -0.7057575716915831521 ) ) ;
#7933=CARTESIAN_POINT ( 'NONE',  ( 0.6842449982442360135, -0.003663068356172018755, -0.4560737988759725470 ) ) ;
#7935=DIRECTION ( 'NONE',  ( -0.000000000000000000, 1.000000000000000000, 0.000000000000000000 ) ) ;
#7936=AXIS2_PLACEMENT_3D ( 'NONE', #7042, #2277, #6961 ) ;
#7944=ORIENTED_EDGE ( 'NONE', *, *, #5691, .F. ) ;
#7949=DIRECTION ( 'NONE',  ( -3.552713678800500929E-15, 0.000000000000000000, -1.000000000000000000 ) ) ;
#7956=EDGE_CURVE ( 'NONE', #34, #12566, #13102, .T. ) ;
#7957=CARTESIAN_POINT ( 'NONE',  ( 3.475290612095097043, 0.9969999999995592388, -0.4509139744054365129 ) ) ;
#7958=CARTESIAN_POINT ( 'NONE',  ( 2.567289415621048843, 0.8512991579513186080, 0.4032946756736222604 ) ) ;
#7962=CARTESIAN_POINT ( 'NONE',  ( -0.7406097974541305806, 0.1956296296296295978, -9.087557275443343323E-17 ) ) ;
#7964=( BOUNDED_SURFACE ( )  B_SPLINE_SURFACE ( 3, 2, ( 
 ( #1073, #12710, #15087 ),
 ( #3699, #4619, #12942 ),
 ( #6992, #9208, #8305 ),
 ( #1304, #148, #4848 ),
 ( #8374, #13009, #8069 ),
 ( #5847, #6917, #2545 ),
 ( #11649, #6069, #9292 ),
 ( #7221, #2, #13927 ),
 ( #10507, #11877, #15008 ),
 ( #8222, #5760, #2391 ),
 ( #4536, #3463, #8140 ),
 ( #12781, #4693, #9362 ),
 ( #7074, #12859, #11735 ),
 ( #1230, #74, #4766 ) ),
 .UNSPECIFIED., .F., .F., .T. ) 
 B_SPLINE_SURFACE_WITH_KNOTS ( ( 4, 2, 2, 2, 2, 2, 4 ),
 ( 3, 3 ),
 ( 0.001551397270042531020, 0.002805300020215408929, 0.004059202770388286620, 0.004686154145474725682, 0.005313105520561163878, 0.005940056895647602940, 0.006567008270734042003 ),
 ( 0.000000000000000000, 1.000000000000000000 ),
 .UNSPECIFIED. ) 
 GEOMETRIC_REPRESENTATION_ITEM ( )  RATIONAL_B_SPLINE_SURFACE ( (
 ( 1.000000000000000000, 0.8091170061680436065, 1.000000000000000000),
 ( 1.000000000000000000, 0.8270513381946407172, 1.000000000000000000),
 ( 1.000000000000000000, 0.8430705034767305150, 1.000000000000000000),
 ( 1.000000000000000000, 0.8715016528491055237, 1.000000000000000000),
 ( 1.000000000000000000, 0.8830758126917526152, 1.000000000000000000),
 ( 1.000000000000000000, 0.8962350306361513974, 1.000000000000000000),
 ( 1.000000000000000000, 0.8997443014201252920, 1.000000000000000000),
 ( 1.000000000000000000, 0.9049100909108197532, 1.000000000000000000),
 ( 1.000000000000000000, 0.9065649576647897279, 1.000000000000000000),
 ( 1.000000000000000000, 0.9077684922225368602, 1.000000000000000000),
 ( 1.000000000000000000, 0.9073563424328562332, 1.000000000000000000),
 ( 1.000000000000000000, 0.9044691270897152746, 1.000000000000000000),
 ( 1.000000000000000000, 0.9020443801115979321, 1.000000000000000000),
 ( 1.000000000000000000, 0.8987017906623447905, 1.000000000000000000) ) ) 
 REPRESENTATION_ITEM ( '' )  SURFACE ( )  );
#7966=CARTESIAN_POINT ( 'NONE',  ( -0.3725000000000002198, -0.6590000000000000302, -0.3725000000000000533 ) ) ;
#7969=AXIS2_PLACEMENT_3D ( 'NONE', #7353, #1288, #5056 ) ;
#7971=CARTESIAN_POINT ( 'NONE',  ( 0.9749999999999999778, -0.4829448521957644402, -0.3685736694538739866 ) ) ;
#7974=CARTESIAN_POINT ( 'NONE',  ( 3.249780665369844002, 0.6798122612590479230, -0.3942284963568287171 ) ) ;
#7978=CARTESIAN_POINT ( 'NONE',  ( 1.973079680968039540, -0.1265933021007059067, 0.4721316429241801949 ) ) ;
#7981=DIRECTION ( 'NONE',  ( -1.325335837957481409E-16, 0.7071067811865369146, 0.7071067811865581199 ) ) ;
#7983=CARTESIAN_POINT ( 'NONE',  ( 0.7856509485162610495, -0.4829999999999998739, -0.3627813902276397218 ) ) ;
#7984=CARTESIAN_POINT ( 'NONE',  ( -0.4125000000000001998, 0.1859999999999983611, -0.4125000000000000333 ) ) ;
#7992=DIRECTION ( 'NONE',  ( 0.000000000000000000, 0.000000000000000000, -1.000000000000000000 ) ) ;
#7993=CARTESIAN_POINT ( 'NONE',  ( 0.9861847369717875456, -0.4411715500842205429, -0.4414675945143460845 ) ) ;
#7998=CARTESIAN_POINT ( 'NONE',  ( 8.850000000000001421, 0.8819999999999995621, 6.829619984160658046E-17 ) ) ;
#8007=DIRECTION ( 'NONE',  ( -0.7070715176384835265, -0.7070715176384801959, -0.009986885842354482207 ) ) ;
#8011=EDGE_CURVE ( 'NONE', #14571, #11839, #1807, .T. ) ;
#8014=CARTESIAN_POINT ( 'NONE',  ( 0.6757966763794752696, -0.06127796977734757677, -0.4909001136280312649 ) ) ;
#8021=AXIS2_PLACEMENT_3D ( 'NONE', #15040, #12887, #176 ) ;
#8035=TOROIDAL_SURFACE ( 'NONE', #5340, 0.8653656741516848605, 0.05999999999999999778 ) ;
#8039=AXIS2_PLACEMENT_3D ( 'NONE', #11249, #9038, #13682 ) ;
#8043=DIRECTION ( 'NONE',  ( -0.000000000000000000, -0.000000000000000000, -1.000000000000000000 ) ) ;
#8054=DIRECTION ( 'NONE',  ( -1.655665450705613915E-16, 0.000000000000000000, -1.000000000000000000 ) ) ;
#8063=CARTESIAN_POINT ( 'NONE',  ( 3.390179639970222869, 0.6913388717410869910, -0.3921396980529558984 ) ) ;
#8065=AXIS2_PLACEMENT_3D ( 'NONE', #2186, #8007, #10374 ) ;
#8066=CARTESIAN_POINT ( 'NONE',  ( 0.9749999999999999778, -0.4829448521957645513, -0.3806875438604847561 ) ) ;
#8069=CARTESIAN_POINT ( 'NONE',  ( 0.7142320474717208656, -0.4324499512733493423, 0.4648272691893456932 ) ) ;
#8076=ADVANCED_FACE ( 'NONE', ( #3275 ), #13332, .F. ) ;
#8081=DIRECTION ( 'NONE',  ( -1.365923996832131609E-16, 1.000000000000000000, 0.000000000000000000 ) ) ;
#8092=CARTESIAN_POINT ( 'NONE',  ( 0.8663287207495570241, -0.4696786839792623236, -0.4423263022352180718 ) ) ;
#8093=CARTESIAN_POINT ( 'NONE',  ( 0.7856509485162611606, -0.4429999999999998939, -0.3627813902276396663 ) ) ;
#8094=FACE_OUTER_BOUND ( 'NONE', #11053, .T. ) ;
#8095=ORIENTED_EDGE ( 'NONE', *, *, #8768, .F. ) ;
#8097=CARTESIAN_POINT ( 'NONE',  ( 0.6766392826275201555, -0.01683334090771668179, -0.4729147972022855195 ) ) ;
#8103=VERTEX_POINT ( 'NONE', #14749 ) ;
#8106=ORIENTED_EDGE ( 'NONE', *, *, #3918, .T. ) ;
#8108=CARTESIAN_POINT ( 'NONE',  ( 2.414213562373087374, 0.1427864376268978830, 0.5000000000000000000 ) ) ;
#8112=DIRECTION ( 'NONE',  ( -1.365923996832131609E-16, 1.000000000000000000, 0.000000000000000000 ) ) ;
#8118=CARTESIAN_POINT ( 'NONE',  ( 0.007386697474241961034, -0.2214999999999999469, 0.5229781811763314359 ) ) ;
#8121=DIRECTION ( 'NONE',  ( 1.365923996832131609E-16, -1.000000000000000000, 0.000000000000000000 ) ) ;
#8127=CIRCLE ( 'NONE', #12021, 0.06000000000000001860 ) ;
#8135=CARTESIAN_POINT ( 'NONE',  ( 3.314866445692595587, 0.7487158587811556520, -0.4531798524619690682 ) ) ;
#8138=CARTESIAN_POINT ( 'NONE',  ( 0.9698268135359039421, -0.4829915030289423927, -0.4029731821154563520 ) ) ;
#8139=VERTEX_POINT ( 'NONE', #3131 ) ;
#8140=CARTESIAN_POINT ( 'NONE',  ( 0.7009701624869705272, -0.3993173672959148823, 0.4879883456728136837 ) ) ;
#8143=CIRCLE ( 'NONE', #12756, 0.7406097974541305806 ) ;
#8151=ADVANCED_FACE ( 'NONE', ( #13506 ), #2035, .T. ) ;
#8153=CARTESIAN_POINT ( 'NONE',  ( 1.886930864188312684, -0.2403504688569103875, -0.4733484341216795399 ) ) ;
#8154=EDGE_CURVE ( 'NONE', #10897, #3922, #802, .T. ) ;
#8156=ADVANCED_FACE ( 'NONE', ( #5501 ), #2200, .F. ) ;
#8164=CARTESIAN_POINT ( 'NONE',  ( 0.4424999999999981726, -0.6589999999999996971, -0.3725000000000000533 ) ) ;
#8167=CARTESIAN_POINT ( 'NONE',  ( 0.9430132649493776498, -0.4732728608467155484, -0.4367770835854211109 ) ) ;
#8169=PLANE ( 'NONE',  #7064 ) ;
#8172=DIRECTION ( 'NONE',  ( 0.7071067811865452413, -0.7071067811865497932, 0.000000000000000000 ) ) ;
#8176=LINE ( 'NONE', #12896, #7400 ) ;
#8181=ORIENTED_EDGE ( 'NONE', *, *, #6524, .F. ) ;
#8191=PLANE ( 'NONE',  #14874 ) ;
#8193=DIRECTION ( 'NONE',  ( 0.01412288512831212997, 0.000000000000000000, -0.9999002670844990837 ) ) ;
#8196=DIRECTION ( 'NONE',  ( -1.000000000000000000, 0.000000000000000000, 0.000000000000000000 ) ) ;
#8198=AXIS2_PLACEMENT_3D ( 'NONE', #11394, #14690, #13597 ) ;
#8205=FACE_OUTER_BOUND ( 'NONE', #12718, .T. ) ;
#8208=CARTESIAN_POINT ( 'NONE',  ( 2.413794065081886764, 0.1423669403356975505, 0.4065001219506589325 ) ) ;
#8209=CIRCLE ( 'NONE', #1578, 0.07500000000000002498 ) ;
#8210=DIRECTION ( 'NONE',  ( 0.000000000000000000, 0.000000000000000000, -1.000000000000000000 ) ) ;
#8221=AXIS2_PLACEMENT_3D ( 'NONE', #13701, #12634, #6920 ) ;
#8222=CARTESIAN_POINT ( 'NONE',  ( 0.6552615383573069385, -0.4102766179311354566, 0.5074994761915148089 ) ) ;
#8224=AXIS2_PLACEMENT_3D ( 'NONE', #5667, #8278, #8196 ) ;
#8232=ORIENTED_EDGE ( 'NONE', *, *, #4020, .T. ) ;
#8233=DIRECTION ( 'NONE',  ( -1.000000000000000000, 0.000000000000000000, 0.000000000000000000 ) ) ;
#8234=VECTOR ( 'NONE', #5975, 39.37007874015748854 ) ;
#8235=CARTESIAN_POINT ( 'NONE',  ( 2.414633059664288428, 0.1432059349180978269, -0.4658950132815782852 ) ) ;
#8236=CIRCLE ( 'NONE', #1603, 0.7435009325572419225 ) ;
#8238=DIRECTION ( 'NONE',  ( -0.9999002670844990837, -1.110054405283695815E-35, -0.01412288512831213171 ) ) ;
#8243=ORIENTED_EDGE ( 'NONE', *, *, #1520, .F. ) ;
#8249=CIRCLE ( 'NONE', #3597, 0.07500000000000002498 ) ;
#8253=DIRECTION ( 'NONE',  ( 8.659560562354988325E-17, 0.7071067811865430208, -0.7071067811865520136 ) ) ;
#8255=CARTESIAN_POINT ( 'NONE',  ( 0.4425000000000002820, 0.2159999999999999420, -0.3725000000000000533 ) ) ;
#8257=DIRECTION ( 'NONE',  ( -0.7071067811865431318, 0.7071067811865520136, 0.000000000000000000 ) ) ;
#8268=B_SPLINE_CURVE_WITH_KNOTS ( 'NONE', 3,
 ( #2247, #3244, #7993, #6927, #6774, #9067, #3403, #3100, #7910, #5630, #6856, #11509, #1010, #5700, #10361, #15021, #8455, #14176 ),
 .UNSPECIFIED., .F., .F.,
 ( 4, 2, 2, 2, 2, 2, 2, 2, 4 ),
 ( 0.000000000000000000, 0.0007116342341493022122, 0.001423268468298604424, 0.002134902702447906420, 0.002846536936597208849, 0.003558171170746511278, 0.004269805404895812839, 0.004981439639045115268, 0.005693073873194417697 ),
 .UNSPECIFIED. ) ;
#8275=DIRECTION ( 'NONE',  ( -0.000000000000000000, -0.000000000000000000, -1.000000000000000000 ) ) ;
#8276=LINE ( 'NONE', #6041, #9049 ) ;
#8278=DIRECTION ( 'NONE',  ( -0.000000000000000000, -0.000000000000000000, -1.000000000000000000 ) ) ;
#8288=ORIENTED_EDGE ( 'NONE', *, *, #2397, .F. ) ;
#8293=ORIENTED_EDGE ( 'NONE', *, *, #3162, .T. ) ;
#8304=CIRCLE ( 'NONE', #1672, 0.05999999999999990757 ) ;
#8305=CARTESIAN_POINT ( 'NONE',  ( 0.7350000851713975880, -0.4417469416942715332, 0.4439478790713853873 ) ) ;
#8318=CARTESIAN_POINT ( 'NONE',  ( 1.518565137009270316, -0.3790332973735661692, -0.4187650862911278526 ) ) ;
#8321=FACE_OUTER_BOUND ( 'NONE', #14273, .T. ) ;
#8325=EDGE_CURVE ( 'NONE', #11839, #8139, #10393, .T. ) ;
#8327=TOROIDAL_SURFACE ( 'NONE', #14163, 0.3203340137431718859, 0.05999999999999999778 ) ;
#8331=CARTESIAN_POINT ( 'NONE',  ( -5.764454660286586870E-18, -0.2214999999999999469, 0.000000000000000000 ) ) ;
#8336=ADVANCED_FACE ( 'NONE', ( #4580 ), #2605, .F. ) ;
#8337=CARTESIAN_POINT ( 'NONE',  ( 1.541692889559679314, 0.03598127022577071038, 0.4179989611391359827 ) ) ;
#8340=CARTESIAN_POINT ( 'NONE',  ( 1.814459835756289552, 0.1490781312163599881, -0.4743720362179413841 ) ) ;
#8344=ORIENTED_EDGE ( 'NONE', *, *, #697, .T. ) ;
#8367=CARTESIAN_POINT ( 'NONE',  ( 0.6583797813917272590, -0.06299305549640535351, -0.5137833636068753762 ) ) ;
#8370=CARTESIAN_POINT ( 'NONE',  ( -5.764454660286586870E-18, 0.04143956043956045082, 0.000000000000000000 ) ) ;
#8371=DIRECTION ( 'NONE',  ( -1.655665450705613915E-16, 0.000000000000000000, -1.000000000000000000 ) ) ;
#8372=VERTEX_POINT ( 'NONE', #113 ) ;
#8373=EDGE_CURVE ( 'NONE', #5982, #13550, #8960, .T. ) ;
#8374=CARTESIAN_POINT ( 'NONE',  ( 0.6676004498178099711, -0.4647306784022276482, 0.4667915867939526064 ) ) ;
#8384=CARTESIAN_POINT ( 'NONE',  ( 2.219979583769312814, -0.03321525116784886794, -0.4091553120912245767 ) ) ;
#8392=CARTESIAN_POINT ( 'NONE',  ( 1.000000000000000222, -0.4429999999999998939, -0.3182109165419975683 ) ) ;
#8400=ADVANCED_FACE ( 'NONE', ( #2272 ), #12138, .F. ) ;
#8404=ORIENTED_EDGE ( 'NONE', *, *, #14377, .T. ) ;
#8406=ORIENTED_EDGE ( 'NONE', *, *, #2088, .T. ) ;
#8413=VERTEX_POINT ( 'NONE', #262 ) ;
#8420=DIRECTION ( 'NONE',  ( -1.000000000000000000, 0.000000000000000000, 0.000000000000000000 ) ) ;
#8421=CARTESIAN_POINT ( 'NONE',  ( 0.7983174577546989781, -0.4429999999999999494, -0.4287183451209413132 ) ) ;
#8424=AXIS2_PLACEMENT_3D ( 'NONE', #5062, #7358, #1521 ) ;
#8425=ORIENTED_EDGE ( 'NONE', *, *, #3996, .F. ) ;
#8426=DIRECTION ( 'NONE',  ( 1.000000000000000000, 0.000000000000000000, 0.000000000000000000 ) ) ;
#8427=CARTESIAN_POINT ( 'NONE',  ( 8.475037399843312613, 0.9289129992088663856, -0.3802960819231170908 ) ) ;
#8428=ORIENTED_EDGE ( 'NONE', *, *, #7916, .F. ) ;
#8431=LINE ( 'NONE', #2460, #5090 ) ;
#8433=DIRECTION ( 'NONE',  ( -1.000000000000000000, -1.578435611247398256E-16, 0.000000000000000000 ) ) ;
#8435=CARTESIAN_POINT ( 'NONE',  ( 0.9652705920801474271, -0.4828330467331338749, -0.4119425203458967344 ) ) ;
#8436=ADVANCED_FACE ( 'NONE', ( #14346 ), #4964, .F. ) ;
#8437=CIRCLE ( 'NONE', #12321, 0.06000000000000001860 ) ;
#8438=DIRECTION ( 'NONE',  ( -0.01412288512831128343, 0.000000000000000000, 0.9999002670844990837 ) ) ;
#8439=( BOUNDED_SURFACE ( )  B_SPLINE_SURFACE ( 3, 2, ( 
 ( #4888, #14472, #9976 ),
 ( #8828, #14408, #3007 ),
 ( #14553, #463, #5160 ),
 ( #10610, #8340, #12972 ),
 ( #13398, #8605, #4003 ),
 ( #11834, #8671, #14637 ),
 ( #7597, #11110, #6026 ),
 ( #2935, #10690, #12256 ),
 ( #13243, #5227, #7522 ),
 ( #1700, #611, #7672 ) ),
 .UNSPECIFIED., .F., .F., .F. ) 
 B_SPLINE_SURFACE_WITH_KNOTS ( ( 4, 2, 2, 2, 4 ),
 ( 3, 3 ),
 ( 3.926990816987240063, 4.123340357836602799, 4.319689898685965090, 4.516039439535327382, 4.712388980384689674 ),
 ( 0.000000000000000000, 1.000000000000000000 ),
 .UNSPECIFIED. ) 
 GEOMETRIC_REPRESENTATION_ITEM ( )  RATIONAL_B_SPLINE_SURFACE ( (
 ( 1.000000000000000000, 0.7035672008258530008, 1.000000000000000000),
 ( 1.000000000000000000, 0.7037994241814377050, 1.000000000000000000),
 ( 1.000000000000000000, 0.7040544485608896119, 1.000000000000000000),
 ( 1.000000000000000000, 0.7046000480551916079, 1.000000000000000000),
 ( 1.000000000000000000, 0.7048906332649017559, 1.000000000000000000),
 ( 1.000000000000000000, 0.7054961263469431421, 1.000000000000000000),
 ( 1.000000000000000000, 0.7058110186547629228, 1.000000000000000000),
 ( 1.000000000000000000, 0.7064529522745538470, 1.000000000000000000),
 ( 1.000000000000000000, 0.7067799747770939778, 1.000000000000000000),
 ( 1.000000000000000000, 0.7071067811865475727, 1.000000000000000000) ) ) 
 REPRESENTATION_ITEM ( '' )  SURFACE ( )  );
#8443=DIRECTION ( 'NONE',  ( 0.000000000000000000, 0.000000000000000000, -1.000000000000000000 ) ) ;
#8447=CIRCLE ( 'NONE', #5509, 0.06999999999999823030 ) ;
#8451=CARTESIAN_POINT ( 'NONE',  ( 0.7006934119264054406, -0.03740617389313986157, 0.4858827016952782518 ) ) ;
#8455=CARTESIAN_POINT ( 'NONE',  ( 0.8044756265521625371, -0.4430000000000000049, -0.4357542965500932342 ) ) ;
#8456=CARTESIAN_POINT ( 'NONE',  ( 1.130901178792334205, -0.4429999999999999494, 0.4240763015380700773 ) ) ;
#8459=CIRCLE ( 'NONE', #12344, 0.1150000000000000050 ) ;
#8464=ORIENTED_EDGE ( 'NONE', *, *, #14977, .F. ) ;
#8466=CARTESIAN_POINT ( 'NONE',  ( 8.475037399843312613, 0.9289129992088663856, -0.3802960819231170353 ) ) ;
#8468=AXIS2_PLACEMENT_3D ( 'NONE', #5557, #8713, #6355 ) ;
#8482=ADVANCED_FACE ( 'NONE', ( #8694 ), #15070, .F. ) ;
#8483=CARTESIAN_POINT ( 'NONE',  ( 8.849999999999999645, 0.9399413264884247665, 6.829619984160658046E-17 ) ) ;
#8486=CARTESIAN_POINT ( 'NONE',  ( 3.602264755523620465, 1.056999999999999940, 0.4491205543005138412 ) ) ;
#8495=CARTESIAN_POINT ( 'NONE',  ( 0.8408323664393989594, -0.4817063029767711391, -0.4215754322849089575 ) ) ;
#8496=VECTOR ( 'NONE', #12117, 39.37007874015748854 ) ;
#8500=CARTESIAN_POINT ( 'NONE',  ( 0.6940273316166114537, -0.4844395604395604904, 0.4146485309448422751 ) ) ;
#8507=CARTESIAN_POINT ( 'NONE',  ( 0.6555107925675720537, -0.04007716038812948744, -0.5098556521091194282 ) ) ;
#8513=CARTESIAN_POINT ( 'NONE',  ( 0.6609716345676563964, 0.006273129652074246713, 0.4835254040074365989 ) ) ;
#8541=ADVANCED_FACE ( 'NONE', ( #4185 ), #10922, .T. ) ;
#8543=VERTEX_POINT ( 'NONE', #7694 ) ;
#8551=CARTESIAN_POINT ( 'NONE',  ( 2.633946444925666874, 0.3625193201794747466, 0.5000000000000000000 ) ) ;
#8555=EDGE_CURVE ( 'NONE', #2763, #13066, #2114, .T. ) ;
#8557=ORIENTED_EDGE ( 'NONE', *, *, #3747, .F. ) ;
#8564=EDGE_LOOP ( 'NONE', ( #4603, #10035, #11043, #13736, #310, #4953, #10496, #11114 ) ) ;
#8569=CARTESIAN_POINT ( 'NONE',  ( 0.8500459336821362122, -0.4777141770823781775, -0.4313442189758466272 ) ) ;
#8572=VERTEX_POINT ( 'NONE', #7923 ) ;
#8573=CARTESIAN_POINT ( 'NONE',  ( 0.6558215032553998958, -0.4245176963943231296, 0.5012403847680007019 ) ) ;
#8578=CARTESIAN_POINT ( 'NONE',  ( 0.6570838759023788223, -0.05534809311702808265, -0.5130260770772536727 ) ) ;
#8579=DIRECTION ( 'NONE',  ( -0.9999002670844991947, 0.000000000000000000, 0.01412288512831583534 ) ) ;
#8580=EDGE_LOOP ( 'NONE', ( #7584, #1812, #456, #4568, #12229 ) ) ;
#8581=CARTESIAN_POINT ( 'NONE',  ( -5.764454660286586870E-18, 0.1759999999999999065, -0.7057575716915831521 ) ) ;
#8582=CARTESIAN_POINT ( 'NONE',  ( 0.6558077255084613366, -0.01864179535143308669, 0.5013227096633768864 ) ) ;
#8585=ADVANCED_FACE ( 'NONE', ( #10005 ), #7502, .F. ) ;
#8591=AXIS2_PLACEMENT_3D ( 'NONE', #10282, #14942, #13775 ) ;
#8600=CARTESIAN_POINT ( 'NONE',  ( 2.045495128834867060, 0.3295048711651353268, -0.4105035982572215469 ) ) ;
#8601=FACE_OUTER_BOUND ( 'NONE', #12440, .T. ) ;
#8605=CARTESIAN_POINT ( 'NONE',  ( 1.749262710669750254, 0.1141659463772587563, -0.4752928995667935475 ) ) ;
#8606=ORIENTED_EDGE ( 'NONE', *, *, #5691, .T. ) ;
#8609=CARTESIAN_POINT ( 'NONE',  ( 8.792093969803303821, 0.8799778768673193197, -0.04156183585338790037 ) ) ;
#8620=ORIENTED_EDGE ( 'NONE', *, *, #12623, .F. ) ;
#8625=CARTESIAN_POINT ( 'NONE',  ( 0.4124999999999997558, -0.6590000000000000302, -0.3725000000000000533 ) ) ;
#8641=ORIENTED_EDGE ( 'NONE', *, *, #5139, .F. ) ;
#8649=CARTESIAN_POINT ( 'NONE',  ( 1.250000000000000000, 1.125000000000000000, 0.5000000000000000000 ) ) ;
#8650=EDGE_CURVE ( 'NONE', #14113, #2273, #12499, .T. ) ;
#8651=CARTESIAN_POINT ( 'NONE',  ( 0.7349234941866829018, -0.001280354426432115137, 0.4440226803674693912 ) ) ;
#8652=CARTESIAN_POINT ( 'NONE',  ( -0.3725000000000002198, -0.6290000000000005587, -0.3725000000000000533 ) ) ;
#8659=CARTESIAN_POINT ( 'NONE',  ( 0.7072031222531450778, -0.01850174782952182864, 0.4735570389444677675 ) ) ;
#8668=EDGE_CURVE ( 'NONE', #11754, #4318, #9700, .T. ) ;
#8671=CARTESIAN_POINT ( 'NONE',  ( 1.613287804444621276, 0.05773177243533618441, -0.4772134490897831927 ) ) ;
#8676=CARTESIAN_POINT ( 'NONE',  ( 8.729039508763628774, 0.8777759665679270018, -0.1953148678277565609 ) ) ;
#8678=ADVANCED_FACE ( 'NONE', ( #9231 ), #1619, .F. ) ;
#8683=VECTOR ( 'NONE', #1162, 39.37007874015748854 ) ;
#8694=FACE_OUTER_BOUND ( 'NONE', #4048, .T. ) ;
#8703=CIRCLE ( 'NONE', #10669, 0.7057575716915831521 ) ;
#8704=CARTESIAN_POINT ( 'NONE',  ( 8.840280274186266496, 0.9396554517976990484, 0.09865722066567160498 ) ) ;
#8705=CARTESIAN_POINT ( 'NONE',  ( 0.9082793173477334836, -0.4296060023189146038, -0.4649570271612626371 ) ) ;
#8709=ADVANCED_FACE ( 'NONE', ( #12884 ), #6522, .T. ) ;
#8713=DIRECTION ( 'NONE',  ( -2.602462600580851747E-17, -1.000000000000000000, 0.000000000000000000 ) ) ;
#8716=VERTEX_POINT ( 'NONE', #10526 ) ;
#8725=CARTESIAN_POINT ( 'NONE',  ( 0.6773748815706875925, -0.06659206035557797831, 0.4904325581699059966 ) ) ;
#8726=CARTESIAN_POINT ( 'NONE',  ( 0.9747916292782434766, -0.4829471944798794381, -0.3667554846915876410 ) ) ;
#8731=( CONVERSION_BASED_UNIT ( 'INCH', #7436 ) LENGTH_UNIT ( ) NAMED_UNIT ( #2954 ) );
#8738=ORIENTED_EDGE ( 'NONE', *, *, #4878, .F. ) ;
#8742=CARTESIAN_POINT ( 'NONE',  ( 1.518565137009187049, -0.3790332973735826005, 0.4187650862912378202 ) ) ;
#8743=CARTESIAN_POINT ( 'NONE',  ( 0.8108060929038567455, -0.4429999999999998939, -0.3024090436974092300 ) ) ;
#8768=EDGE_CURVE ( 'NONE', #2309, #7417, #12805, .T. ) ;
#8774=ORIENTED_EDGE ( 'NONE', *, *, #4555, .F. ) ;
#8778=EDGE_CURVE ( 'NONE', #9366, #3025, #8916, .T. ) ;
#8779=CARTESIAN_POINT ( 'NONE',  ( 2.715114969688405377, 0.8546659208690539078, 0.4012693820655806598 ) ) ;
#8785=CIRCLE ( 'NONE', #8065, 0.05999999999999997696 ) ;
#8787=CARTESIAN_POINT ( 'NONE',  ( 8.849999999999999645, 0.9399413264884969310, 0.04934655444147957593 ) ) ;
#8793=DIRECTION ( 'NONE',  ( -2.602462600580851747E-17, -1.000000000000000000, 0.000000000000000000 ) ) ;
#8799=PLANE ( 'NONE',  #10458 ) ;
#8800=CARTESIAN_POINT ( 'NONE',  ( 8.695322983473955603, 0.9353919960747725248, 0.3771847036232494066 ) ) ;
#8801=VERTEX_POINT ( 'NONE', #6167 ) ;
#8804=EDGE_CURVE ( 'NONE', #10756, #8139, #13324, .T. ) ;
#8808=CARTESIAN_POINT ( 'NONE',  ( 0.3724999999999999423, -0.6290000000000003366, 0.3724999999999999423 ) ) ;
#8812=DIRECTION ( 'NONE',  ( 1.000000000000000000, 0.000000000000000000, 0.000000000000000000 ) ) ;
#8813=ORIENTED_EDGE ( 'NONE', *, *, #5066, .F. ) ;
#8816=ORIENTED_EDGE ( 'NONE', *, *, #7082, .T. ) ;
#8824=LINE ( 'NONE', #13238, #6547 ) ;
#8825=FACE_OUTER_BOUND ( 'NONE', #10491, .T. ) ;
#8826=ORIENTED_EDGE ( 'NONE', *, *, #15122, .T. ) ;
#8828=CARTESIAN_POINT ( 'NONE',  ( 2.033926451083618581, 0.2322360065624563819, -0.4712722252671806555 ) ) ;
#8829=( BOUNDED_SURFACE ( )  B_SPLINE_SURFACE ( 3, 2, ( 
 ( #7381, #6226, #14469 ),
 ( #10890, #3998, #5156 ),
 ( #12252, #1763, #13391 ),
 ( #9816, #12327, #14707 ),
 ( #7518, #1842, #7445 ),
 ( #6527, #4076, #2852 ),
 ( #5084, #12185, #6451 ),
 ( #6379, #9746, #13465 ),
 ( #5224, #9888, #14546 ),
 ( #8743, #4161, #11106 ) ),
 .UNSPECIFIED., .F., .F., .F. ) 
 B_SPLINE_SURFACE_WITH_KNOTS ( ( 4, 2, 2, 2, 4 ),
 ( 3, 3 ),
 ( -1.734723475976807094E-18, 0.0004185101295155288113, 0.0008370202590310593573, 0.001255530388546589795, 0.001674040518062120449 ),
 ( 0.000000000000000000, 1.000000000000000000 ),
 .UNSPECIFIED. ) 
 GEOMETRIC_REPRESENTATION_ITEM ( )  RATIONAL_B_SPLINE_SURFACE ( (
 ( 1.000000000000000000, 0.7071067811865455743, 1.000000000000000000),
 ( 1.000000000000000000, 0.6772247906454890165, 1.000000000000000000),
 ( 1.000000000000000000, 0.6514134713743581218, 1.000000000000000000),
 ( 1.000000000000000000, 0.6151943024887206457, 1.000000000000000000),
 ( 1.000000000000000000, 0.6049727253982803976, 1.000000000000000000),
 ( 1.000000000000000000, 0.6047532838980109737, 1.000000000000000000),
 ( 1.000000000000000000, 0.6149432554843776710, 1.000000000000000000),
 ( 1.000000000000000000, 0.6512885360441196259, 1.000000000000000000),
 ( 1.000000000000000000, 0.6772121499288246138, 1.000000000000000000),
 ( 1.000000000000000000, 0.7071067811865454633, 1.000000000000000000) ) ) 
 REPRESENTATION_ITEM ( '' )  SURFACE ( )  );
#8832=ORIENTED_EDGE ( 'NONE', *, *, #5473, .F. ) ;
#8835=VERTEX_POINT ( 'NONE', #4949 ) ;
#8837=VECTOR ( 'NONE', #10351, 39.37007874015748143 ) ;
#8841=ORIENTED_EDGE ( 'NONE', *, *, #4842, .T. ) ;
#8859=PRODUCT ( 'Handle', 'Handle', '', ( #4967 ) ) ;
#8874=CARTESIAN_POINT ( 'NONE',  ( 5.296717816638158993, 3.110143505634317407, 0.3651816168881241720 ) ) ;
#8876=CARTESIAN_POINT ( 'NONE',  ( 2.320261876820363334, 0.5185714323014329885, -0.4672279395929326840 ) ) ;
#8889=CARTESIAN_POINT ( 'NONE',  ( 0.9684363542373335410, -0.4829999999999998184, -0.3436319188865934460 ) ) ;
#8892=CARTESIAN_POINT ( 'NONE',  ( 2.592367411162173063, 0.4049457270506676143, -0.4633846410852801023 ) ) ;
#8910=CARTESIAN_POINT ( 'NONE',  ( 0.7058998964907862161, -0.3830000000000000071, -0.4900296624789436950 ) ) ;
#8911=DIRECTION ( 'NONE',  ( -1.000000000000000000, 0.000000000000000000, 0.000000000000000000 ) ) ;
#8916=( BOUNDED_CURVE ( )  B_SPLINE_CURVE ( 3, ( #13870, #14109, #12732, #3486 ),
 .UNSPECIFIED., .F., .T. ) 
 B_SPLINE_CURVE_WITH_KNOTS ( ( 4, 4 ),
 ( 4.747295565424568764, 5.497787143782132624 ),
 .UNSPECIFIED. ) 
 CURVE ( )  GEOMETRIC_REPRESENTATION_ITEM ( )  RATIONAL_B_SPLINE_CURVE ( ( 1.000000000000000000, 0.9536117119880160864, 0.9536117119880160864, 1.000000000000000000 ) ) 
 REPRESENTATION_ITEM ( '' )  );
#8938=B_SPLINE_CURVE_WITH_KNOTS ( 'NONE', 3,
 ( #920, #3312, #12333, #838, #7750, #14860, #9057, #2153, #13544, #4461 ),
 .UNSPECIFIED., .F., .F.,
 ( 4, 2, 2, 2, 4 ),
 ( 0.000000000000000000, 0.0002748923109770301477, 0.0005497846219540602954, 0.0008246769329310904431, 0.001099569243908120591 ),
 .UNSPECIFIED. ) ;
#8948=DIRECTION ( 'NONE',  ( -0.01412288512831212997, 0.000000000000000000, 0.9999002670844990837 ) ) ;
#8949=DIRECTION ( 'NONE',  ( 1.365923996832131609E-16, -1.000000000000000000, -0.000000000000000000 ) ) ;
#8952=CARTESIAN_POINT ( 'NONE',  ( 0.007060738305901492935, -0.2214999999999999469, 0.4999002720578262782 ) ) ;
#8954=AXIS2_PLACEMENT_3D ( 'NONE', #11926, #10707, #8420 ) ;
#8957=CARTESIAN_POINT ( 'NONE',  ( 3.602264755523621353, 0.9969999999999997753, -0.4491205543005138412 ) ) ;
#8958=CARTESIAN_POINT ( 'NONE',  ( 1.000000000000000222, -0.4429999999999998939, -0.3182109165419976238 ) ) ;
#8960=CIRCLE ( 'NONE', #3589, 0.07000000000000047851 ) ;
#8961=CARTESIAN_POINT ( 'NONE',  ( 0.007060738305901492935, -0.2214999999999999469, 0.4999002720578262782 ) ) ;
#8968=DIRECTION ( 'NONE',  ( -0.000000000000000000, -1.000000000000000000, -0.000000000000000000 ) ) ;
#8975=CARTESIAN_POINT ( 'NONE',  ( 2.644772327656221833, 0.4573506435465171105, -0.4626444586489234512 ) ) ;
#8981=LINE ( 'NONE', #7824, #13146 ) ;
#8987=DIRECTION ( 'NONE',  ( -0.000000000000000000, 1.000000000000000000, -0.000000000000000000 ) ) ;
#8988=ORIENTED_EDGE ( 'NONE', *, *, #11960, .F. ) ;
#8990=CARTESIAN_POINT ( 'NONE',  ( 1.569329279054357151, -0.05999999999999996309, 0.4778343322167462603 ) ) ;
#8992=CARTESIAN_POINT ( 'NONE',  ( -0.3725000000000002198, -0.6290000000000005587, -0.4125000000000000333 ) ) ;
#8993=VECTOR ( 'NONE', #7702, 39.37007874015748143 ) ;
#8995=CARTESIAN_POINT ( 'NONE',  ( 0.6746193685512168470, -0.3871368118416071424, -0.4906972545532032326 ) ) ;
#8996=CARTESIAN_POINT ( 'NONE',  ( -5.764454660286586870E-18, 0.2159999999999999420, 0.000000000000000000 ) ) ;
#9009=CARTESIAN_POINT ( 'NONE',  ( 0.7810927279646683319, -0.4443615595214102099, -0.3417200794260679131 ) ) ;
#9011=DIRECTION ( 'NONE',  ( -1.000000000000000000, 0.000000000000000000, -0.000000000000000000 ) ) ;
#9012=ORIENTED_EDGE ( 'NONE', *, *, #10910, .F. ) ;
#9014=CARTESIAN_POINT ( 'NONE',  ( 1.000048944713735732, -0.4428998280398802612, -0.4293350073753851581 ) ) ;
#9024=ORIENTED_EDGE ( 'NONE', *, *, #2507, .F. ) ;
#9028=ORIENTED_EDGE ( 'NONE', *, *, #10356, .T. ) ;
#9033=FACE_OUTER_BOUND ( 'NONE', #14750, .T. ) ;
#9035=CARTESIAN_POINT ( 'NONE',  ( 3.348322488999905477, 0.9844945895120515988, -0.4527073094774025086 ) ) ;
#9036=CARTESIAN_POINT ( 'NONE',  ( 0.9751447534947045304, -0.4829432260179055136, -0.3788763210631934664 ) ) ;
#9037=ORIENTED_EDGE ( 'NONE', *, *, #8325, .T. ) ;
#9038=DIRECTION ( 'NONE',  ( 1.000000000000000000, 0.000000000000000000, -1.224646799147353207E-16 ) ) ;
#9041=AXIS2_PLACEMENT_3D ( 'NONE', #5817, #1128, #12689 ) ;
#9046=VERTEX_POINT ( 'NONE', #6463 ) ;
#9049=VECTOR ( 'NONE', #10849, 39.37007874015748143 ) ;
#9051=CARTESIAN_POINT ( 'NONE',  ( 0.6866570596051723152, -0.4820476896543666179, -0.4282026755330073375 ) ) ;
#9052=CARTESIAN_POINT ( 'NONE',  ( 0.4425000000000003375, 0.2159999999999999420, 0.3724999999999999423 ) ) ;
#9057=CARTESIAN_POINT ( 'NONE',  ( 0.8282255603916048869, -0.4835890072320069843, -0.3529491429379406631 ) ) ;
#9059=PLANE ( 'NONE',  #8221 ) ;
#9061=ORIENTED_EDGE ( 'NONE', *, *, #2217, .T. ) ;
#9063=CARTESIAN_POINT ( 'NONE',  ( -5.764454660286586870E-18, 0.2159999999999999420, 0.000000000000000000 ) ) ;
#9066=CARTESIAN_POINT ( 'NONE',  ( 0.7050899422473165812, -0.4211548882865318033, -0.4765263839844885996 ) ) ;
#9067=CARTESIAN_POINT ( 'NONE',  ( 0.9445547394994807666, -0.4333281022995865706, -0.4594661707618462598 ) ) ;
#9069=VERTEX_POINT ( 'NONE', #8992 ) ;
#9080=CARTESIAN_POINT ( 'NONE',  ( 0.7818484599429001980, -0.4435097816930692605, -0.3509885469871208974 ) ) ;
#9081=EDGE_CURVE ( 'NONE', #14657, #5216, #4323, .T. ) ;
#9094=ORIENTED_EDGE ( 'NONE', *, *, #8154, .T. ) ;
#9105=CARTESIAN_POINT ( 'NONE',  ( 2.956986065683827825, 0.9548522091764033437, -0.3979556114001199796 ) ) ;
#9106=CARTESIAN_POINT ( 'NONE',  ( 2.187203820042824542, 0.4712135623730921985, 0.4085020630706684974 ) ) ;
#9107=CIRCLE ( 'NONE', #6922, 0.05999999999999994227 ) ;
#9116=FACE_OUTER_BOUND ( 'NONE', #5766, .T. ) ;
#9120=CARTESIAN_POINT ( 'NONE',  ( 3.113342878570759531, 0.6489923502455472448, -0.4560262305286361673 ) ) ;
#9121=CARTESIAN_POINT ( 'NONE',  ( 1.886930864189484636, -0.2403504688573024906, 0.4733484341213513580 ) ) ;
#9123=LINE ( 'NONE', #3307, #13060 ) ;
#9126=ORIENTED_EDGE ( 'NONE', *, *, #2180, .T. ) ;
#9127=DIRECTION ( 'NONE',  ( 0.000000000000000000, 0.000000000000000000, -1.000000000000000000 ) ) ;
#9129=ORIENTED_EDGE ( 'NONE', *, *, #9714, .T. ) ;
#9141=CARTESIAN_POINT ( 'NONE',  ( 0.7013471289190510438, -0.4108388036608545679, -0.4834044059207726618 ) ) ;
#9142=CARTESIAN_POINT ( 'NONE',  ( 0.8999999999999999112, -0.6230000000000016636, -0.3750000000000000555 ) ) ;
#9145=AXIS2_PLACEMENT_3D ( 'NONE', #4748, #9423, #128 ) ;
#9146=AXIS2_PLACEMENT_3D ( 'NONE', #7141, #2461, #9354 ) ;
#9149=ORIENTED_EDGE ( 'NONE', *, *, #1090, .F. ) ;
#9151=ORIENTED_EDGE ( 'NONE', *, *, #3163, .F. ) ;
#9153=DIRECTION ( 'NONE',  ( 1.224646799147353207E-16, 0.000000000000000000, -1.000000000000000000 ) ) ;
#9157=ORIENTED_EDGE ( 'NONE', *, *, #13842, .F. ) ;
#9160=CARTESIAN_POINT ( 'NONE',  ( 0.6734872051250744285, -0.02989652563654837669, -0.4827143163826136396 ) ) ;
#9162=ADVANCED_FACE ( 'NONE', ( #2613 ), #14679, .T. ) ;
#9167=DIRECTION ( 'NONE',  ( 0.000000000000000000, -1.000000000000000000, 0.000000000000000000 ) ) ;
#9171=DIRECTION ( 'NONE',  ( -1.365923996832131609E-16, 1.000000000000000000, 0.000000000000000000 ) ) ;
#9174=DIRECTION ( 'NONE',  ( -0.9999002670844989726, 3.570356213862801578E-15, -0.01412288512831216640 ) ) ;
#9180=CARTESIAN_POINT ( 'NONE',  ( -0.3725000000000002198, -0.6590000000000000302, -0.4424999999999983391 ) ) ;
#9183=DIRECTION ( 'NONE',  ( -0.7070715176384851919, -0.7070715176384786416, -0.009986885842350882656 ) ) ;
#9184=EDGE_CURVE ( 'NONE', #11117, #8801, #10375, .T. ) ;
#9187=CARTESIAN_POINT ( 'NONE',  ( 1.250000000000000000, 0.000000000000000000, 0.5000000000000000000 ) ) ;
#9190=VECTOR ( 'NONE', #7420, 39.37007874015748143 ) ;
#9196=AXIS2_PLACEMENT_3D ( 'NONE', #13719, #8793, #502 ) ;
#9200=APPLICATION_CONTEXT ( 'automotive_design' ) ;
#9201=CARTESIAN_POINT ( 'NONE',  ( 3.319863249854039022, 0.6888833692903484351, -0.3931858364370118819 ) ) ;
#9203=CARTESIAN_POINT ( 'NONE',  ( 2.184227569363401233, 0.01449120636682154316, 0.4691493281163361395 ) ) ;
#9205=CARTESIAN_POINT ( 'NONE',  ( 8.800855648616872529, 0.9403204140914576126, 0.3156881446850350326 ) ) ;
#9208=CARTESIAN_POINT ( 'NONE',  ( 0.7010945348274502109, -0.4463672506600663281, 0.4266201320538802744 ) ) ;
#9214=AXIS2_PLACEMENT_3D ( 'NONE', #12435, #14807, #2097 ) ;
#9216=VERTEX_POINT ( 'NONE', #9508 ) ;
#9218=CARTESIAN_POINT ( 'NONE',  ( 3.388933043275772494, 0.7513023213622327390, 0.4521337140780258279 ) ) ;
#9223=VECTOR ( 'NONE', #11134, 39.37007874015748854 ) ;
#9231=FACE_OUTER_BOUND ( 'NONE', #14069, .T. ) ;
#9238=CARTESIAN_POINT ( 'NONE',  ( 0.6731911676472074335, -0.04506618701452713011, -0.4888638514297005688 ) ) ;
#9239=CARTESIAN_POINT ( 'NONE',  ( -0.4125000000000000333, 0.1859999999999983611, 0.3724999999999999423 ) ) ;
#9251=EDGE_CURVE ( 'NONE', #13964, #13774, #8437, .T. ) ;
#9254=ORIENTED_EDGE ( 'NONE', *, *, #9805, .F. ) ;
#9255=ORIENTED_EDGE ( 'NONE', *, *, #14082, .F. ) ;
#9266=CARTESIAN_POINT ( 'NONE',  ( -0.7287617923574203349, -0.6590000000000000302, -0.8499999999999999778 ) ) ;
#9271=VECTOR ( 'NONE', #7218, 39.37007874015748143 ) ;
#9272=FACE_OUTER_BOUND ( 'NONE', #7831, .T. ) ;
#9279=VERTEX_POINT ( 'NONE', #13217 ) ;
#9281=VECTOR ( 'NONE', #4488, 39.37007874015748854 ) ;
#9287=CARTESIAN_POINT ( 'NONE',  ( 2.738674485065001551, 0.4577639129046691124, -0.4613181569906135149 ) ) ;
#9289=DIRECTION ( 'NONE',  ( -1.365923996832131609E-16, 1.000000000000000000, 0.000000000000000000 ) ) ;
#9292=CARTESIAN_POINT ( 'NONE',  ( 0.7051258599873114763, -0.4212171685758493433, 0.4764739269522876297 ) ) ;
#9293=DIRECTION ( 'NONE',  ( -0.9999002670844991947, 2.602203049398214110E-17, 0.01412288512831213171 ) ) ;
#9296=CARTESIAN_POINT ( 'NONE',  ( 3.390179639970223313, 0.6913388717410868800, 0.5000000000000000000 ) ) ;
#9298=CARTESIAN_POINT ( 'NONE',  ( 0.3724999999999997757, 0.2159999999999999420, -0.4425000000000005596 ) ) ;
#9305=DIRECTION ( 'NONE',  ( 1.655665450705613915E-16, 0.000000000000000000, 1.000000000000000000 ) ) ;
#9314=ORIENTED_EDGE ( 'NONE', *, *, #1090, .T. ) ;
#9316=EDGE_CURVE ( 'NONE', #10863, #3169, #14030, .T. ) ;
#9318=DIRECTION ( 'NONE',  ( -0.7070715176384847478, -0.7070715176384790857, 0.009986885842352487275 ) ) ;
#9319=CARTESIAN_POINT ( 'NONE',  ( -5.764454660286586870E-18, 0.1759999999999999065, 0.000000000000000000 ) ) ;
#9320=FACE_OUTER_BOUND ( 'NONE', #10040, .T. ) ;
#9331=EDGE_CURVE ( 'NONE', #15092, #2489, #9794, .T. ) ;
#9332=DIRECTION ( 'NONE',  ( -0.000000000000000000, -0.000000000000000000, -1.000000000000000000 ) ) ;
#9336=EDGE_CURVE ( 'NONE', #1080, #4626, #9896, .T. ) ;
#9340=FACE_OUTER_BOUND ( 'NONE', #2234, .T. ) ;
#9346=CARTESIAN_POINT ( 'NONE',  ( 8.472944879060717582, 0.9288399267729603448, 0.3803256373014023417 ) ) ;
#9348=VERTEX_POINT ( 'NONE', #10318 ) ;
#9351=ORIENTED_EDGE ( 'NONE', *, *, #10964, .T. ) ;
#9352=ORIENTED_EDGE ( 'NONE', *, *, #11669, .T. ) ;
#9354=DIRECTION ( 'NONE',  ( 0.000000000000000000, 0.000000000000000000, -1.000000000000000000 ) ) ;
#9357=( BOUNDED_SURFACE ( )  B_SPLINE_SURFACE ( 3, 2, ( 
 ( #2046, #6509, #5592 ),
 ( #12605, #6737, #8876 ),
 ( #4215, #897, #10255 ),
 ( #3144, #1976, #7807 ),
 ( #14913, #741, #7726 ),
 ( #9105, #10183, #12460 ),
 ( #3061, #4440, #10104 ),
 ( #13747, #3287, #9035 ),
 ( #5438, #11246, #7957 ),
 ( #4291, #13679, #8957 ) ),
 .UNSPECIFIED., .F., .F., .F. ) 
 B_SPLINE_SURFACE_WITH_KNOTS ( ( 4, 2, 2, 2, 4 ),
 ( 3, 3 ),
 ( 0.7853981633974462806, 0.9817477042468089055, 1.178097245096171530, 1.374446785945534044, 1.570796326794896558 ),
 ( 0.000000000000000000, 1.000000000000000000 ),
 .UNSPECIFIED. ) 
 GEOMETRIC_REPRESENTATION_ITEM ( )  RATIONAL_B_SPLINE_SURFACE ( (
 ( 1.000000000000000000, 0.7035672008258542220, 1.000000000000000000),
 ( 1.000000000000000000, 0.7037994241808144258, 1.000000000000000000),
 ( 1.000000000000000000, 0.7040544485617191706, 1.000000000000000000),
 ( 1.000000000000000000, 0.7046000480543618272, 1.000000000000000000),
 ( 1.000000000000000000, 0.7048906332660594964, 1.000000000000000000),
 ( 1.000000000000000000, 0.7054961263457840692, 1.000000000000000000),
 ( 1.000000000000000000, 0.7058110186534256592, 1.000000000000000000),
 ( 1.000000000000000000, 0.7064529522758904445, 1.000000000000000000),
 ( 1.000000000000000000, 0.7067799747760905582, 1.000000000000000000),
 ( 1.000000000000000000, 0.7071067811865475727, 1.000000000000000000) ) ) 
 REPRESENTATION_ITEM ( '' )  SURFACE ( )  );
#9361=ORIENTED_EDGE ( 'NONE', *, *, #8650, .F. ) ;
#9362=CARTESIAN_POINT ( 'NONE',  ( 0.7026382878072456872, -0.3911443797526893973, 0.4896667335905586227 ) ) ;
#9366=VERTEX_POINT ( 'NONE', #11387 ) ;
#9367=EDGE_CURVE ( 'NONE', #9653, #9554, #8209, .T. ) ;
#9373=ORIENTED_EDGE ( 'NONE', *, *, #10322, .F. ) ;
#9379=EDGE_CURVE ( 'NONE', #4605, #10756, #8447, .T. ) ;
#9388=CARTESIAN_POINT ( 'NONE',  ( 0.3724999999999997757, 0.2159999999999999698, -0.4125000000000000333 ) ) ;
#9392=ORIENTED_EDGE ( 'NONE', *, *, #13320, .T. ) ;
#9395=VECTOR ( 'NONE', #8043, 39.37007874015748143 ) ;
#9407=EDGE_CURVE ( 'NONE', #259, #1274, #6024, .T. ) ;
#9413=FACE_OUTER_BOUND ( 'NONE', #12595, .T. ) ;
#9415=FACE_OUTER_BOUND ( 'NONE', #9696, .T. ) ;
#9418=DIRECTION ( 'NONE',  ( -0.9999002670844990837, 5.351333901719070118E-15, 0.01412288512831215426 ) ) ;
#9423=DIRECTION ( 'NONE',  ( -0.7070715176384830825, -0.7070715176384807510, 0.009986885842350853165 ) ) ;
#9424=ORIENTED_EDGE ( 'NONE', *, *, #7782, .T. ) ;
#9427=EDGE_LOOP ( 'NONE', ( #4692, #9024, #13504, #8641 ) ) ;
#9430=EDGE_CURVE ( 'NONE', #9069, #2309, #6808, .T. ) ;
#9435=CARTESIAN_POINT ( 'NONE',  ( 0.3724999999999999423, 0.2159999999999999420, 0.4425000000000003930 ) ) ;
#9448=ORIENTED_EDGE ( 'NONE', *, *, #12871, .T. ) ;
#9455=CARTESIAN_POINT ( 'NONE',  ( 1.625945750339073292, -0.2839166429012424109, -0.4770346645432335664 ) ) ;
#9472=CARTESIAN_POINT ( 'NONE',  ( 1.844710921988372831, 0.09661955516503824282, 0.4739447609888647328 ) ) ;
#9474=CIRCLE ( 'NONE', #4589, 0.7173254825712085392 ) ;
#9479=ORIENTED_EDGE ( 'NONE', *, *, #12325, .T. ) ;
#9482=EDGE_LOOP ( 'NONE', ( #4407, #9392, #8095, #7600 ) ) ;
#9489=AXIS2_PLACEMENT_3D ( 'NONE', #284, #7140, #13994 ) ;
#9507=CARTESIAN_POINT ( 'NONE',  ( -0.3725000000000000533, 0.2159999999999999420, 0.3724999999999999423 ) ) ;
#9508=CARTESIAN_POINT ( 'NONE',  ( 2.592367411162173507, 0.4049457270506671147, 0.4633846410852800468 ) ) ;
#9513=( BOUNDED_SURFACE ( )  B_SPLINE_SURFACE ( 3, 2, ( 
 ( #607, #13467, #3004 ),
 ( #12328, #1843, #6529 ),
 ( #11185, #687, #5385 ),
 ( #758, #5458, #14162 ) ),
 .UNSPECIFIED., .F., .F., .F. ) 
 B_SPLINE_SURFACE_WITH_KNOTS ( ( 4, 4 ),
 ( 3, 3 ),
 ( -3.252606517456513302E-18, 0.0001672156045178513220 ),
 ( 0.000000000000000000, 1.000000000000000000 ),
 .UNSPECIFIED. ) 
 GEOMETRIC_REPRESENTATION_ITEM ( )  RATIONAL_B_SPLINE_SURFACE ( (
 ( 1.000000000000000000, 0.7075975758264662074, 1.000000000000000000),
 ( 1.000000000000000000, 0.7105806483792744821, 1.000000000000000000),
 ( 1.000000000000000000, 0.7138423292275878351, 1.000000000000000000),
 ( 1.000000000000000000, 0.7173416231802122178, 1.000000000000000000) ) ) 
 REPRESENTATION_ITEM ( '' )  SURFACE ( )  );
#9515=CIRCLE ( 'NONE', #12914, 0.6412116890856960350 ) ;
#9516=CARTESIAN_POINT ( 'NONE',  ( 0.9749999999999999778, -0.4829448521957645513, -0.3750000000000000555 ) ) ;
#9527=ORIENTED_EDGE ( 'NONE', *, *, #9407, .F. ) ;
#9531=ADVANCED_FACE ( 'NONE', ( #736 ), #15023, .F. ) ;
#9535=DIRECTION ( 'NONE',  ( 0.000000000000000000, -1.000000000000000000, 0.000000000000000000 ) ) ;
#9538=VERTEX_POINT ( 'NONE', #12981 ) ;
#9539=ORIENTED_EDGE ( 'NONE', *, *, #12713, .F. ) ;
#9540=ORIENTED_EDGE ( 'NONE', *, *, #4853, .F. ) ;
#9543=( BOUNDED_CURVE ( )  B_SPLINE_CURVE ( 3, ( #64, #7571, #1668, #6360 ),
 .UNSPECIFIED., .F., .F. ) 
 B_SPLINE_CURVE_WITH_KNOTS ( ( 4, 4 ),
 ( 4.712388980384689674, 5.497787143782139729 ),
 .UNSPECIFIED. ) 
 CURVE ( )  GEOMETRIC_REPRESENTATION_ITEM ( )  RATIONAL_B_SPLINE_CURVE ( ( 1.000000000000000000, 0.9492530216741910110, 0.9492530216741910110, 1.000000000000000000 ) ) 
 REPRESENTATION_ITEM ( '' )  );
#9549=CARTESIAN_POINT ( 'NONE',  ( 1.993930392107535754, 0.2778841324402123725, 0.4718371413544162341 ) ) ;
#9550=CARTESIAN_POINT ( 'NONE',  ( -0.4125000000000001998, 0.1859999999999983611, -0.3725000000000000533 ) ) ;
#9554=VERTEX_POINT ( 'NONE', #10548 ) ;
#9556=EDGE_LOOP ( 'NONE', ( #14798, #3952, #8832, #12246 ) ) ;
#9567=B_SPLINE_CURVE_WITH_KNOTS ( 'NONE', 3,
 ( #8435, #1526, #2537, #13002 ),
 .UNSPECIFIED., .F., .F.,
 ( 4, 4 ),
 ( 0.000000000000000000, 0.0001090996491984598624 ),
 .UNSPECIFIED. ) ;
#9571=CARTESIAN_POINT ( 'NONE',  ( 8.559253539154882517, 0.8718469098602882328, 0.3109429831200923311 ) ) ;
#9575=EDGE_CURVE ( 'NONE', #2708, #2201, #10777, .T. ) ;
#9577=VERTEX_POINT ( 'NONE', #265 ) ;
#9584=CARTESIAN_POINT ( 'NONE',  ( 2.634365942216866152, 0.3629388174706738024, 0.4627914414941119436 ) ) ;
#9589=FACE_OUTER_BOUND ( 'NONE', #9556, .T. ) ;
#9601=EDGE_LOOP ( 'NONE', ( #6938, #14650, #8606, #14084 ) ) ;
#9606=EDGE_CURVE ( 'NONE', #3169, #9554, #7122, .T. ) ;
#9608=EDGE_CURVE ( 'NONE', #498, #4318, #14285, .T. ) ;
#9609=ORIENTED_EDGE ( 'NONE', *, *, #10072, .T. ) ;
#9612=CARTESIAN_POINT ( 'NONE',  ( 1.014081760637643104, -0.4429513723158955973, -0.3902785865519532438 ) ) ;
#9614=CARTESIAN_POINT ( 'NONE',  ( 3.080868217518119678, 0.9969999999999996643, 0.4564849121819474220 ) ) ;
#9617=ORIENTED_EDGE ( 'NONE', *, *, #2286, .T. ) ;
#9626=ORIENTED_EDGE ( 'NONE', *, *, #3291, .T. ) ;
#9627=CARTESIAN_POINT ( 'NONE',  ( 0.3724999999999999423, 0.2159999999999999420, 0.4425000000000003930 ) ) ;
#9634=EDGE_LOOP ( 'NONE', ( #9314, #6312 ) ) ;
#9642=CARTESIAN_POINT ( 'NONE',  ( 0.8664489288624988017, -0.4696205524674798015, -0.4424002136836096000 ) ) ;
#9647=CARTESIAN_POINT ( 'NONE',  ( 0.6867356290494766036, -0.4821011294950960369, 0.4280493037418064417 ) ) ;
#9651=LINE ( 'NONE', #8208, #5579 ) ;
#9652=CARTESIAN_POINT ( 'NONE',  ( 3.249780665369845778, 0.6798122612590481451, 0.3942284963567643241 ) ) ;
#9653=VERTEX_POINT ( 'NONE', #5180 ) ;
#9658=CARTESIAN_POINT ( 'NONE',  ( 0.6566194192392924567, -0.01184293933552419895, 0.4974488347804321142 ) ) ;
#9666=DIRECTION ( 'NONE',  ( 1.874307916738608820E-16, -1.000000000000000000, -0.000000000000000000 ) ) ;
#9667=EDGE_LOOP ( 'NONE', ( #14633, #3664, #9129, #3046 ) ) ;
#9668=VECTOR ( 'NONE', #10346, 39.37007874015748143 ) ;
#9669=CIRCLE ( 'NONE', #3547, 0.06000000000000001166 ) ;
#9676=LINE ( 'NONE', #2559, #12645 ) ;
#9677=CARTESIAN_POINT ( 'NONE',  ( 2.229630226914017577, 0.4287871555018993863, -0.4085020630706684974 ) ) ;
#9685=CARTESIAN_POINT ( 'NONE',  ( 8.665761398406338856, 0.8755662462622739728, -0.3295708899403233527 ) ) ;
#9692=VECTOR ( 'NONE', #3909, 39.37007874015748143 ) ;
#9696=EDGE_LOOP ( 'NONE', ( #961, #5656, #13008, #12225 ) ) ;
#9700=CIRCLE ( 'NONE', #3104, 0.8499999999999999778 ) ;
#9706=EDGE_CURVE ( 'NONE', #2309, #13167, #12331, .T. ) ;
#9714=EDGE_CURVE ( 'NONE', #251, #13167, #7550, .T. ) ;
#9724=CARTESIAN_POINT ( 'NONE',  ( 0.6552635435737792502, -0.03280443401857551650, 0.5075266421723674259 ) ) ;
#9736=AXIS2_PLACEMENT_3D ( 'NONE', #13724, #12660, #1955 ) ;
#9739=ADVANCED_FACE ( 'NONE', ( #1501 ), #2669, .T. ) ;
#9744=CARTESIAN_POINT ( 'NONE',  ( 0.7435009325572420336, -0.6334543218446812007, 0.000000000000000000 ) ) ;
#9746=CARTESIAN_POINT ( 'NONE',  ( 0.8364764264237143365, -0.4366331065633826669, -0.3349451187573404543 ) ) ;
#9747=CIRCLE ( 'NONE', #11454, 0.3203340137431719414 ) ;
#9749=AXIS2_PLACEMENT_3D ( 'NONE', #3211, #3438, #7949 ) ;
#9757=CARTESIAN_POINT ( 'NONE',  ( 8.850000000000575184, 0.8820000000023066056, -0.04908333765187990194 ) ) ;
#9760=DIRECTION ( 'NONE',  ( 0.01412288512831213171, -3.675428035873182550E-19, -0.9999002670844991947 ) ) ;
#9775=ORIENTED_EDGE ( 'NONE', *, *, #4094, .F. ) ;
#9793=CARTESIAN_POINT ( 'NONE',  ( 0.6609607771814278721, 0.006241162926370197317, 0.4835552281312084921 ) ) ;
#9794=LINE ( 'NONE', #9946, #14531 ) ;
#9798=ADVANCED_FACE ( 'NONE', ( #11524 ), #4339, .F. ) ;
#9800=CARTESIAN_POINT ( 'NONE',  ( 0.7058998964907849949, -0.06000000000000026840, 0.4900296624789436950 ) ) ;
#9803=CARTESIAN_POINT ( 'NONE',  ( 2.034917172172060251, -0.2365099525741251041, -0.4116907716851759269 ) ) ;
#9805=EDGE_CURVE ( 'NONE', #184, #14657, #13624, .T. ) ;
#9809=VERTEX_POINT ( 'NONE', #1023 ) ;
#9812=CARTESIAN_POINT ( 'NONE',  ( 2.230477600021715467, 0.4287871555018996084, 0.4684960790957384824 ) ) ;
#9815=CARTESIAN_POINT ( 'NONE',  ( 1.127821516536285484, -0.3829999999995594151, 0.4840703175630468036 ) ) ;
#9816=CARTESIAN_POINT ( 'NONE',  ( 0.7809470991741572776, -0.4447677964980547571, -0.3372808541555822881 ) ) ;
#9824=ORIENTED_EDGE ( 'NONE', *, *, #12144, .T. ) ;
#9825=DIRECTION ( 'NONE',  ( 0.000000000000000000, -1.000000000000000000, 0.000000000000000000 ) ) ;
#9829=CARTESIAN_POINT ( 'NONE',  ( 8.695322983473955603, 0.9353919960747727469, -0.3771847036232491845 ) ) ;
#9831=AXIS2_PLACEMENT_3D ( 'NONE', #2392, #9293, #5761 ) ;
#9833=EDGE_CURVE ( 'NONE', #6905, #5216, #7302, .T. ) ;
#9849=EDGE_CURVE ( 'NONE', #1866, #8413, #12578, .T. ) ;
#9857=ORIENTED_EDGE ( 'NONE', *, *, #13660, .F. ) ;
#9859=CARTESIAN_POINT ( 'NONE',  ( 2.186775859711120873, 0.4707856020413885290, 0.4085081077081219592 ) ) ;
#9863=AXIS2_PLACEMENT_3D ( 'NONE', #12867, #10585, #3397 ) ;
#9868=CARTESIAN_POINT ( 'NONE',  ( 1.003158059735369090, -0.4829975555521401898, -0.4258273028168328422 ) ) ;
#9872=CARTESIAN_POINT ( 'NONE',  ( 0.6757896753473211504, -0.06125439598094604282, 0.4909021876970666720 ) ) ;
#9874=( GEOMETRIC_REPRESENTATION_CONTEXT ( 3 ) GLOBAL_UNCERTAINTY_ASSIGNED_CONTEXT ( ( #1248 ) ) GLOBAL_UNIT_ASSIGNED_CONTEXT ( ( #2906, #7720, #6426 ) ) REPRESENTATION_CONTEXT ( 'NONE', 'WORKASPACE' ) );
#9888=CARTESIAN_POINT ( 'NONE',  ( 0.8386818780009405172, -0.4394694382868568061, -0.3315263062002954952 ) ) ;
#9896=( BOUNDED_CURVE ( )  B_SPLINE_CURVE ( 3, ( #14447, #8800, #3975, #7642 ),
 .UNSPECIFIED., .F., .F. ) 
 B_SPLINE_CURVE_WITH_KNOTS ( ( 4, 4 ),
 ( 4.726512335037235779, 6.283185307179586232 ),
 .UNSPECIFIED. ) 
 CURVE ( )  GEOMETRIC_REPRESENTATION_ITEM ( )  RATIONAL_B_SPLINE_CURVE ( ( 1.000000000000000000, 0.8080549792898084061, 0.8080549792898084061, 1.000000000000000000 ) ) 
 REPRESENTATION_ITEM ( '' )  );
#9898=VERTEX_POINT ( 'NONE', #3572 ) ;
#9902=CARTESIAN_POINT ( 'NONE',  ( 8.664307099992953454, 0.9344797629247183490, -0.3304588241376550384 ) ) ;
#9912=VECTOR ( 'NONE', #6764, 39.37007874015748143 ) ;
#9916=ORIENTED_EDGE ( 'NONE', *, *, #14463, .T. ) ;
#9921=CARTESIAN_POINT ( 'NONE',  ( 2.088768908813758873, 0.2870784642939425146, -0.4704976142822915319 ) ) ;
#9929=AXIS2_PLACEMENT_3D ( 'NONE', #10192, #4448, #8054 ) ;
#9931=CARTESIAN_POINT ( 'NONE',  ( 0.7513246802501660770, -0.5029999999999998916, 0.4293820849162031661 ) ) ;
#9935=LINE ( 'NONE', #4122, #4017 ) ;
#9940=LINE ( 'NONE', #7494, #9190 ) ;
#9943=CARTESIAN_POINT ( 'NONE',  ( 0.6866196799637447334, 0.03902977929019532666, 0.4282732318476364930 ) ) ;
#9944=EDGE_CURVE ( 'NONE', #10100, #10863, #7173, .T. ) ;
#9945=SHAPE_REPRESENTATION_RELATIONSHIP ( 'NONE' , 'NONE' ,  #1014, #14219 ) ;
#9946=CARTESIAN_POINT ( 'NONE',  ( 0.6577550957999035441, -0.3830000000000000071, -0.4907096737881370130 ) ) ;
#9947=ORIENTED_EDGE ( 'NONE', *, *, #15049, .T. ) ;
#9953=CARTESIAN_POINT ( 'NONE',  ( 0.6583850202313106248, -0.06301572931163962332, 0.5137832895838605474 ) ) ;
#9954=CARTESIAN_POINT ( 'NONE',  ( 0.9705585225209942823, -0.4431353997581937709, -0.3488554439965182996 ) ) ;
#9957=LINE ( 'NONE', #6295, #41 ) ;
#9959=CARTESIAN_POINT ( 'NONE',  ( 8.469665986256828205, 1.056999999999999940, 6.829619984160658046E-17 ) ) ;
#9960=ORIENTED_EDGE ( 'NONE', *, *, #602, .F. ) ;
#9967=ADVANCED_FACE ( 'NONE', ( #14188 ), #8169, .T. ) ;
#9969=AXIS2_PLACEMENT_3D ( 'NONE', #12953, #10751, #2326 ) ;
#9973=ORIENTED_EDGE ( 'NONE', *, *, #2162, .T. ) ;
#9976=CARTESIAN_POINT ( 'NONE',  ( 2.045495128834867060, 0.3295048711651352713, -0.4105035982572216580 ) ) ;
#9979=LINE ( 'NONE', #9627, #1044 ) ;
#9982=ADVANCED_FACE ( 'NONE', ( #8094 ), #2342, .F. ) ;
#9985=CARTESIAN_POINT ( 'NONE',  ( 8.517841687953392693, 0.8704007761502546847, -0.3197150928555233529 ) ) ;
#9989=VECTOR ( 'NONE', #11731, 39.37007874015748143 ) ;
#9990=CARTESIAN_POINT ( 'NONE',  ( 0.6609716345676606153, -0.4492731296520721673, -0.4835254040074319359 ) ) ;
#9993=AXIS2_PLACEMENT_3D ( 'NONE', #11729, #1224, #910 ) ;
#9997=AXIS2_PLACEMENT_3D ( 'NONE', #8118, #6969, #9418 ) ;
#10000=VERTEX_POINT ( 'NONE', #13327 ) ;
#10005=FACE_OUTER_BOUND ( 'NONE', #377, .T. ) ;
#10008=DIRECTION ( 'NONE',  ( 0.000000000000000000, 0.000000000000000000, 1.000000000000000000 ) ) ;
#10011=CARTESIAN_POINT ( 'NONE',  ( 8.280000379048722224E-17, 0.2159999999999999420, 0.7057575716915831521 ) ) ;
#10017=CARTESIAN_POINT ( 'NONE',  ( 0.9484310486901441628, -0.4761373899265420317, -0.4326466961088093477 ) ) ;
#10025=ORIENTED_EDGE ( 'NONE', *, *, #12713, .T. ) ;
#10035=ORIENTED_EDGE ( 'NONE', *, *, #2107, .T. ) ;
#10040=EDGE_LOOP ( 'NONE', ( #8988, #6187, #2811, #8293 ) ) ;
#10049=FACE_OUTER_BOUND ( 'NONE', #14573, .T. ) ;
#10072=EDGE_CURVE ( 'NONE', #12211, #4169, #1653, .T. ) ;
#10073=ORIENTED_EDGE ( 'NONE', *, *, #3887, .F. ) ;
#10082=DIRECTION ( 'NONE',  ( 0.2251194151855832049, -0.9743259920144012876, 0.003179652756858328440 ) ) ;
#10085=EDGE_CURVE ( 'NONE', #12293, #6203, #4014, .T. ) ;
#10100=VERTEX_POINT ( 'NONE', #13254 ) ;
#10101=DIRECTION ( 'NONE',  ( 1.000000000000000000, 0.000000000000000000, 0.000000000000000000 ) ) ;
#10104=CARTESIAN_POINT ( 'NONE',  ( 3.099256572624759176, 0.9349522984524822888, -0.4562251896521926642 ) ) ;
#10105=CARTESIAN_POINT ( 'NONE',  ( 1.008061589492043719, -0.4429852717212066637, -0.3350037431595069282 ) ) ;
#10107=DIRECTION ( 'NONE',  ( 0.9999002670844989726, 0.000000000000000000, -0.01412288512831216640 ) ) ;
#10113=CARTESIAN_POINT ( 'NONE',  ( 0.7058998964907862161, -0.3830000000000000071, 0.4900296624789436950 ) ) ;
#10116=DIRECTION ( 'NONE',  ( 0.9999002670844991947, -2.602203049398214110E-17, 0.01412288512831213171 ) ) ;
#10118=FACE_OUTER_BOUND ( 'NONE', #5146, .T. ) ;
#10130=DIRECTION ( 'NONE',  ( -1.874307916738606601E-16, 1.000000000000000000, 0.000000000000000000 ) ) ;
#10131=ORIENTED_EDGE ( 'NONE', *, *, #3934, .F. ) ;
#10134=ORIENTED_EDGE ( 'NONE', *, *, #14233, .F. ) ;
#10141=CIRCLE ( 'NONE', #3546, 0.04000000000000006328 ) ;
#10144=ORIENTED_EDGE ( 'NONE', *, *, #5256, .T. ) ;
#10147=ORIENTED_EDGE ( 'NONE', *, *, #4853, .T. ) ;
#10149=AXIS2_PLACEMENT_3D ( 'NONE', #11743, #1315, #7992 ) ;
#10152=CARTESIAN_POINT ( 'NONE',  ( 0.8712764764800380313, -1.315297834523746934, -0.4276878505061766922 ) ) ;
#10155=CARTESIAN_POINT ( 'NONE',  ( 2.837768005214870382, 0.5663408804686755893, 0.4003582515643820394 ) ) ;
#10156=DIRECTION ( 'NONE',  ( -0.9999002670844991947, -1.607565641772518678E-17, 0.01412288512831583534 ) ) ;
#10157=CARTESIAN_POINT ( 'NONE',  ( 8.474190026735612946, 0.9289129992088663856, 0.3203020658980472168 ) ) ;
#10161=CARTESIAN_POINT ( 'NONE',  ( 0.9065573155407952166, -0.4416294641957835831, -0.4501509288694744981 ) ) ;
#10164=ORIENTED_EDGE ( 'NONE', *, *, #10574, .T. ) ;
#10172=AXIS2_PLACEMENT_3D ( 'NONE', #7966, #8968, #12394 ) ;
#10175=EDGE_CURVE ( 'NONE', #1037, #4626, #8304, .T. ) ;
#10177=FACE_OUTER_BOUND ( 'NONE', #1322, .T. ) ;
#10183=CARTESIAN_POINT ( 'NONE',  ( 2.957700166090663885, 0.9550922613677363948, -0.4582245739254896533 ) ) ;
#10184=CARTESIAN_POINT ( 'NONE',  ( 0.9682536368877157074, -0.4829999999707417224, -0.3433101715744485971 ) ) ;
#10191=CIRCLE ( 'NONE', #7271, 0.03999999999999999389 ) ;
#10192=CARTESIAN_POINT ( 'NONE',  ( 0.4124999999999997558, -0.6590000000000000302, -0.4125000000000000333 ) ) ;
#10195=AXIS2_PLACEMENT_3D ( 'NONE', #12134, #7615, #1713 ) ;
#10212=CARTESIAN_POINT ( 'NONE',  ( 0.6555286510801260347, -0.4026824885229741136, -0.5099168278768623219 ) ) ;
#10223=AXIS2_PLACEMENT_3D ( 'NONE', #14418, #7462, #13111 ) ;
#10226=AXIS2_PLACEMENT_3D ( 'NONE', #9868, #7804, #7576 ) ;
#10228=CARTESIAN_POINT ( 'NONE',  ( 2.280218097287834311, 0.5641718375782867057, 0.4677935296993194214 ) ) ;
#10229=ORIENTED_EDGE ( 'NONE', *, *, #11770, .T. ) ;
#10231=FACE_OUTER_BOUND ( 'NONE', #5309, .T. ) ;
#10237=AXIS2_PLACEMENT_3D ( 'NONE', #8551, #8257, #4956 ) ;
#10247=CARTESIAN_POINT ( 'NONE',  ( 0.007908111413600218964, -0.2214999999999999469, 0.5598942880828960966 ) ) ;
#10251=DIRECTION ( 'NONE',  ( 0.7071067811865462405, -0.7071067811865489050, 0.000000000000000000 ) ) ;
#10255=CARTESIAN_POINT ( 'NONE',  ( 2.418884559267300727, 0.5995087936326214395, -0.4658349638521568359 ) ) ;
#10257=CARTESIAN_POINT ( 'NONE',  ( 8.661818191809109280, 0.8754285464536269989, 0.3176815264168136865 ) ) ;
#10261=DIRECTION ( 'NONE',  ( 0.4961857140186716753, -0.000000000000000000, 0.8682164115033652596 ) ) ;
#10264=AXIS2_PLACEMENT_3D ( 'NONE', #772, #8081, #8911 ) ;
#10270=CARTESIAN_POINT ( 'NONE',  ( -0.03836742111524548554, 0.6316479427872651042, -0.4405359281558275941 ) ) ;
#10273=CARTESIAN_POINT ( 'NONE',  ( -0.7435009325572419225, -0.6334543218446815338, -9.105260372192982189E-17 ) ) ;
#10282=CARTESIAN_POINT ( 'NONE',  ( -0.3725000000000002198, -0.6590000000000000302, -0.3725000000000000533 ) ) ;
#10285=CARTESIAN_POINT ( 'NONE',  ( 2.592367411162172619, 0.4049457270506669482, 0.4633846410852800468 ) ) ;
#10294=ORIENTED_EDGE ( 'NONE', *, *, #11655, .F. ) ;
#10300=CARTESIAN_POINT ( 'NONE',  ( 0.7905038590255393238, -0.4446454637884403871, -0.3161764760585322187 ) ) ;
#10301=CARTESIAN_POINT ( 'NONE',  ( 2.187203820042824098, 0.4712135623730924205, 0.4085020630706684974 ) ) ;
#10306=CARTESIAN_POINT ( 'NONE',  ( 0.6583927779709175532, -0.06304930530161369229, -0.5137831800632942647 ) ) ;
#10311=CARTESIAN_POINT ( 'NONE',  ( 3.390179639970223313, 0.6913388717410868800, 0.3921396980529558429 ) ) ;
#10318=CARTESIAN_POINT ( 'NONE',  ( 0.8999999999999999112, -0.6230000000000016636, -0.2999999999999999889 ) ) ;
#10321=CARTESIAN_POINT ( 'NONE',  ( 8.474191475755167957, 0.8688764771518150409, -0.3203316212763323567 ) ) ;
#10322=EDGE_CURVE ( 'NONE', #3025, #8103, #14392, .T. ) ;
#10334=MANIFOLD_SOLID_BREP ( 'Fillet4', #549 ) ;
#10335=ORIENTED_EDGE ( 'NONE', *, *, #1084, .T. ) ;
#10336=CARTESIAN_POINT ( 'NONE',  ( 3.601417382415921686, 0.9969999999999999973, -0.3891265382754440227 ) ) ;
#10337=EDGE_LOOP ( 'NONE', ( #13614, #4276, #3014, #9351, #6354, #8841, #14786, #14320, #3452, #7660, #10470, #11501, #695 ) ) ;
#10339=SPHERICAL_SURFACE ( 'NONE', #701, 0.8499999999999999778 ) ;
#10340=CARTESIAN_POINT ( 'NONE',  ( 2.917021349547980424, 0.5710164562864796789, -0.4587991334809999877 ) ) ;
#10341=CARTESIAN_POINT ( 'NONE',  ( 0.6894988814560869539, -0.4425276619544661894, -0.4465617225471331664 ) ) ;
#10346=DIRECTION ( 'NONE',  ( 1.655665450705613915E-16, 3.103226861728128995E-32, 1.000000000000000000 ) ) ;
#10349=DIRECTION ( 'NONE',  ( 0.000000000000000000, 0.000000000000000000, -1.000000000000000000 ) ) ;
#10351=DIRECTION ( 'NONE',  ( 0.000000000000000000, -0.7071067811865595631, 0.7071067811865354713 ) ) ;
#10354=AXIS2_PLACEMENT_3D ( 'NONE', #11393, #2127, #8193 ) ;
#10355=CARTESIAN_POINT ( 'NONE',  ( 3.096478849372236386, 0.7064487239733231450, 0.4562644230314655824 ) ) ;
#10356=EDGE_CURVE ( 'NONE', #12826, #1005, #12093, .T. ) ;
#10361=CARTESIAN_POINT ( 'NONE',  ( 0.8276409636798741642, -0.4389750926356451033, -0.4504658872936693204 ) ) ;
#10363=EDGE_CURVE ( 'NONE', #3778, #8716, #9747, .T. ) ;
#10371=VERTEX_POINT ( 'NONE', #7371 ) ;
#10374=DIRECTION ( 'NONE',  ( 0.7071067811865459074, -0.7071067811865492381, 0.000000000000000000 ) ) ;
#10375=CIRCLE ( 'NONE', #6968, 0.8653656741516848605 ) ;
#10379=CARTESIAN_POINT ( 'NONE',  ( 0.6940259540059535714, 0.04143956037114119445, -0.4146509415068644899 ) ) ;
#10386=EDGE_LOOP ( 'NONE', ( #4124, #2585, #6975, #3423, #13307 ) ) ;
#10390=CIRCLE ( 'NONE', #14288, 0.8083085967350902568 ) ;
#10393=LINE ( 'NONE', #11614, #871 ) ;
#10395=( BOUNDED_SURFACE ( )  B_SPLINE_SURFACE ( 3, 2, ( 
 ( #2761, #8725, #9800 ),
 ( #9953, #9872, #7364 ),
 ( #2692, #4992, #14607 ),
 ( #7429, #6433, #2985 ),
 ( #14452, #3919, #4142 ),
 ( #8582, #1819, #14525 ),
 ( #9658, #13296, #5206 ),
 ( #13222, #3981, #2837 ),
 ( #8513, #6211, #12087 ),
 ( #13156, #13367, #6290 ),
 ( #2917, #366, #5068 ),
 ( #10946, #7578, #290 ),
 ( #441, #12164, #6366 ),
 ( #12017, #5142, #8651 ),
 ( #10873, #14307, #1678 ),
 ( #11019, #3842, #10800 ) ),
 .UNSPECIFIED., .F., .F., .F. ) 
 B_SPLINE_SURFACE_WITH_KNOTS ( ( 4, 2, 2, 2, 2, 2, 2, 4 ),
 ( 3, 3 ),
 ( 0.002083263661281777729, 0.002712596804664463811, 0.003341929948047149893, 0.003971263091429835974, 0.004600596234812522056, 0.005229929378195208138, 0.005859262521577894220, 0.007117928808343267251 ),
 ( 0.000000000000000000, 1.000000000000000000 ),
 .UNSPECIFIED. ) 
 GEOMETRIC_REPRESENTATION_ITEM ( )  RATIONAL_B_SPLINE_SURFACE ( (
 ( 1.000000000000000000, 0.8987017906623451236, 1.000000000000000000),
 ( 1.000000000000000000, 0.9020594141852221748, 1.000000000000000000),
 ( 1.000000000000000000, 0.9044651860912357177, 1.000000000000000000),
 ( 1.000000000000000000, 0.9073335834958523582, 1.000000000000000000),
 ( 1.000000000000000000, 0.9077660037302067719, 1.000000000000000000),
 ( 1.000000000000000000, 0.9065807100087762693, 1.000000000000000000),
 ( 1.000000000000000000, 0.9049576633627300914, 1.000000000000000000),
 ( 1.000000000000000000, 0.8998093858009506008, 1.000000000000000000),
 ( 1.000000000000000000, 0.8963317359660779582, 1.000000000000000000),
 ( 1.000000000000000000, 0.8876325024793222385, 1.000000000000000000),
 ( 1.000000000000000000, 0.8824894405371271899, 1.000000000000000000),
 ( 1.000000000000000000, 0.8708860455746204599, 1.000000000000000000),
 ( 1.000000000000000000, 0.8643359190951755977, 1.000000000000000000),
 ( 1.000000000000000000, 0.8432203508675353287, 1.000000000000000000),
 ( 1.000000000000000000, 0.8269334966168219170, 1.000000000000000000),
 ( 1.000000000000000000, 0.8091170061680454939, 1.000000000000000000) ) ) 
 REPRESENTATION_ITEM ( '' )  SURFACE ( )  );
#10399=ORIENTED_EDGE ( 'NONE', *, *, #9944, .F. ) ;
#10407=DIRECTION ( 'NONE',  ( 0.7071067811865450192, -0.7071067811865501263, 0.000000000000000000 ) ) ;
#10409=DIRECTION ( 'NONE',  ( -0.000000000000000000, -0.000000000000000000, -1.000000000000000000 ) ) ;
#10412=EDGE_CURVE ( 'NONE', #3646, #8801, #12088, .T. ) ;
#10418=AXIS2_PLACEMENT_3D ( 'NONE', #3407, #1654, #11067 ) ;
#10430=ADVANCED_FACE ( 'NONE', ( #11364 ), #2259, .T. ) ;
#10431=ORIENTED_EDGE ( 'NONE', *, *, #14383, .T. ) ;
#10432=AXIS2_PLACEMENT_3D ( 'NONE', #10679, #2420, #7103 ) ;
#10437=CARTESIAN_POINT ( 'NONE',  ( 1.519298119451390150, -0.3788322150374328068, -0.4785409870133183752 ) ) ;
#10450=DIRECTION ( 'NONE',  ( 0.000000000000000000, 0.000000000000000000, -1.000000000000000000 ) ) ;
#10451=CARTESIAN_POINT ( 'NONE',  ( 2.003951500898715654, -0.1834701832127830778, 0.4716956002697921257 ) ) ;
#10456=CARTESIAN_POINT ( 'NONE',  ( 0.7142320474717510637, -0.01055004872664746032, -0.4648272691893420294 ) ) ;
#10458=AXIS2_PLACEMENT_3D ( 'NONE', #1591, #14446, #6205 ) ;
#10459=CARTESIAN_POINT ( 'NONE',  ( 0.8999999999999999112, -0.4829999999999998739, -0.3750000000000000555 ) ) ;
#10467=ORIENTED_EDGE ( 'NONE', *, *, #9608, .T. ) ;
#10470=ORIENTED_EDGE ( 'NONE', *, *, #1065, .T. ) ;
#10475=VECTOR ( 'NONE', #1071, 39.37007874015748143 ) ;
#10477=DIRECTION ( 'NONE',  ( 0.9992912762382413216, 0.03489602031262311471, 0.01411428356268702201 ) ) ;
#10479=EDGE_CURVE ( 'NONE', #8413, #5428, #6635, .T. ) ;
#10483=VECTOR ( 'NONE', #10477, 39.37007874015748854 ) ;
#10490=B_SPLINE_CURVE_WITH_KNOTS ( 'NONE', 3,
 ( #13168, #2707, #13384, #14241, #8451, #7376, #14464, #8659, #14398, #1537, #6221, #10886, #12248, #2847 ),
 .UNSPECIFIED., .F., .F.,
 ( 4, 2, 2, 2, 2, 2, 4 ),
 ( 8.673617379884035472E-19, 0.0003612929182777952029, 0.0007225858365555895384, 0.001083878754833383874, 0.001445171673111178209, 0.002167757509666766880, 0.002890343346222355551 ),
 .UNSPECIFIED. ) ;
#10491=EDGE_LOOP ( 'NONE', ( #466, #708, #3354, #5949 ) ) ;
#10492=AXIS2_PLACEMENT_3D ( 'NONE', #829, #5528, #14848 ) ;
#10496=ORIENTED_EDGE ( 'NONE', *, *, #5785, .T. ) ;
#10499=CARTESIAN_POINT ( 'NONE',  ( -5.764454660286586870E-18, -0.2214999999999999469, 0.000000000000000000 ) ) ;
#10500=EDGE_CURVE ( 'NONE', #14149, #12577, #8785, .T. ) ;
#10504=LINE ( 'NONE', #15152, #9989 ) ;
#10507=CARTESIAN_POINT ( 'NONE',  ( 0.6558154374103718487, -0.4244538358989483617, 0.5012742423172266149 ) ) ;
#10520=DIRECTION ( 'NONE',  ( -1.000000000000000000, -1.837151692781460616E-16, 0.000000000000000000 ) ) ;
#10522=VERTEX_POINT ( 'NONE', #5482 ) ;
#10526=CARTESIAN_POINT ( 'NONE',  ( 8.789999999999999147, 1.056999999999999940, 6.829619984160658046E-17 ) ) ;
#10538=AXIS2_PLACEMENT_3D ( 'NONE', #7539, #547, #1303 ) ;
#10543=VERTEX_POINT ( 'NONE', #5788 ) ;
#10548=CARTESIAN_POINT ( 'NONE',  ( 0.8249999999999999556, -0.4829999999999998739, -0.3750000000000000555 ) ) ;
#10553=FACE_OUTER_BOUND ( 'NONE', #10337, .T. ) ;
#10556=DIRECTION ( 'NONE',  ( -1.000000000000000000, 0.000000000000000000, 0.000000000000000000 ) ) ;
#10562=ORIENTED_EDGE ( 'NONE', *, *, #5796, .F. ) ;
#10564=CARTESIAN_POINT ( 'NONE',  ( 0.4124999999999999223, 0.1859999999999983611, 0.3724999999999999423 ) ) ;
#10568=FACE_OUTER_BOUND ( 'NONE', #9482, .T. ) ;
#10569=ORIENTED_EDGE ( 'NONE', *, *, #10853, .F. ) ;
#10573=CARTESIAN_POINT ( 'NONE',  ( 0.8999999999999999112, -0.4429999999999998939, -0.3750000000000000555 ) ) ;
#10574=EDGE_CURVE ( 'NONE', #2309, #14837, #13170, .T. ) ;
#10582=ORIENTED_EDGE ( 'NONE', *, *, #10500, .F. ) ;
#10585=DIRECTION ( 'NONE',  ( -1.874307916738608820E-16, 1.000000000000000000, 0.000000000000000000 ) ) ;
#10588=VECTOR ( 'NONE', #13850, 39.37007874015748143 ) ;
#10589=CARTESIAN_POINT ( 'NONE',  ( 2.322097220811789597, 0.05061516561976652645, -0.4672020166538503050 ) ) ;
#10590=CARTESIAN_POINT ( 'NONE',  ( -0.3725000000000000533, -0.6590000000000000302, 0.3724999999999999423 ) ) ;
#10591=CARTESIAN_POINT ( 'NONE',  ( -0.4425000000000006706, 0.2159999999999999420, -0.3725000000000000533 ) ) ;
#10598=CARTESIAN_POINT ( 'NONE',  ( 1.008069866910759504, -0.4429852340093067831, -0.3350284807826328093 ) ) ;
#10601=CARTESIAN_POINT ( 'NONE',  ( 0.9652705920801474271, -0.4828330467331338749, -0.4119425203458967344 ) ) ;
#10602=CARTESIAN_POINT ( 'NONE',  ( 0.3724999999999997757, -0.6290000000000004476, -0.4125000000000000333 ) ) ;
#10606=DIRECTION ( 'NONE',  ( -1.000000000000000000, -1.689854595570744117E-16, 2.664535259100375303E-15 ) ) ;
#10608=LINE ( 'NONE', #9239, #3936 ) ;
#10610=CARTESIAN_POINT ( 'NONE',  ( 1.844710921988106378, 0.09661955516503979713, -0.4739447609888686741 ) ) ;
#10614=ORIENTED_EDGE ( 'NONE', *, *, #2195, .T. ) ;
#10623=VERTEX_POINT ( 'NONE', #9812 ) ;
#10632=DIRECTION ( 'NONE',  ( 0.000000000000000000, -0.000000000000000000, -1.000000000000000000 ) ) ;
#10644=DIRECTION ( 'NONE',  ( -1.365923996832131609E-16, 1.000000000000000000, 0.000000000000000000 ) ) ;
#10646=ORIENTED_EDGE ( 'NONE', *, *, #9367, .T. ) ;
#10648=CIRCLE ( 'NONE', #10149, 0.7406097974541305806 ) ;
#10667=CARTESIAN_POINT ( 'NONE',  ( 1.130901178792395934, -0.4430000000000001714, -0.4240763015376258216 ) ) ;
#10668=ADVANCED_FACE ( 'NONE', ( #10118 ), #1924, .T. ) ;
#10669=AXIS2_PLACEMENT_3D ( 'NONE', #9063, #766, #6539 ) ;
#10672=CARTESIAN_POINT ( 'NONE',  ( 0.6601485485260571995, -0.3723516483516483011, 0.5137583810202324131 ) ) ;
#10673=VECTOR ( 'NONE', #14902, 39.37007874015748143 ) ;
#10677=B_SPLINE_CURVE_WITH_KNOTS ( 'NONE', 3,
 ( #13689, #7971, #14701, #6671, #8889, #7818 ),
 .UNSPECIFIED., .F., .F.,
 ( 4, 2, 4 ),
 ( 0.0008693723071205420889, 0.001360522261323142672, 0.001851672215525743256 ),
 .UNSPECIFIED. ) ;
#10678=CARTESIAN_POINT ( 'NONE',  ( -0.3725000000000002198, 0.1859999999999983611, -0.4125000000000000333 ) ) ;
#10679=CARTESIAN_POINT ( 'NONE',  ( 7.623651669702752511E-17, -0.6589999999999998082, 0.000000000000000000 ) ) ;
#10682=CARTESIAN_POINT ( 'NONE',  ( 0.7072875780376989274, -0.01837860891257681734, -0.4734421766419254496 ) ) ;
#10690=CARTESIAN_POINT ( 'NONE',  ( 1.398131049395801906, 0.007369456331666564795, -0.4802523863080122579 ) ) ;
#10698=CIRCLE ( 'NONE', #14875, 0.03999999999999998002 ) ;
#10700=CARTESIAN_POINT ( 'NONE',  ( 0.4124999999999999223, -0.6290000000000003366, 0.3724999999999999423 ) ) ;
#10704=CIRCLE ( 'NONE', #7296, 0.7173254825712085392 ) ;
#10707=DIRECTION ( 'NONE',  ( -1.874307916738608820E-16, 1.000000000000000000, 0.000000000000000000 ) ) ;
#10708=CARTESIAN_POINT ( 'NONE',  ( 0.7017867892446607581, 0.04143956043956044388, -0.4010711782184314678 ) ) ;
#10711=ORIENTED_EDGE ( 'NONE', *, *, #13123, .F. ) ;
#10712=CARTESIAN_POINT ( 'NONE',  ( 0.6592591305498914922, -0.4437908075296089216, 0.4883895785410081736 ) ) ;
#10721=CARTESIAN_POINT ( 'NONE',  ( 2.684185600478663503, 0.4127059874548060781, 0.4620877740044938009 ) ) ;
#10725=CIRCLE ( 'NONE', #11191, 0.07000000000000047851 ) ;
#10729=ADVANCED_FACE ( 'NONE', ( #6753 ), #10339, .T. ) ;
#10751=DIRECTION ( 'NONE',  ( 2.602462600580851747E-17, 1.000000000000000000, -0.000000000000000000 ) ) ;
#10756=VERTEX_POINT ( 'NONE', #4760 ) ;
#10775=EDGE_CURVE ( 'NONE', #4169, #14557, #14401, .T. ) ;
#10777=LINE ( 'NONE', #10700, #105 ) ;
#10786=CARTESIAN_POINT ( 'NONE',  ( 0.8552050450108602542, -0.4750535095564970001, -0.4355134298035638341 ) ) ;
#10791=LINE ( 'NONE', #5907, #8234 ) ;
#10793=ORIENTED_EDGE ( 'NONE', *, *, #1437, .T. ) ;
#10794=DIRECTION ( 'NONE',  ( -0.2251194151855828718, -0.9743259920144011765, -0.003179652756857814528 ) ) ;
#10796=CARTESIAN_POINT ( 'NONE',  ( 3.391025564058367525, 0.6913684120611767181, 0.4521041586997406325 ) ) ;
#10800=CARTESIAN_POINT ( 'NONE',  ( 0.7513246802501646338, 4.268512490100411279E-17, 0.4293820849162031661 ) ) ;
#10803=CARTESIAN_POINT ( 'NONE',  ( -5.764454660286586870E-18, 0.1956296296296295978, 0.000000000000000000 ) ) ;
#10806=CARTESIAN_POINT ( 'NONE',  ( 8.789999999999999147, 0.9399413264884247665, 6.829619984160658046E-17 ) ) ;
#10809=ORIENTED_EDGE ( 'NONE', *, *, #13155, .T. ) ;
#10810=EDGE_CURVE ( 'NONE', #13120, #12826, #13017, .T. ) ;
#10824=CARTESIAN_POINT ( 'NONE',  ( 8.477129920625907644, 0.8689790899078102537, -0.3802665265448318399 ) ) ;
#10829=LINE ( 'NONE', #8255, #6588 ) ;
#10830=EDGE_CURVE ( 'NONE', #12064, #1986, #9567, .T. ) ;
#10833=AXIS2_PLACEMENT_3D ( 'NONE', #12322, #10116, #14771 ) ;
#10836=CARTESIAN_POINT ( 'NONE',  ( 0.7034553201775799458, -0.4178655479186547117, -0.4790822413290380388 ) ) ;
#10839=CARTESIAN_POINT ( 'NONE',  ( 0.8999999999999999112, -0.4829999999999998739, -0.3750000000000000555 ) ) ;
#10849=DIRECTION ( 'NONE',  ( 0.000000000000000000, -0.7071067811865600072, 0.7071067811865350272 ) ) ;
#10852=CARTESIAN_POINT ( 'NONE',  ( 0.8852267783403774404, -0.4626342325507599162, -0.4488287372993887692 ) ) ;
#10853=EDGE_CURVE ( 'NONE', #8572, #498, #1410, .T. ) ;
#10860=ORIENTED_EDGE ( 'NONE', *, *, #10910, .T. ) ;
#10863=VERTEX_POINT ( 'NONE', #6286 ) ;
#10865=DIRECTION ( 'NONE',  ( 1.365923996832131609E-16, -1.000000000000000000, 0.000000000000000000 ) ) ;
#10869=DIRECTION ( 'NONE',  ( 0.000000000000000000, -0.000000000000000000, -1.000000000000000000 ) ) ;
#10873=CARTESIAN_POINT ( 'NONE',  ( 0.6940843099860303234, 0.04143956054457292176, 0.4145488311989756758 ) ) ;
#10877=CARTESIAN_POINT ( 'NONE',  ( 0.4424999999999979505, -0.6589999999999996971, -0.8500000000000000888 ) ) ;
#10886=CARTESIAN_POINT ( 'NONE',  ( 0.7371172985291578605, -0.0009284805720397705606, 0.4420151072446019125 ) ) ;
#10889=CARTESIAN_POINT ( 'NONE',  ( 0.9999999999999966693, -0.3829999999999998961, 0.4858757062146893402 ) ) ;
#10890=CARTESIAN_POINT ( 'NONE',  ( 0.7830035894062601365, -0.4429999999999999494, -0.3557498141818015713 ) ) ;
#10897=VERTEX_POINT ( 'NONE', #14303 ) ;
#10900=LINE ( 'NONE', #5092, #12353 ) ;
#10909=B_SPLINE_CURVE_WITH_KNOTS ( 'NONE', 3,
 ( #5198, #13362, #10941, #11011, #9724, #12300, #5271, #2905, #9793, #6425, #13512, #11078, #576, #9943, #5061, #12011 ),
 .UNSPECIFIED., .F., .F.,
 ( 4, 2, 2, 2, 2, 2, 2, 4 ),
 ( 0.000000000000000000, 0.0005886476847306626632, 0.001177295369461325326, 0.001765943054191987990, 0.002354590738922650653, 0.002943238423653313316, 0.003531886108383975979, 0.004709181477845301306 ),
 .UNSPECIFIED. ) ;
#10910=EDGE_CURVE ( 'NONE', #13774, #3778, #288, .T. ) ;
#10911=AXIS2_PLACEMENT_3D ( 'NONE', #14824, #7715, #3352 ) ;
#10916=ORIENTED_EDGE ( 'NONE', *, *, #10412, .T. ) ;
#10917=EDGE_CURVE ( 'NONE', #8716, #7260, #7776, .T. ) ;
#10919=DIRECTION ( 'NONE',  ( -1.365923996832131609E-16, 1.000000000000000000, 0.000000000000000000 ) ) ;
#10920=CARTESIAN_POINT ( 'NONE',  ( 1.250847373107698779, -0.05999999999999997696, -0.4823326642216426707 ) ) ;
#10922=CONICAL_SURFACE ( 'NONE', #13341, 0.05500000000000146438, 0.7853981633974547183 ) ;
#10924=CARTESIAN_POINT ( 'NONE',  ( 2.418884559267909129, 0.5995087936327320177, 0.4658349638521481761 ) ) ;
#10926=DIRECTION ( 'NONE',  ( 0.01412288512831128343, 0.000000000000000000, 0.9999002670844990837 ) ) ;
#10927=DIRECTION ( 'NONE',  ( -0.9999002670844991947, -1.365787769249574922E-16, 0.01412288512831213171 ) ) ;
#10934=ORIENTED_EDGE ( 'NONE', *, *, #3534, .F. ) ;
#10936=CARTESIAN_POINT ( 'NONE',  ( 2.599160627732594264, 0.7974701832127792933, -0.4632886916986921344 ) ) ;
#10938=VERTEX_POINT ( 'NONE', #11796 ) ;
#10941=CARTESIAN_POINT ( 'NONE',  ( 0.6570999327328048700, -0.05543034563825118000, 0.5130307608016103638 ) ) ;
#10942=DIRECTION ( 'NONE',  ( 0.000000000000000000, 0.000000000000000000, -1.000000000000000000 ) ) ;
#10946=CARTESIAN_POINT ( 'NONE',  ( 0.6735393331370996828, 0.02844630743745005588, 0.4543474816912275727 ) ) ;
#10947=DIRECTION ( 'NONE',  ( -0.000000000000000000, -1.000000000000000000, -0.000000000000000000 ) ) ;
#10949=EDGE_LOOP ( 'NONE', ( #10399, #3929, #4173, #13533, #7866 ) ) ;
#10964=EDGE_CURVE ( 'NONE', #10623, #9809, #6430, .T. ) ;
#10966=DIRECTION ( 'NONE',  ( -0.000000000000000000, 1.000000000000000000, -0.000000000000000000 ) ) ;
#10968=DIRECTION ( 'NONE',  ( 0.7070715176384831935, 0.7070715176384805289, -0.009986885842351453380 ) ) ;
#10969=STYLED_ITEM('',(#15185),#10334);
#10974=ORIENTED_EDGE ( 'NONE', *, *, #10363, .F. ) ;
#10980=CARTESIAN_POINT ( 'NONE',  ( 0.9749999999999999778, -0.6429999999999999050, -0.3750000000000000555 ) ) ;
#10984=FACE_OUTER_BOUND ( 'NONE', #1689, .T. ) ;
#10996=LINE ( 'NONE', #6188, #8993 ) ;
#10998=DIRECTION ( 'NONE',  ( -1.365923996832131609E-16, 1.000000000000000000, 0.000000000000000000 ) ) ;
#11001=CARTESIAN_POINT ( 'NONE',  ( 0.8444447451257305337, -0.4472863611497946423, -0.4262169690687090395 ) ) ;
#11011=CARTESIAN_POINT ( 'NONE',  ( 0.6555297760382670091, -0.04033343379914773597, 0.5099209754895145386 ) ) ;
#11015=CARTESIAN_POINT ( 'NONE',  ( -0.4125000000000000333, -0.6590000000000000302, 0.3724999999999999423 ) ) ;
#11019=CARTESIAN_POINT ( 'NONE',  ( 0.7017867892446607581, 0.04143956043956047164, 0.4010711782184315233 ) ) ;
#11020=DIRECTION ( 'NONE',  ( 0.000000000000000000, 0.000000000000000000, 1.000000000000000000 ) ) ;
#11027=ORIENTED_EDGE ( 'NONE', *, *, #14562, .F. ) ;
#11035=DIRECTION ( 'NONE',  ( 0.7071067811865497932, -0.7071067811865452413, 0.000000000000000000 ) ) ;
#11042=CARTESIAN_POINT ( 'NONE',  ( 8.840371647876699157, 0.8816637705349000820, -0.09817148304380067525 ) ) ;
#11043=ORIENTED_EDGE ( 'NONE', *, *, #2533, .T. ) ;
#11049=CARTESIAN_POINT ( 'NONE',  ( 2.414633059664291093, 0.1432059349181007413, 0.4658950132815778411 ) ) ;
#11052=ORIENTED_EDGE ( 'NONE', *, *, #1676, .T. ) ;
#11053=EDGE_LOOP ( 'NONE', ( #4653, #13443, #10073, #9973 ) ) ;
#11055=DIRECTION ( 'NONE',  ( -1.365923996832131609E-16, 1.000000000000000000, 0.000000000000000000 ) ) ;
#11061=CARTESIAN_POINT ( 'NONE',  ( 3.348322488999904145, 0.9844945895124916913, 0.4527073094774024531 ) ) ;
#11063=CARTESIAN_POINT ( 'NONE',  ( 2.633946444925666874, 0.3625193201794746356, -0.4033906250602100618 ) ) ;
#11067=DIRECTION ( 'NONE',  ( 0.8841960195243572240, 0.000000000000000000, 0.4671160445299247232 ) ) ;
#11068=CARTESIAN_POINT ( 'NONE',  ( 0.9317123296983564895, -0.4679219388635364463, -0.4432830823677768595 ) ) ;
#11078=CARTESIAN_POINT ( 'NONE',  ( 0.6735138268600963096, 0.02841772179894979516, 0.4544009417003765927 ) ) ;
#11080=( BOUNDED_CURVE ( )  B_SPLINE_CURVE ( 3, ( #7249, #5871, #10451, #4717 ),
 .UNSPECIFIED., .F., .F. ) 
 B_SPLINE_CURVE_WITH_KNOTS ( ( 4, 4 ),
 ( 4.712388980384689674, 5.497787143782132624 ),
 .UNSPECIFIED. ) 
 CURVE ( )  GEOMETRIC_REPRESENTATION_ITEM ( )  RATIONAL_B_SPLINE_CURVE ( ( 1.000000000000000000, 0.9492530216741918991, 0.9492530216741918991, 1.000000000000000000 ) ) 
 REPRESENTATION_ITEM ( '' )  );
#11087=EDGE_CURVE ( 'NONE', #7417, #14371, #3056, .T. ) ;
#11090=EDGE_CURVE ( 'NONE', #14804, #3133, #10725, .T. ) ;
#11092=ADVANCED_FACE ( 'NONE', ( #1896 ), #13595, .F. ) ;
#11093=CARTESIAN_POINT ( 'NONE',  ( 8.469665986256828205, 0.8689060174719044349, 6.829619984160658046E-17 ) ) ;
#11096=ORIENTED_EDGE ( 'NONE', *, *, #9336, .T. ) ;
#11098=LINE ( 'NONE', #12319, #4790 ) ;
#11100=EDGE_CURVE ( 'NONE', #1733, #1986, #6559, .T. ) ;
#11103=ORIENTED_EDGE ( 'NONE', *, *, #9606, .T. ) ;
#11106=CARTESIAN_POINT ( 'NONE',  ( 0.8418300605894719624, -0.4829999999999998739, -0.3276580719765713190 ) ) ;
#11110=CARTESIAN_POINT ( 'NONE',  ( 1.542522555076166313, 0.03620193991704893921, -0.4782129582615927132 ) ) ;
#11114=ORIENTED_EDGE ( 'NONE', *, *, #602, .T. ) ;
#11116=CARTESIAN_POINT ( 'NONE',  ( 8.783907589752294243, 0.8796920021765863851, -0.08309344507350861775 ) ) ;
#11117=VERTEX_POINT ( 'NONE', #2983 ) ;
#11131=CIRCLE ( 'NONE', #608, 0.06000000000000004635 ) ;
#11133=ORIENTED_EDGE ( 'NONE', *, *, #9379, .F. ) ;
#11134=DIRECTION ( 'NONE',  ( -0.9999002670844989726, 2.602203049398213494E-17, -0.01412288512831212997 ) ) ;
#11138=CARTESIAN_POINT ( 'NONE',  ( 3.340400805683176877, 1.044207302812038440, 0.4528191976597221169 ) ) ;
#11141=CYLINDRICAL_SURFACE ( 'NONE', #2913, 0.06000000000000001860 ) ;
#11150=CARTESIAN_POINT ( 'NONE',  ( -5.764454660286586870E-18, 0.000000000000000000, 0.000000000000000000 ) ) ;
#11160=EDGE_LOOP ( 'NONE', ( #12974, #13416, #7262, #3652 ) ) ;
#11172=CARTESIAN_POINT ( 'NONE',  ( 0.7006931131589942963, -0.4056294202290754991, 0.4858697363291138438 ) ) ;
#11179=AXIS2_PLACEMENT_3D ( 'NONE', #3084, #1923, #4308 ) ;
#11185=CARTESIAN_POINT ( 'NONE',  ( 1.001118301508059583, -0.4429655524010116530, -0.4281838130439684642 ) ) ;
#11187=EDGE_CURVE ( 'NONE', #11754, #259, #5838, .T. ) ;
#11191=AXIS2_PLACEMENT_3D ( 'NONE', #7724, #13445, #12382 ) ;
#11195=CARTESIAN_POINT ( 'NONE',  ( 2.088768908813758873, 0.2870784642939425146, 0.4704976142822915319 ) ) ;
#11201=CARTESIAN_POINT ( 'NONE',  ( 0.7040121242107760802, -0.3870851776472034600, -0.4900563259292263218 ) ) ;
#11203=EDGE_CURVE ( 'NONE', #13460, #10938, #4821, .T. ) ;
#11214=ADVANCED_FACE ( 'NONE', ( #10177 ), #8191, .F. ) ;
#11217=CARTESIAN_POINT ( 'NONE',  ( 3.388087119187628282, 0.7512727810421430119, -0.4521456621583668234 ) ) ;
#11221=DIRECTION ( 'NONE',  ( 0.2251194151855830106, -0.9743259920144011765, -0.003179652756858232596 ) ) ;
#11222=CARTESIAN_POINT ( 'NONE',  ( 3.388085670168073715, 0.7513023213622326280, -0.3921396980529558429 ) ) ;
#11226=EDGE_CURVE ( 'NONE', #9279, #14642, #14910, .T. ) ;
#11228=CARTESIAN_POINT ( 'NONE',  ( 0.9644366315231677200, -0.4455811681533944912, -0.4137692285681027760 ) ) ;
#11234=ADVANCED_FACE ( 'NONE', ( #9033, #14053 ), #196, .F. ) ;
#11245=DIRECTION ( 'NONE',  ( -1.000000000000000000, 0.000000000000000000, 0.000000000000000000 ) ) ;
#11246=CARTESIAN_POINT ( 'NONE',  ( 3.471303878679115051, 1.057055486693973645, -0.4509702841989021715 ) ) ;
#11249=CARTESIAN_POINT ( 'NONE',  ( 8.066592045432399679E-17, 0.1759999999999999065, 0.7057575716915831521 ) ) ;
#11252=ORIENTED_EDGE ( 'NONE', *, *, #1553, .F. ) ;
#11276=CARTESIAN_POINT ( 'NONE',  ( 0.7070095302585194252, -0.4241756164644422400, -0.4738366780029937275 ) ) ;
#11278=DIRECTION ( 'NONE',  ( -0.000000000000000000, 1.000000000000000000, -0.000000000000000000 ) ) ;
#11293=CARTESIAN_POINT ( 'NONE',  ( 2.320261876819214919, 0.5185714323020406136, 0.4672279395929489487 ) ) ;
#11296=DIRECTION ( 'NONE',  ( -0.000000000000000000, 1.000000000000000000, -0.000000000000000000 ) ) ;
#11297=CARTESIAN_POINT ( 'NONE',  ( 0.9884490062245532283, -0.4415602900406226383, -0.4398366647702034449 ) ) ;
#11303=CARTESIAN_POINT ( 'NONE',  ( 0.6784300926939517140, -1.122412978718160259, -0.4304116694862061832 ) ) ;
#11315=DIRECTION ( 'NONE',  ( 0.000000000000000000, 0.7071067811865600072, 0.7071067811865350272 ) ) ;
#11317=CARTESIAN_POINT ( 'NONE',  ( 1.007158160401918190, -0.4429913151844830921, -0.4174182184235564197 ) ) ;
#11325=CARTESIAN_POINT ( 'NONE',  ( 0.7072875780376983723, -0.4246213910874223063, 0.4734421766419261157 ) ) ;
#11326=CARTESIAN_POINT ( 'NONE',  ( 1.250000000000000000, 0.000000000000000000, -0.4223386481965726302 ) ) ;
#11329=ORIENTED_EDGE ( 'NONE', *, *, #895, .T. ) ;
#11332=ADVANCED_FACE ( 'NONE', ( #3895 ), #14356, .T. ) ;
#11333=CARTESIAN_POINT ( 'NONE',  ( 0.7017867892446607581, -0.4844395604395603239, -0.4010711782184314678 ) ) ;
#11337=DIRECTION ( 'NONE',  ( -0.000000000000000000, 1.000000000000000000, -0.000000000000000000 ) ) ;
#11340=CARTESIAN_POINT ( 'NONE',  ( 0.7072031222531457439, -0.4244982521704789291, -0.4735570389444669348 ) ) ;
#11344=ORIENTED_EDGE ( 'NONE', *, *, #10917, .F. ) ;
#11355=VERTEX_POINT ( 'NONE', #2595 ) ;
#11363=DIRECTION ( 'NONE',  ( -0.7755991921403738720, 0.000000000000000000, 0.6312257069790484509 ) ) ;
#11364=FACE_OUTER_BOUND ( 'NONE', #12514, .T. ) ;
#11370=FACE_OUTER_BOUND ( 'NONE', #22, .T. ) ;
#11372=CARTESIAN_POINT ( 'NONE',  ( 8.792093969802149189, 0.8799778768672790186, 6.829619984160658046E-17 ) ) ;
#11387=CARTESIAN_POINT ( 'NONE',  ( 3.388933043275772494, 0.7513023213622327390, -0.4521337140780258279 ) ) ;
#11391=ADVANCED_FACE ( 'NONE', ( #9413 ), #11141, .T. ) ;
#11393=CARTESIAN_POINT ( 'NONE',  ( -0.0008473731076987472792, -0.3830000000000000626, -0.4400059839749300150 ) ) ;
#11394=CARTESIAN_POINT ( 'NONE',  ( 0.7513246802501661881, 0.05999999999999999778, -0.4293820849162031661 ) ) ;
#11395=DIRECTION ( 'NONE',  ( 0.000000000000000000, 0.000000000000000000, 1.000000000000000000 ) ) ;
#11401=EDGE_CURVE ( 'NONE', #9366, #9279, #2661, .T. ) ;
#11402=CARTESIAN_POINT ( 'NONE',  ( 0.7023896125859220296, -0.3918271903216897778, 0.4896155492289064881 ) ) ;
#11405=EDGE_LOOP ( 'NONE', ( #10164, #4579, #8428, #5687 ) ) ;
#11411=CARTESIAN_POINT ( 'NONE',  ( 0.7513246802501664101, -0.4429999999999999494, -0.4293820849162031106 ) ) ;
#11412=LINE ( 'NONE', #9052, #5248 ) ;
#11416=CARTESIAN_POINT ( 'NONE',  ( -0.3725000000000000533, 0.1859999999999983611, 0.4124999999999999223 ) ) ;
#11419=VERTEX_POINT ( 'NONE', #10011 ) ;
#11440=ADVANCED_FACE ( 'NONE', ( #5183 ), #12188, .T. ) ;
#11443=AXIS2_PLACEMENT_3D ( 'NONE', #13801, #3031, #9011 ) ;
#11447=CARTESIAN_POINT ( 'NONE',  ( 0.7819547768050734149, -0.4450707063672663111, -0.3325235620832113770 ) ) ;
#11449=VERTEX_POINT ( 'NONE', #12143 ) ;
#11451=CARTESIAN_POINT ( 'NONE',  ( 0.7022716438625531410, -0.02843846521930830026, -0.4812718407965440592 ) ) ;
#11452=AXIS2_PLACEMENT_3D ( 'NONE', #9205, #11800, #14083 ) ;
#11454=AXIS2_PLACEMENT_3D ( 'NONE', #9959, #14614, #8812 ) ;
#11472=CIRCLE ( 'NONE', #1447, 0.7057575716915831521 ) ;
#11489=CARTESIAN_POINT ( 'NONE',  ( -0.4425000000000005596, 0.2159999999999999420, 0.3724999999999999423 ) ) ;
#11495=CARTESIAN_POINT ( 'NONE',  ( 1.250000000000000000, 0.000000000000000000, 0.4223386481965726857 ) ) ;
#11499=DIRECTION ( 'NONE',  ( 0.9943395781194692695, 0.000000000000000000, -0.1062487806292197745 ) ) ;
#11501=ORIENTED_EDGE ( 'NONE', *, *, #1413, .T. ) ;
#11502=CARTESIAN_POINT ( 'NONE',  ( 0.7441558489118157427, -0.4430000000000000049, -0.4356293359425710832 ) ) ;
#11507=CARTESIAN_POINT ( 'NONE',  ( 3.314866445692599584, 0.7487158587810271992, 0.4531798524619689017 ) ) ;
#11509=CARTESIAN_POINT ( 'NONE',  ( 0.8622576496911000810, -0.4326094837641099589, -0.4616145281884125873 ) ) ;
#11512=VECTOR ( 'NONE', #14194, 39.37007874015748143 ) ;
#11524=FACE_OUTER_BOUND ( 'NONE', #6651, .T. ) ;
#11526=LINE ( 'NONE', #1025, #9281 ) ;
#11527=CARTESIAN_POINT ( 'NONE',  ( 0.6773748815706879256, -0.06659206035557820036, -0.4904325581699052750 ) ) ;
#11530=VECTOR ( 'NONE', #5409, 39.37007874015748143 ) ;
#11535=EDGE_LOOP ( 'NONE', ( #3050, #535, #2253, #10025 ) ) ;
#11543=ORIENTED_EDGE ( 'NONE', *, *, #11087, .T. ) ;
#11546=DIRECTION ( 'NONE',  ( 0.000000000000000000, 0.000000000000000000, 1.000000000000000000 ) ) ;
#11553=( BOUNDED_SURFACE ( )  B_SPLINE_SURFACE ( 3, 2, ( 
 ( #5421, #238, #1317 ),
 ( #8456, #14545, #9815 ),
 ( #604, #12104, #4075 ),
 ( #8742, #7666, #13390 ),
 ( #14706, #5756, #12543 ),
 ( #2066, #9121, #1921 ),
 ( #11566, #3305, #7978 ),
 ( #6606, #4531, #9203 ),
 ( #13843, #3383, #1069 ),
 ( #6987, #11049, #13481 ) ),
 .UNSPECIFIED., .F., .F., .F. ) 
 B_SPLINE_SURFACE_WITH_KNOTS ( ( 4, 2, 2, 2, 4 ),
 ( 3, 3 ),
 ( 4.712388980384689674, 4.908738521234050189, 5.105088062083410705, 5.301437602932772108, 5.497787143782132624 ),
 ( 0.000000000000000000, 1.000000000000000000 ),
 .UNSPECIFIED. ) 
 GEOMETRIC_REPRESENTATION_ITEM ( )  RATIONAL_B_SPLINE_SURFACE ( (
 ( 1.000000000000000000, 0.7071067811865475727, 1.000000000000000000),
 ( 1.000000000000000000, 0.7074335897363954739, 1.000000000000000000),
 ( 1.000000000000000000, 0.7077601512488349567, 1.000000000000000000),
 ( 1.000000000000000000, 0.7084003186185308110, 1.000000000000000000),
 ( 1.000000000000000000, 0.7087139042191036298, 1.000000000000000000),
 ( 1.000000000000000000, 0.7093161336544245854, 1.000000000000000000),
 ( 1.000000000000000000, 0.7096047632059221399, 1.000000000000000000),
 ( 1.000000000000000000, 0.7101460984466749782, 1.000000000000000000),
 ( 1.000000000000000000, 0.7103988163344383544, 1.000000000000000000),
 ( 1.000000000000000000, 0.7106287314217416551, 1.000000000000000000) ) ) 
 REPRESENTATION_ITEM ( '' )  SURFACE ( )  );
#11557=DIRECTION ( 'NONE',  ( 1.000000000000000000, 0.000000000000000000, 0.000000000000000000 ) ) ;
#11560=CARTESIAN_POINT ( 'NONE',  ( 0.6733268703976358349, 0.02909690080488760294, -0.4545075337565437912 ) ) ;
#11563=CARTESIAN_POINT ( 'NONE',  ( 3.320735777595769989, 0.6889667851712865110, -0.4530969522937798311 ) ) ;
#11566=CARTESIAN_POINT ( 'NONE',  ( 2.002301348309616813, -0.1786631980419839394, 0.4121376268991519543 ) ) ;
#11570=LINE ( 'NONE', #5916, #10475 ) ;
#11573=FACE_OUTER_BOUND ( 'NONE', #550, .T. ) ;
#11582=DIRECTION ( 'NONE',  ( -0.000000000000000000, 0.000000000000000000, -1.000000000000000000 ) ) ;
#11592=CARTESIAN_POINT ( 'NONE',  ( 3.388085670168073715, 0.7513023213622326280, 0.3921396980529558429 ) ) ;
#11594=DIRECTION ( 'NONE',  ( -0.000000000000000000, -1.000000000000000000, -0.000000000000000000 ) ) ;
#11595=CARTESIAN_POINT ( 'NONE',  ( 0.9482181556124942290, -0.4760276150436455467, -0.4328224131969262700 ) ) ;
#11597=EDGE_CURVE ( 'NONE', #6053, #9069, #11526, .T. ) ;
#11600=ORIENTED_EDGE ( 'NONE', *, *, #2043, .F. ) ;
#11603=DIRECTION ( 'NONE',  ( 0.000000000000000000, 0.000000000000000000, 1.000000000000000000 ) ) ;
#11611=ORIENTED_EDGE ( 'NONE', *, *, #9331, .F. ) ;
#11614=CARTESIAN_POINT ( 'NONE',  ( -0.4125000000000000333, -0.6290000000000005587, 0.4124999999999999223 ) ) ;
#11622=CARTESIAN_POINT ( 'NONE',  ( 0.6552635435737790282, -0.4101955659814244814, -0.5075266421723672039 ) ) ;
#11624=LINE ( 'NONE', #1208, #15142 ) ;
#11638=ORIENTED_EDGE ( 'NONE', *, *, #4195, .T. ) ;
#11639=ORIENTED_EDGE ( 'NONE', *, *, #13429, .T. ) ;
#11642=CARTESIAN_POINT ( 'NONE',  ( 0.7017867892446607581, 0.04143956043956044388, -0.4010711782184314678 ) ) ;
#11649=CARTESIAN_POINT ( 'NONE',  ( 0.6592465977460899573, -0.4437463589180128953, 0.4884267951992171675 ) ) ;
#11655=EDGE_CURVE ( 'NONE', #6823, #4756, #4232, .T. ) ;
#11658=ORIENTED_EDGE ( 'NONE', *, *, #7147, .F. ) ;
#11661=AXIS2_PLACEMENT_3D ( 'NONE', #5178, #7338, #14427 ) ;
#11662=CARTESIAN_POINT ( 'NONE',  ( 1.131687341751868248, -0.4429445645322986902, -0.4840157155117131293 ) ) ;
#11666=CARTESIAN_POINT ( 'NONE',  ( 7.144847001653046861E-17, -0.6334543218446814228, 0.000000000000000000 ) ) ;
#11669=EDGE_CURVE ( 'NONE', #3133, #251, #10829, .T. ) ;
#11671=VERTEX_POINT ( 'NONE', #2572 ) ;
#11676=CARTESIAN_POINT ( 'NONE',  ( 0.8336852985356731915, -0.4829999999999998739, -0.4100337033397443709 ) ) ;
#11683=CARTESIAN_POINT ( 'NONE',  ( 0.7513246802501661881, 2.561107494060246767E-17, -0.4293820849162032216 ) ) ;
#11687=CARTESIAN_POINT ( 'NONE',  ( 1.522243911113194681, -0.3829999999999998961, -0.4784993797865369491 ) ) ;
#11688=DIRECTION ( 'NONE',  ( 0.01412288512831213171, -3.675428035873183031E-19, -0.9999002670844990837 ) ) ;
#11698=LINE ( 'NONE', #8108, #4859 ) ;
#11701=ORIENTED_EDGE ( 'NONE', *, *, #3887, .T. ) ;
#11704=CARTESIAN_POINT ( 'NONE',  ( 0.6566154142300546503, -0.4311287871771214975, -0.4974659767684403433 ) ) ;
#11716=CIRCLE ( 'NONE', #682, 0.6700292969071727223 ) ;
#11725=CIRCLE ( 'NONE', #7090, 0.07500000000000002498 ) ;
#11727=DIRECTION ( 'NONE',  ( 0.000000000000000000, 0.000000000000000000, -1.000000000000000000 ) ) ;
#11729=CARTESIAN_POINT ( 'NONE',  ( 3.015109087180224771E-17, -0.4844395604395604904, 0.000000000000000000 ) ) ;
#11730=CARTESIAN_POINT ( 'NONE',  ( 1.250000000000000000, -0.05999999999999986594, -0.4223386481965726857 ) ) ;
#11731=DIRECTION ( 'NONE',  ( -1.000000000000000000, 0.000000000000000000, 0.000000000000000000 ) ) ;
#11732=VECTOR ( 'NONE', #1761, 39.37007874015748143 ) ;
#11735=CARTESIAN_POINT ( 'NONE',  ( 0.7040204553987591263, -0.3870671487057328886, 0.4900562082570797950 ) ) ;
#11743=CARTESIAN_POINT ( 'NONE',  ( -5.764454660286586870E-18, 0.1956296296296295978, 0.000000000000000000 ) ) ;
#11745=CARTESIAN_POINT ( 'NONE',  ( 1.644431316733000026, -0.3408522091760272099, -0.4170406485181324396 ) ) ;
#11749=ORIENTED_EDGE ( 'NONE', *, *, #9849, .F. ) ;
#11753=CARTESIAN_POINT ( 'NONE',  ( 0.7372049720039718368, -0.0009098304392685509310, -0.4419334053338275226 ) ) ;
#11754=VERTEX_POINT ( 'NONE', #5875 ) ;
#11757=CARTESIAN_POINT ( 'NONE',  ( 1.558097216777236227, -0.02209972869556197164, 0.4779929771641632796 ) ) ;
#11763=FACE_OUTER_BOUND ( 'NONE', #14174, .T. ) ;
#11770=EDGE_CURVE ( 'NONE', #4626, #7795, #14580, .T. ) ;
#11778=DIRECTION ( 'NONE',  ( 0.000000000000000000, -0.000000000000000000, -1.000000000000000000 ) ) ;
#11782=CARTESIAN_POINT ( 'NONE',  ( 8.792093969802149189, 0.8799778768672790186, 6.829619984160658046E-17 ) ) ;
#11784=PLANE ( 'NONE',  #197 ) ;
#11793=CARTESIAN_POINT ( 'NONE',  ( 0.3724999999999997757, -0.6590000000000000302, -0.3725000000000000533 ) ) ;
#11796=CARTESIAN_POINT ( 'NONE',  ( 0.7017867892446607581, -0.4844395604395603239, -0.4010711782184315233 ) ) ;
#11800=DIRECTION ( 'NONE',  ( -0.9992912762382414327, -0.03489602031262312859, 0.01411428356268702201 ) ) ;
#11814=CIRCLE ( 'NONE', #13792, 0.03999999999999998002 ) ;
#11823=PRODUCT_DEFINITION_CONTEXT ( 'detailed design', #9200, 'design' ) ;
#11828=EDGE_LOOP ( 'NONE', ( #711, #2089, #6276, #3865 ) ) ;
#11834=CARTESIAN_POINT ( 'NONE',  ( 1.632672928280230362, 0.0005225660665716322373, -0.4769396479056465243 ) ) ;
#11835=EDGE_LOOP ( 'NONE', ( #2504, #6253, #3010, #3374 ) ) ;
#11839=VERTEX_POINT ( 'NONE', #13479 ) ;
#11848=DIRECTION ( 'NONE',  ( -2.602462600580851747E-17, -1.000000000000000000, 0.000000000000000000 ) ) ;
#11856=CARTESIAN_POINT ( 'NONE',  ( 0.7017867892446606470, 0.04143956043956045082, 0.4010711782184315233 ) ) ;
#11860=CARTESIAN_POINT ( 'NONE',  ( 0.6610344722576404486, -0.4494579783924679273, 0.4833528575413044148 ) ) ;
#11863=ORIENTED_EDGE ( 'NONE', *, *, #236, .F. ) ;
#11867=CARTESIAN_POINT ( 'NONE',  ( 2.824624536279283671, 0.5882431044538737330, 0.4601041732163942410 ) ) ;
#11877=CARTESIAN_POINT ( 'NONE',  ( 0.6734872051250879732, -0.4131034743634533490, 0.4827143163826072003 ) ) ;
#11883=EDGE_CURVE ( 'NONE', #8572, #11419, #11472, .T. ) ;
#11887=ORIENTED_EDGE ( 'NONE', *, *, #1822, .F. ) ;
#11896=ORIENTED_EDGE ( 'NONE', *, *, #11187, .T. ) ;
#11897=DIRECTION ( 'NONE',  ( 0.000000000000000000, 0.000000000000000000, 1.000000000000000000 ) ) ;
#11901=CARTESIAN_POINT ( 'NONE',  ( 0.8999999999999999112, -0.6429999999999999050, -0.3750000000000000555 ) ) ;
#11908=ADVANCED_FACE ( 'NONE', ( #851 ), #12560, .T. ) ;
#11916=AXIS2_PLACEMENT_3D ( 'NONE', #1613, #10968, #7823 ) ;
#11918=CARTESIAN_POINT ( 'NONE',  ( 0.8249999999999999556, -0.6429999999999999050, -0.3750000000000000555 ) ) ;
#11926=CARTESIAN_POINT ( 'NONE',  ( 0.3724999999999999423, -0.6589999999999996971, 0.3724999999999999423 ) ) ;
#11940=ORIENTED_EDGE ( 'NONE', *, *, #14843, .T. ) ;
#11946=EDGE_CURVE ( 'NONE', #9348, #12293, #11725, .T. ) ;
#11954=DIRECTION ( 'NONE',  ( -0.000000000000000000, -0.000000000000000000, 1.000000000000000000 ) ) ;
#11960=EDGE_CURVE ( 'NONE', #14534, #3646, #3912, .T. ) ;
#11964=CARTESIAN_POINT ( 'NONE',  ( 2.002301348309084350, -0.1786631980423395716, -0.4121376268991520098 ) ) ;
#11968=CARTESIAN_POINT ( 'NONE',  ( 2.592367411162173063, 0.4049457270506677808, -0.4633846410852800468 ) ) ;
#11977=B_SPLINE_CURVE_WITH_KNOTS ( 'NONE', 3,
 ( #14221, #8500, #9647, #6132, #1443, #11860, #10712, #7493, #8573, #3908, #4910, #12995, #13212, #2607 ),
 .UNSPECIFIED., .F., .F.,
 ( 4, 2, 2, 2, 2, 2, 4 ),
 ( 0.000000000000000000, 0.001176052134299115362, 0.002352104268598230723, 0.002940130335747791115, 0.003528156402897351940, 0.004116182470046913199, 0.004704208537196473590 ),
 .UNSPECIFIED. ) ;
#11981=EDGE_CURVE ( 'NONE', #5075, #11671, #8268, .T. ) ;
#11992=CARTESIAN_POINT ( 'NONE',  ( 2.279764930208930007, 0.5637746725391985514, 0.4072339235668807067 ) ) ;
#12002=CARTESIAN_POINT ( 'NONE',  ( 0.8671983899133194340, -0.4446438992933860468, -0.4431244221569915487 ) ) ;
#12007=DIRECTION ( 'NONE',  ( 0.000000000000000000, -0.7071067811865350272, -0.7071067811865600072 ) ) ;
#12011=CARTESIAN_POINT ( 'NONE',  ( 0.7017867892446606470, 0.04143956043956045082, 0.4010711782184315233 ) ) ;
#12012=CARTESIAN_POINT ( 'NONE',  ( 3.388933043275772494, 0.7513023213622327390, 0.4521337140780258279 ) ) ;
#12017=CARTESIAN_POINT ( 'NONE',  ( 0.6866570596051649877, 0.03904768965436217903, 0.4282026755330212708 ) ) ;
#12021=AXIS2_PLACEMENT_3D ( 'NONE', #4268, #12581, #792 ) ;
#12029=ADVANCED_FACE ( 'NONE', ( #162 ), #8327, .T. ) ;
#12038=ADVANCED_FACE ( 'NONE', ( #5929 ), #991, .T. ) ;
#12049=CARTESIAN_POINT ( 'NONE',  ( 2.033926451083719833, 0.2322360065625572456, 0.4712722252671790457 ) ) ;
#12051=AXIS2_PLACEMENT_3D ( 'NONE', #11150, #9167, #12446 ) ;
#12063=CARTESIAN_POINT ( 'NONE',  ( 3.083590687937821428, 0.9932358216845013077, 0.4564464592100380136 ) ) ;
#12064=VERTEX_POINT ( 'NONE', #1391 ) ;
#12079=ORIENTED_EDGE ( 'NONE', *, *, #1081, .F. ) ;
#12085=AXIS2_PLACEMENT_3D ( 'NONE', #14936, #1993, #4392 ) ;
#12087=CARTESIAN_POINT ( 'NONE',  ( 0.7070095302584743502, -0.01882438353555513505, 0.4738366780029916736 ) ) ;
#12088=B_SPLINE_CURVE_WITH_KNOTS ( 'NONE', 3,
 ( #8093, #7853, #9080, #9009, #14889, #11447, #6704, #14731, #3259, #10300, #14809, #3191, #5713, #13723 ),
 .UNSPECIFIED., .F., .F.,
 ( 4, 2, 2, 2, 2, 2, 4 ),
 ( 1.734723475976807094E-18, 0.0004702396892684933098, 0.0007053595339027388805, 0.0009404793785369844512, 0.001175599223171230022, 0.001410719067805475593, 0.001880958757073978010 ),
 .UNSPECIFIED. ) ;
#12090=ORIENTED_EDGE ( 'NONE', *, *, #1822, .T. ) ;
#12093=LINE ( 'NONE', #7510, #2909 ) ;
#12098=ORIENTED_EDGE ( 'NONE', *, *, #11655, .T. ) ;
#12099=CIRCLE ( 'NONE', #2817, 0.03999999999999998002 ) ;
#12100=CARTESIAN_POINT ( 'NONE',  ( 1.831696981322114670, 0.1157067236523830062, 0.4136843993219122551 ) ) ;
#12104=CARTESIAN_POINT ( 'NONE',  ( 1.262572881824611803, -0.4300086559495954752, 0.4821670496917128679 ) ) ;
#12115=CONICAL_SURFACE ( 'NONE', #10172, 0.06999999999999829969, 0.7853981633974298493 ) ;
#12117=DIRECTION ( 'NONE',  ( 0.000000000000000000, 0.7071067811865612285, -0.7071067811865336949 ) ) ;
#12118=AXIS2_PLACEMENT_3D ( 'NONE', #7092, #13943, #9305 ) ;
#12127=EDGE_CURVE ( 'NONE', #10000, #3132, #7663, .T. ) ;
#12134=CARTESIAN_POINT ( 'NONE',  ( 0.007908111413600218964, -0.2214999999999999469, 0.5598942880828960966 ) ) ;
#12138=TOROIDAL_SURFACE ( 'NONE', #10195, 0.7173254825712083171, 0.05999999999999999778 ) ;
#12143=CARTESIAN_POINT ( 'NONE',  ( -0.4125000000000000333, -0.6290000000000005587, 0.3724999999999999423 ) ) ;
#12144=EDGE_CURVE ( 'NONE', #4756, #3922, #5010, .T. ) ;
#12145=CARTESIAN_POINT ( 'NONE',  ( 2.449076186954514686E-17, -0.4430000000000000049, 0.000000000000000000 ) ) ;
#12158=FACE_OUTER_BOUND ( 'NONE', #777, .T. ) ;
#12160=ORIENTED_EDGE ( 'NONE', *, *, #601, .F. ) ;
#12161=LINE ( 'NONE', #11015, #3075 ) ;
#12164=CARTESIAN_POINT ( 'NONE',  ( 0.6922886459387326274, 0.0009147467600669257660, 0.4416098182902893909 ) ) ;
#12165=CARTESIAN_POINT ( 'NONE',  ( 0.007386697474241961034, -0.2214999999999999469, 0.5229781811763314359 ) ) ;
#12166=AXIS2_PLACEMENT_3D ( 'NONE', #357, #656, #3913 ) ;
#12179=ORIENTED_EDGE ( 'NONE', *, *, #1262, .F. ) ;
#12185=CARTESIAN_POINT ( 'NONE',  ( 0.8329939018324243882, -0.4323038960628863281, -0.3410777879097737775 ) ) ;
#12188=CONICAL_SURFACE ( 'NONE', #1180, 0.05500000000000146438, 0.7853981633974547183 ) ;
#12195=ORIENTED_EDGE ( 'NONE', *, *, #7638, .T. ) ;
#12210=CARTESIAN_POINT ( 'NONE',  ( 3.471303878679313115, 1.057055486693972757, 0.4509702841988744715 ) ) ;
#12211=VERTEX_POINT ( 'NONE', #9744 ) ;
#12218=EDGE_CURVE ( 'NONE', #14149, #7690, #4143, .T. ) ;
#12225=ORIENTED_EDGE ( 'NONE', *, *, #4180, .T. ) ;
#12228=ORIENTED_EDGE ( 'NONE', *, *, #10072, .F. ) ;
#12229=ORIENTED_EDGE ( 'NONE', *, *, #14265, .T. ) ;
#12246=ORIENTED_EDGE ( 'NONE', *, *, #627, .F. ) ;
#12247=ADVANCED_FACE ( 'NONE', ( #1612 ), #13174, .F. ) ;
#12248=CARTESIAN_POINT ( 'NONE',  ( 0.7441558489118152986, 4.164134020615923019E-16, 0.4356293359425711387 ) ) ;
#12252=CARTESIAN_POINT ( 'NONE',  ( 0.7815405595936760763, -0.4436696693102589184, -0.3492667155310359983 ) ) ;
#12256=CARTESIAN_POINT ( 'NONE',  ( 1.397260334976608398, 0.007251848866960407085, -0.4201477693899776100 ) ) ;
#12260=EDGE_LOOP ( 'NONE', ( #6495, #6162, #12930, #8288 ) ) ;
#12263=CARTESIAN_POINT ( 'NONE',  ( 8.849999999999999645, 0.9399413264884247665, 6.829619984160658046E-17 ) ) ;
#12266=CARTESIAN_POINT ( 'NONE',  ( 0.6735393331370975734, -0.4714463074374599660, -0.4543474816912257408 ) ) ;
#12272=SPHERICAL_SURFACE ( 'NONE', #3711, 0.8499999999999999778 ) ;
#12276=ORIENTED_EDGE ( 'NONE', *, *, #1965, .F. ) ;
#12287=CARTESIAN_POINT ( 'NONE',  ( 8.840371647876674288, 0.8816637705348994158, 0.09817148304380068913 ) ) ;
#12288=CARTESIAN_POINT ( 'NONE',  ( 0.9542757771954346602, -0.4472635993787555386, -0.4276257322837787034 ) ) ;
#12293=VERTEX_POINT ( 'NONE', #7046 ) ;
#12300=CARTESIAN_POINT ( 'NONE',  ( 0.6558056096843538629, -0.01866721106089168705, 0.5013356986195881548 ) ) ;
#12315=EDGE_CURVE ( 'NONE', #1080, #9538, #11624, .T. ) ;
#12319=CARTESIAN_POINT ( 'NONE',  ( 2.045067168503163391, 0.3290769108334317683, -0.4105096428946750642 ) ) ;
#12321=AXIS2_PLACEMENT_3D ( 'NONE', #359, #8579, #4209 ) ;
#12322=CARTESIAN_POINT ( 'NONE',  ( 3.613973162031111741, 0.9969999999999999973, -0.3889491967554554730 ) ) ;
#12325=EDGE_CURVE ( 'NONE', #10522, #436, #7744, .T. ) ;
#12327=CARTESIAN_POINT ( 'NONE',  ( 0.8287146145289983057, -0.4323349699879636132, -0.3513609214607458231 ) ) ;
#12328=CARTESIAN_POINT ( 'NONE',  ( 1.002134052359566097, -0.4429990928571921338, -0.4270146172744395674 ) ) ;
#12330=ORIENTED_EDGE ( 'NONE', *, *, #14939, .T. ) ;
#12331=CIRCLE ( 'NONE', #12897, 0.03999999999999998002 ) ;
#12333=CARTESIAN_POINT ( 'NONE',  ( 0.8374673721983860730, -0.4832242842617602840, -0.3334348852663109875 ) ) ;
#12338=CARTESIAN_POINT ( 'NONE',  ( 0.7017867892446606470, -0.4844395604395603239, 0.4010711782184315233 ) ) ;
#12344=AXIS2_PLACEMENT_3D ( 'NONE', #12457, #8112, #13821 ) ;
#12345=CIRCLE ( 'NONE', #5763, 0.03999999999999997308 ) ;
#12347=ADVANCED_FACE ( 'NONE', ( #10553 ), #4591, .T. ) ;
#12350=ORIENTED_EDGE ( 'NONE', *, *, #11401, .F. ) ;
#12352=ORIENTED_EDGE ( 'NONE', *, *, #3269, .F. ) ;
#12353=VECTOR ( 'NONE', #13250, 39.37007874015748143 ) ;
#12356=CARTESIAN_POINT ( 'NONE',  ( -5.764454660286586870E-18, -0.2214999999999999469, 0.000000000000000000 ) ) ;
#12359=ORIENTED_EDGE ( 'NONE', *, *, #13842, .T. ) ;
#12367=CARTESIAN_POINT ( 'NONE',  ( 8.792093969803303821, 0.8799778768673193197, 0.04156183585338274478 ) ) ;
#12368=CARTESIAN_POINT ( 'NONE',  ( 0.9577688866514744159, -0.4806004831388784870, -0.4232852336075703104 ) ) ;
#12373=B_SPLINE_CURVE_WITH_KNOTS ( 'NONE', 3,
 ( #693, #14712, #1931, #6112, #6178, #6613, #10836, #11340, #14940, #6683, #3173, #842, #11502, #4623 ),
 .UNSPECIFIED., .F., .F.,
 ( 4, 2, 2, 2, 2, 2, 4 ),
 ( 0.000000000000000000, 0.0003612929182778039307, 0.0007225858365556078614, 0.001083878754833411846, 0.001445171673111215723, 0.002167757509666824126, 0.002890343346222432747 ),
 .UNSPECIFIED. ) ;
#12375=DIRECTION ( 'NONE',  ( -0.7070715176384831935, -0.7070715176384805289, -0.009986885842351453380 ) ) ;
#12376=ORIENTED_EDGE ( 'NONE', *, *, #958, .F. ) ;
#12382=DIRECTION ( 'NONE',  ( 0.000000000000000000, 0.000000000000000000, -1.000000000000000000 ) ) ;
#12394=DIRECTION ( 'NONE',  ( 0.000000000000000000, 0.000000000000000000, -1.000000000000000000 ) ) ;
#12417=ORIENTED_EDGE ( 'NONE', *, *, #6560, .T. ) ;
#12421=CARTESIAN_POINT ( 'NONE',  ( 0.6729666568098592316, -0.4031619489883325191, -0.4872504569466303836 ) ) ;
#12422=AXIS2_PLACEMENT_3D ( 'NONE', #10152, #950, #12501 ) ;
#12427=ORIENTED_EDGE ( 'NONE', *, *, #9575, .T. ) ;
#12428=AXIS2_PLACEMENT_3D ( 'NONE', #8808, #2986, #11395 ) ;
#12431=ORIENTED_EDGE ( 'NONE', *, *, #11981, .F. ) ;
#12435=CARTESIAN_POINT ( 'NONE',  ( -0.3725000000000002198, 0.2159999999999999420, -0.3725000000000000533 ) ) ;
#12436=DIRECTION ( 'NONE',  ( -1.000000000000000000, 0.000000000000000000, 0.000000000000000000 ) ) ;
#12440=EDGE_LOOP ( 'NONE', ( #12417, #1728, #13263, #2317 ) ) ;
#12441=CARTESIAN_POINT ( 'NONE',  ( 3.390179639970223313, 0.6913388717410868800, 0.3921396980529558429 ) ) ;
#12446=DIRECTION ( 'NONE',  ( 0.000000000000000000, 0.000000000000000000, -1.000000000000000000 ) ) ;
#12453=CARTESIAN_POINT ( 'NONE',  ( 0.7406097974541305806, 0.1956296296296295978, 0.000000000000000000 ) ) ;
#12455=CARTESIAN_POINT ( 'NONE',  ( 0.8999999999999999112, -0.4829999999999998739, -0.3750000000000000555 ) ) ;
#12457=CARTESIAN_POINT ( 'NONE',  ( 0.8999999999999999112, -0.4429999999999998939, -0.3750000000000000555 ) ) ;
#12460=CARTESIAN_POINT ( 'NONE',  ( 2.977166378293599980, 0.8979166429007079397, -0.4579496274252315979 ) ) ;
#12461=CARTESIAN_POINT ( 'NONE',  ( 1.010163005730224883, -0.4429751326668778244, -0.4086419528574875004 ) ) ;
#12470=EDGE_CURVE ( 'NONE', #14804, #7417, #8276, .T. ) ;
#12471=CARTESIAN_POINT ( 'NONE',  ( 0.7349234941866550352, -0.4417196455735734606, -0.4440226803674550138 ) ) ;
#12478=LINE ( 'NONE', #9296, #10588 ) ;
#12489=DIRECTION ( 'NONE',  ( -1.000000000000000000, 0.000000000000000000, 0.000000000000000000 ) ) ;
#12492=EDGE_LOOP ( 'NONE', ( #763, #13890, #2300, #5540 ) ) ;
#12497=B_SPLINE_CURVE_WITH_KNOTS ( 'NONE', 3,
 ( #13456, #12537, #2924, #1830, #6516, #6667, #11325, #3072, #4223, #11172, #7737, #11402, #823, #10113 ),
 .UNSPECIFIED., .F., .F.,
 ( 4, 2, 2, 2, 2, 2, 4 ),
 ( 0.000000000000000000, 0.0007185039784459185813, 0.001437007956891837163, 0.001796259946114796020, 0.002155511935337754877, 0.002514763924560713734, 0.002874015913783673024 ),
 .UNSPECIFIED. ) ;
#12499=LINE ( 'NONE', #2018, #9223 ) ;
#12501=DIRECTION ( 'NONE',  ( -0.7071067811865441310, 0.7071067811865509034, 0.000000000000000000 ) ) ;
#12510=CARTESIAN_POINT ( 'NONE',  ( 0.9618999659839394534, -0.4466846464728802535, -0.4182560267626411754 ) ) ;
#12514=EDGE_LOOP ( 'NONE', ( #13001, #14445, #13836, #9373 ) ) ;
#12518=( BOUNDED_CURVE ( )  B_SPLINE_CURVE ( 3, ( #7881, #6436, #1902, #6592 ),
 .UNSPECIFIED., .F., .F. ) 
 B_SPLINE_CURVE_WITH_KNOTS ( ( 4, 4 ),
 ( 3.926990816987247168, 4.677482395344810584 ),
 .UNSPECIFIED. ) 
 CURVE ( )  GEOMETRIC_REPRESENTATION_ITEM ( )  RATIONAL_B_SPLINE_CURVE ( ( 1.000000000000000000, 0.9536117119880161974, 0.9536117119880161974, 1.000000000000000000 ) ) 
 REPRESENTATION_ITEM ( '' )  );
#12520=DIRECTION ( 'NONE',  ( -0.01412288512831213171, 3.675428035873182550E-19, 0.9999002670844991947 ) ) ;
#12526=CARTESIAN_POINT ( 'NONE',  ( 2.187203820042824542, 0.4712135623730921985, 0.5000000000000000000 ) ) ;
#12527=FACE_OUTER_BOUND ( 'NONE', #13364, .T. ) ;
#12532=CYLINDRICAL_SURFACE ( 'NONE', #13865, 0.3803340137431718282 ) ;
#12537=CARTESIAN_POINT ( 'NONE',  ( 0.7441595030246626052, -0.4430000000000003935, 0.4356261515797149042 ) ) ;
#12539=ORIENTED_EDGE ( 'NONE', *, *, #14843, .F. ) ;
#12543=CARTESIAN_POINT ( 'NONE',  ( 1.625945750338193108, -0.2839166429008007642, 0.4770346645432458343 ) ) ;
#12544=CARTESIAN_POINT ( 'NONE',  ( 0.7241094260644779235, -0.4377363598224605634, -0.4546250289486069018 ) ) ;
#12547=ORIENTED_EDGE ( 'NONE', *, *, #12325, .F. ) ;
#12559=CARTESIAN_POINT ( 'NONE',  ( 0.7117500205947747682, -0.4296287437428823464, -0.4679153652930406193 ) ) ;
#12560=CYLINDRICAL_SURFACE ( 'NONE', #3168, 0.07500000000000002498 ) ;
#12566=VERTEX_POINT ( 'NONE', #790 ) ;
#12571=FACE_OUTER_BOUND ( 'NONE', #7637, .T. ) ;
#12577=VERTEX_POINT ( 'NONE', #4192 ) ;
#12578=B_SPLINE_CURVE_WITH_KNOTS ( 'NONE', 3,
 ( #26, #7107, #11753, #14031, #15114, #1406, #10682, #2424, #97, #3417, #3490, #6019, #4718, #1254 ),
 .UNSPECIFIED., .F., .F.,
 ( 4, 2, 2, 2, 2, 2, 4 ),
 ( 0.000000000000000000, 0.0007185039784458951626, 0.001437007956891790325, 0.001796259946114739424, 0.002155511935337688957, 0.002514763924560637839, 0.002874015913783587155 ),
 .UNSPECIFIED. ) ;
#12580=CARTESIAN_POINT ( 'NONE',  ( 0.7010945348274493227, 0.003367250660063846480, -0.4266201320538819397 ) ) ;
#12581=DIRECTION ( 'NONE',  ( -0.9999002670844991947, 0.000000000000000000, -0.01412288512831585095 ) ) ;
#12583=CONICAL_SURFACE ( 'NONE', #6014, 0.6412116890856960350, 1.326062729686469988 ) ;
#12594=EDGE_LOOP ( 'NONE', ( #15085, #11940, #9254, #453 ) ) ;
#12595=EDGE_LOOP ( 'NONE', ( #8106, #1238, #9157, #5176 ) ) ;
#12599=DIRECTION ( 'NONE',  ( -1.000000000000000000, 0.000000000000000000, 0.000000000000000000 ) ) ;
#12605=CARTESIAN_POINT ( 'NONE',  ( 2.279764930209268847, 0.5637746725395378355, -0.4072339235673128610 ) ) ;
#12609=DIRECTION ( 'NONE',  ( 0.8682164115033652596, 0.000000000000000000, -0.4961857140186719528 ) ) ;
#12610=( BOUNDED_CURVE ( )  B_SPLINE_CURVE ( 3, ( #9106, #7958, #2213, #4593 ),
 .UNSPECIFIED., .F., .F. ) 
 B_SPLINE_CURVE_WITH_KNOTS ( ( 4, 4 ),
 ( 3.926990816987239619, 4.712388980384689674 ),
 .UNSPECIFIED. ) 
 CURVE ( )  GEOMETRIC_REPRESENTATION_ITEM ( )  RATIONAL_B_SPLINE_CURVE ( ( 1.000000000000000000, 0.9492530216741910110, 0.9492530216741910110, 1.000000000000000000 ) ) 
 REPRESENTATION_ITEM ( '' )  );
#12613=EDGE_CURVE ( 'NONE', #14557, #11117, #2131, .T. ) ;
#12623=EDGE_CURVE ( 'NONE', #9538, #3778, #690, .T. ) ;
#12629=VECTOR ( 'NONE', #14281, 39.37007874015748854 ) ;
#12630=ORIENTED_EDGE ( 'NONE', *, *, #12757, .T. ) ;
#12634=DIRECTION ( 'NONE',  ( -0.03489949670249406499, 0.9993908270190959842, 0.000000000000000000 ) ) ;
#12636=CIRCLE ( 'NONE', #5608, 0.06000000000000002554 ) ;
#12637=CARTESIAN_POINT ( 'NONE',  ( 1.863568193433660758, 0.06187774891384333065, 0.4736784153469821290 ) ) ;
#12645=VECTOR ( 'NONE', #3862, 39.37007874015748143 ) ;
#12646=CARTESIAN_POINT ( 'NONE',  ( 8.707077114626732950, 0.8770090228648390607, 0.3011897810131113906 ) ) ;
#12647=CIRCLE ( 'NONE', #12911, 0.1150000000000000050 ) ;
#12653=DIRECTION ( 'NONE',  ( 0.7070715176384831935, 0.7070715176384805289, -0.009986885842351451645 ) ) ;
#12660=DIRECTION ( 'NONE',  ( -0.4961857140186717308, -0.000000000000000000, 0.8682164115033652596 ) ) ;
#12664=CARTESIAN_POINT ( 'NONE',  ( 0.7204397385173409996, -0.006614428813630259842, -0.4582225808237102571 ) ) ;
#12667=CIRCLE ( 'NONE', #6092, 0.7406097974541305806 ) ;
#12668=( GEOMETRIC_REPRESENTATION_CONTEXT ( 3 ) GLOBAL_UNCERTAINTY_ASSIGNED_CONTEXT ( ( #12728 ) ) GLOBAL_UNIT_ASSIGNED_CONTEXT ( ( #8731, #13162, #4151 ) ) REPRESENTATION_CONTEXT ( 'NONE', 'WORKASPACE' ) );
#12679=EDGE_CURVE ( 'NONE', #9898, #3117, #10698, .T. ) ;
#12680=DIRECTION ( 'NONE',  ( -0.9999002670844991947, 0.000000000000000000, -0.01412288512831213171 ) ) ;
#12682=CARTESIAN_POINT ( 'NONE',  ( -0.3725000000000000533, -0.6590000000000000302, 0.3724999999999999423 ) ) ;
#12689=DIRECTION ( 'NONE',  ( 0.9999002670844989726, 0.000000000000000000, -0.01412288512831212997 ) ) ;
#12704=DIRECTION ( 'NONE',  ( 1.000000000000000000, 0.000000000000000000, 0.000000000000000000 ) ) ;
#12705=CARTESIAN_POINT ( 'NONE',  ( 2.854443715606263865, 0.5365358177141184015, -0.4001101571913185384 ) ) ;
#12710=CARTESIAN_POINT ( 'NONE',  ( 0.7134904538003045138, -0.4430000000000007265, 0.4077598229816897235 ) ) ;
#12713=EDGE_CURVE ( 'NONE', #3646, #5710, #14144, .T. ) ;
#12715=CARTESIAN_POINT ( 'NONE',  ( 8.849999999999999645, 0.9969999999999998863, 6.829619984160658046E-17 ) ) ;
#12718=EDGE_LOOP ( 'NONE', ( #7210, #12195, #6176, #9037 ) ) ;
#12720=DIRECTION ( 'NONE',  ( 0.000000000000000000, 0.000000000000000000, -1.000000000000000000 ) ) ;
#12725=EDGE_CURVE ( 'NONE', #8139, #11449, #1677, .T. ) ;
#12728=UNCERTAINTY_MEASURE_WITH_UNIT (LENGTH_MEASURE( 1.000000000000000082E-05 ), #8731, 'distance_accuracy_value', 'NONE');
#12729=CARTESIAN_POINT ( 'NONE',  ( 1.010189475225347078, -0.4429749903950104262, -0.4085521775708274572 ) ) ;
#12732=CARTESIAN_POINT ( 'NONE',  ( 2.807059454666800402, 0.6196377705552925663, -0.4603522675894519689 ) ) ;
#12733=CARTESIAN_POINT ( 'NONE',  ( 0.9022048395661492748, -0.4607945367651646862, -0.4500484056301596314 ) ) ;
#12735=CARTESIAN_POINT ( 'NONE',  ( -0.3725000000000002198, -0.6590000000000000302, -0.3725000000000000533 ) ) ;
#12738=CARTESIAN_POINT ( 'NONE',  ( 0.7040204553985035529, -0.05593285129442519821, -0.4900562082570833478 ) ) ;
#12740=ADVANCED_FACE ( 'NONE', ( #11370 ), #5703, .F. ) ;
#12743=ORIENTED_EDGE ( 'NONE', *, *, #3634, .F. ) ;
#12747=ORIENTED_EDGE ( 'NONE', *, *, #14233, .T. ) ;
#12753=CARTESIAN_POINT ( 'NONE',  ( 0.6601485485260571995, -0.3723516483516483011, -0.5137583810202324131 ) ) ;
#12756=AXIS2_PLACEMENT_3D ( 'NONE', #2819, #7414, #5051 ) ;
#12757=EDGE_CURVE ( 'NONE', #4756, #9216, #12636, .T. ) ;
#12761=EDGE_CURVE ( 'NONE', #1733, #5075, #6721, .T. ) ;
#12775=ADVANCED_FACE ( 'NONE', ( #10231 ), #7275, .T. ) ;
#12776=DIRECTION ( 'NONE',  ( 1.000000000000000000, 1.874307916738609066E-16, 0.000000000000000000 ) ) ;
#12780=ADVANCED_FACE ( 'NONE', ( #1559 ), #1258, .F. ) ;
#12781=CARTESIAN_POINT ( 'NONE',  ( 0.6570965961311159287, -0.3875664237315883387, 0.5130374278108668085 ) ) ;
#12787=CARTESIAN_POINT ( 'NONE',  ( 0.7513246802501661881, -0.4429999999999998939, -0.4293820849162031661 ) ) ;
#12790=AXIS2_PLACEMENT_3D ( 'NONE', #1050, #7876, #10556 ) ;
#12801=ORIENTED_EDGE ( 'NONE', *, *, #5487, .F. ) ;
#12803=CARTESIAN_POINT ( 'NONE',  ( 1.014924625165573246, -0.4429443310102024189, -0.3808900809060754011 ) ) ;
#12805=LINE ( 'NONE', #9388, #7752 ) ;
#12826=VERTEX_POINT ( 'NONE', #14260 ) ;
#12840=CARTESIAN_POINT ( 'NONE',  ( 0.8999999999999999112, -0.6429999999999999050, -0.3199999999999985634 ) ) ;
#12841=CARTESIAN_POINT ( 'NONE',  ( 0.8999999999999999112, -0.6429999999999999050, -0.3750000000000000555 ) ) ;
#12845=PLANE ( 'NONE',  #13083 ) ;
#12849=AXIS2_PLACEMENT_3D ( 'NONE', #5465, #1934, #14716 ) ;
#12857=PLANE ( 'NONE',  #2167 ) ;
#12859=CARTESIAN_POINT ( 'NONE',  ( 0.6757966763796152687, -0.3817220302227288253, 0.4909001136279363409 ) ) ;
#12867=CARTESIAN_POINT ( 'NONE',  ( 0.3724999999999997757, -0.6589999999999996971, -0.3725000000000000533 ) ) ;
#12871=EDGE_CURVE ( 'NONE', #10938, #4169, #4140, .T. ) ;
#12874=DIRECTION ( 'NONE',  ( -2.602462600580851747E-17, -1.000000000000000000, 0.000000000000000000 ) ) ;
#12879=AXIS2_PLACEMENT_3D ( 'NONE', #2739, #7480, #10926 ) ;
#12884=FACE_OUTER_BOUND ( 'NONE', #5287, .T. ) ;
#12887=DIRECTION ( 'NONE',  ( -0.9999002670844991947, 0.000000000000000000, 0.01412288512831128169 ) ) ;
#12891=CARTESIAN_POINT ( 'NONE',  ( 1.973685276483480910, 0.1827974636779289841, 0.4721230893152050245 ) ) ;
#12892=CARTESIAN_POINT ( 'NONE',  ( 2.837768005214870382, 0.5663408804686759224, -0.4003582515643820949 ) ) ;
#12896=CARTESIAN_POINT ( 'NONE',  ( 0.4124999999999999223, 0.2159999999999999698, 0.3724999999999999423 ) ) ;
#12897=AXIS2_PLACEMENT_3D ( 'NONE', #6406, #2957, #10008 ) ;
#12906=ORIENTED_EDGE ( 'NONE', *, *, #9833, .T. ) ;
#12911=AXIS2_PLACEMENT_3D ( 'NONE', #10573, #9289, #4533 ) ;
#12914=AXIS2_PLACEMENT_3D ( 'NONE', #13830, #1056, #13910 ) ;
#12922=CARTESIAN_POINT ( 'NONE',  ( 2.230477600021715912, 0.4287871555018993308, -0.4684960790957384824 ) ) ;
#12930=ORIENTED_EDGE ( 'NONE', *, *, #11597, .F. ) ;
#12935=CARTESIAN_POINT ( 'NONE',  ( 3.390179639970223313, 0.6913388717410869910, 0.3921396980529558429 ) ) ;
#12942=CARTESIAN_POINT ( 'NONE',  ( 0.7429169091362286537, -0.4430000000000002824, 0.4367090053324595988 ) ) ;
#12953=CARTESIAN_POINT ( 'NONE',  ( 8.469665986256828205, 1.056999999999999940, 6.829619984160658046E-17 ) ) ;
#12962=DIRECTION ( 'NONE',  ( 1.000000000000000000, 0.000000000000000000, 0.000000000000000000 ) ) ;
#12969=CARTESIAN_POINT ( 'NONE',  ( 1.936238515863016874, 0.2305039212132600213, 0.4121290732901491394 ) ) ;
#12970=CARTESIAN_POINT ( 'NONE',  ( 3.102108017520305072, 0.6812791890164020536, -0.3964255093850734268 ) ) ;
#12972=CARTESIAN_POINT ( 'NONE',  ( 1.813794508430887964, 0.1486894511058793333, -0.4139507449637808145 ) ) ;
#12974=ORIENTED_EDGE ( 'NONE', *, *, #12470, .T. ) ;
#12976=EDGE_LOOP ( 'NONE', ( #9352, #4146, #5960, #7514 ) ) ;
#12977=ORIENTED_EDGE ( 'NONE', *, *, #4009, .T. ) ;
#12981=CARTESIAN_POINT ( 'NONE',  ( 8.475037399843312613, 0.9969999999999998863, 0.3802960819231170908 ) ) ;
#12995=CARTESIAN_POINT ( 'NONE',  ( 0.6570838759023790443, -0.3876519068829718528, 0.5130260770772535617 ) ) ;
#12998=EDGE_LOOP ( 'NONE', ( #5782, #4399, #7211, #4043, #9775 ) ) ;
#13000=CARTESIAN_POINT ( 'NONE',  ( 3.241046123363278131, 0.7391609583210639878, 0.4542225123818745547 ) ) ;
#13001=ORIENTED_EDGE ( 'NONE', *, *, #6524, .T. ) ;
#13002=CARTESIAN_POINT ( 'NONE',  ( 0.9672769954795885639, -0.4829975555521403008, -0.4081482409674996870 ) ) ;
#13008=ORIENTED_EDGE ( 'NONE', *, *, #13511, .T. ) ;
#13009=CARTESIAN_POINT ( 'NONE',  ( 0.6842449982442055934, -0.4393369316438217598, 0.4560737988759885897 ) ) ;
#13016=ORIENTED_EDGE ( 'NONE', *, *, #13511, .F. ) ;
#13017=( BOUNDED_CURVE ( )  B_SPLINE_CURVE ( 3, ( #6837, #2615, #4919, #7215 ),
 .UNSPECIFIED., .F., .T. ) 
 B_SPLINE_CURVE_WITH_KNOTS ( ( 4, 4 ),
 ( 0.7853981633974534970, 1.570796326794896336 ),
 .UNSPECIFIED. ) 
 CURVE ( )  GEOMETRIC_REPRESENTATION_ITEM ( )  RATIONAL_B_SPLINE_CURVE ( ( 1.000000000000000000, 0.9492530216741918991, 0.9492530216741918991, 1.000000000000000000 ) ) 
 REPRESENTATION_ITEM ( '' )  );
#13020=CARTESIAN_POINT ( 'NONE',  ( 1.261796151055236015, -0.4301078242393568951, -0.4222829664661058580 ) ) ;
#13030=CARTESIAN_POINT ( 'NONE',  ( 0.8369793835502591373, -0.4830000000000001514, -0.4162690208630439037 ) ) ;
#13035=CARTESIAN_POINT ( 'NONE',  ( 3.015109087180224771E-17, -0.4844395604395604904, 0.000000000000000000 ) ) ;
#13038=AXIS2_PLACEMENT_3D ( 'NONE', #9507, #6908, #8210 ) ;
#13051=FACE_OUTER_BOUND ( 'NONE', #6880, .T. ) ;
#13060=VECTOR ( 'NONE', #14230, 39.37007874015748143 ) ;
#13065=ADVANCED_FACE ( 'NONE', ( #14018 ), #2633, .F. ) ;
#13066=VERTEX_POINT ( 'NONE', #3637 ) ;
#13067=DIRECTION ( 'NONE',  ( -0.4938181170261085051, 0.000000000000000000, 0.8695652173913058780 ) ) ;
#13071=DIRECTION ( 'NONE',  ( 0.000000000000000000, 0.7071067811865430208, 0.7071067811865520136 ) ) ;
#13074=CARTESIAN_POINT ( 'NONE',  ( 2.854443715606396648, 0.5365358177142092178, 0.4001101571913798782 ) ) ;
#13082=ORIENTED_EDGE ( 'NONE', *, *, #10775, .F. ) ;
#13083=AXIS2_PLACEMENT_3D ( 'NONE', #2379, #5268, #13358 ) ;
#13088=ADVANCED_FACE ( 'NONE', ( #8321 ), #2398, .F. ) ;
#13097=CARTESIAN_POINT ( 'NONE',  ( 1.503855556006640448, -0.3209522984519411759, -0.4787591023162905413 ) ) ;
#13102=( BOUNDED_CURVE ( )  B_SPLINE_CURVE ( 3, ( #5352, #10936, #3833, #5195 ),
 .UNSPECIFIED., .F., .F. ) 
 B_SPLINE_CURVE_WITH_KNOTS ( ( 4, 4 ),
 ( 0.7853981633974463916, 1.570796326794896558 ),
 .UNSPECIFIED. ) 
 CURVE ( )  GEOMETRIC_REPRESENTATION_ITEM ( )  RATIONAL_B_SPLINE_CURVE ( ( 1.000000000000000000, 0.9492530216741910110, 0.9492530216741910110, 1.000000000000000000 ) ) 
 REPRESENTATION_ITEM ( '' )  );
#13106=ADVANCED_FACE ( 'NONE', ( #4865 ), #4594, .F. ) ;
#13111=DIRECTION ( 'NONE',  ( 1.000000000000000000, 0.000000000000000000, 0.000000000000000000 ) ) ;
#13114=CARTESIAN_POINT ( 'NONE',  ( 1.542522555076119239, 0.03620193991696377817, 0.4782129582616606589 ) ) ;
#13115=DIRECTION ( 'NONE',  ( 0.000000000000000000, -0.7071067811865366926, 0.7071067811865584529 ) ) ;
#13120=VERTEX_POINT ( 'NONE', #7236 ) ;
#13123=EDGE_CURVE ( 'NONE', #8716, #14113, #6308, .T. ) ;
#13127=CARTESIAN_POINT ( 'NONE',  ( 2.630032447663273043, 0.7405933021011417150, 0.4628526490443040653 ) ) ;
#13136=CARTESIAN_POINT ( 'NONE',  ( 0.8369029794110903753, -0.4829999991353697841, -0.4161243967669134847 ) ) ;
#13143=DIRECTION ( 'NONE',  ( 0.8695652173913053229, 0.000000000000000000, 0.4938181170261089492 ) ) ;
#13146=VECTOR ( 'NONE', #1925, 39.37007874015748854 ) ;
#13152=ORIENTED_EDGE ( 'NONE', *, *, #6820, .T. ) ;
#13155=EDGE_CURVE ( 'NONE', #1024, #14149, #9676, .T. ) ;
#13156=CARTESIAN_POINT ( 'NONE',  ( 0.6653223438648792065, 0.01646029051545267255, 0.4725272431374084592 ) ) ;
#13157=PLANE ( 'NONE',  #4627 ) ;
#13162=( NAMED_UNIT ( * ) PLANE_ANGLE_UNIT ( ) SI_UNIT ( $, .RADIAN. ) );
#13167=VERTEX_POINT ( 'NONE', #14326 ) ;
#13168=CARTESIAN_POINT ( 'NONE',  ( 0.7058998964907862161, -0.05999999999999994227, 0.4900296624789436950 ) ) ;
#13170=LINE ( 'NONE', #10602, #5122 ) ;
#13174=CONICAL_SURFACE ( 'NONE', #3180, 0.07000000000000047851, 0.7853981633974297383 ) ;
#13187=CARTESIAN_POINT ( 'NONE',  ( 2.045923089166573394, 0.3299328314968411058, 0.4711027812264608761 ) ) ;
#13195=CIRCLE ( 'NONE', #7362, 0.06000000000000005329 ) ;
#13212=CARTESIAN_POINT ( 'NONE',  ( 0.6583797813917271480, -0.3800069445035944571, 0.5137833636068753762 ) ) ;
#13217=CARTESIAN_POINT ( 'NONE',  ( 3.390179639970223313, 0.6913388717410868800, -0.3921396980529558429 ) ) ;
#13221=ADVANCED_FACE ( 'NONE', ( #10049 ), #8829, .F. ) ;
#13222=CARTESIAN_POINT ( 'NONE',  ( 0.6592137334438901153, 0.0006300111355865889223, 0.4885243083254864338 ) ) ;
#13225=CARTESIAN_POINT ( 'NONE',  ( 2.414213562373087374, 0.1427864376268978830, -0.4064941968476759038 ) ) ;
#13227=DIRECTION ( 'NONE',  ( -0.000000000000000000, -0.000000000000000000, -1.000000000000000000 ) ) ;
#13233=ORIENTED_EDGE ( 'NONE', *, *, #2625, .T. ) ;
#13237=EDGE_CURVE ( 'NONE', #12566, #8835, #8824, .T. ) ;
#13238=CARTESIAN_POINT ( 'NONE',  ( 8.475037399843314390, 0.9969999999999998863, -0.3802960819231170353 ) ) ;
#13243=CARTESIAN_POINT ( 'NONE',  ( 1.328406321535847256, -0.06000000000013446660, -0.4812371988483638008 ) ) ;
#13248=ORIENTED_EDGE ( 'NONE', *, *, #3934, .T. ) ;
#13249=ADVANCED_FACE ( 'NONE', ( #8601 ), #2780, .T. ) ;
#13250=DIRECTION ( 'NONE',  ( 0.7070715176384831935, 0.7070715176384805289, 0.009986885842351455114 ) ) ;
#13253=DIRECTION ( 'NONE',  ( 0.9999002670844990837, 0.000000000000000000, 0.01412288512831215773 ) ) ;
#13254=CARTESIAN_POINT ( 'NONE',  ( 0.8999999999999999112, -0.6429999999999999050, -0.4300000000000014921 ) ) ;
#13263=ORIENTED_EDGE ( 'NONE', *, *, #7729, .F. ) ;
#13265=CARTESIAN_POINT ( 'NONE',  ( 0.3724999999999997757, -0.6589999999999996971, -0.3725000000000000533 ) ) ;
#13269=DIRECTION ( 'NONE',  ( 0.000000000000000000, -1.000000000000000000, -0.000000000000000000 ) ) ;
#13284=PLANE ( 'NONE',  #15037 ) ;
#13296=CARTESIAN_POINT ( 'NONE',  ( 0.6742332106589076224, -0.02527202722326431922, 0.4798232997575394010 ) ) ;
#13307=ORIENTED_EDGE ( 'NONE', *, *, #6820, .F. ) ;
#13317=ORIENTED_EDGE ( 'NONE', *, *, #10412, .F. ) ;
#13320=EDGE_CURVE ( 'NONE', #251, #7417, #2637, .T. ) ;
#13322=CARTESIAN_POINT ( 'NONE',  ( 8.559253539154886070, 0.8718469098602883438, -0.3109429831200917205 ) ) ;
#13324=LINE ( 'NONE', #2720, #8496 ) ;
#13327=CARTESIAN_POINT ( 'NONE',  ( 0.7058998964907862161, -0.3830000000000000071, 0.4900296624789436950 ) ) ;
#13332=CONICAL_SURFACE ( 'NONE', #10911, 0.06999999999999829969, 0.7853981633974298493 ) ;
#13333=DIRECTION ( 'NONE',  ( -1.655665450705613915E-16, 0.000000000000000000, -1.000000000000000000 ) ) ;
#13341=AXIS2_PLACEMENT_3D ( 'NONE', #5640, #4483, #13487 ) ;
#13358=DIRECTION ( 'NONE',  ( 1.000000000000000000, 0.000000000000000000, 0.000000000000000000 ) ) ;
#13362=CARTESIAN_POINT ( 'NONE',  ( 0.6583858180919160974, -0.06301918258053597344, 0.5137832783427485062 ) ) ;
#13364=EDGE_LOOP ( 'NONE', ( #8826, #649, #6072, #403 ) ) ;
#13366=DIRECTION ( 'NONE',  ( -0.7070715176384831935, -0.7070715176384805289, 0.009986885842351455114 ) ) ;
#13367=CARTESIAN_POINT ( 'NONE',  ( 0.6821548861276044429, -0.006955760605970391988, 0.4605830663053103735 ) ) ;
#13368=CARTESIAN_POINT ( 'NONE',  ( 1.014923485655622848, -0.4429443392323548223, -0.3809436922965903083 ) ) ;
#13371=ORIENTED_EDGE ( 'NONE', *, *, #12218, .T. ) ;
#13375=AXIS2_PLACEMENT_3D ( 'NONE', #8961, #1979, #10107 ) ;
#13377=ORIENTED_EDGE ( 'NONE', *, *, #9081, .F. ) ;
#13384=CARTESIAN_POINT ( 'NONE',  ( 0.7023826192914041089, -0.05114289342557994111, 0.4896101277505872651 ) ) ;
#13386=CARTESIAN_POINT ( 'NONE',  ( 2.683697947871302336, 0.4122708231251094313, -0.4026504426247255464 ) ) ;
#13390=CARTESIAN_POINT ( 'NONE',  ( 1.503855556006640004, -0.3209522984523814904, 0.4787591023162903747 ) ) ;
#13391=CARTESIAN_POINT ( 'NONE',  ( 0.8264521039527233937, -0.4832232234379731373, -0.3598827494686853701 ) ) ;
#13398=CARTESIAN_POINT ( 'NONE',  ( 1.775981552640435668, 0.05988294188168103577, -0.4749155147932142551 ) ) ;
#13404=CARTESIAN_POINT ( 'NONE',  ( 8.802840746862885979, 0.9385542876807506651, -0.1899546695978221456 ) ) ;
#13414=EDGE_CURVE ( 'NONE', #5982, #7869, #11412, .T. ) ;
#13415=LINE ( 'NONE', #6323, #7607 ) ;
#13416=ORIENTED_EDGE ( 'NONE', *, *, #13320, .F. ) ;
#13428=CARTESIAN_POINT ( 'NONE',  ( -0.3725000000000000533, 0.1859999999999983611, 0.3724999999999999423 ) ) ;
#13429=EDGE_CURVE ( 'NONE', #11449, #436, #9123, .T. ) ;
#13430=LINE ( 'NONE', #5343, #14057 ) ;
#13440=EDGE_CURVE ( 'NONE', #7690, #5428, #9669, .T. ) ;
#13443=ORIENTED_EDGE ( 'NONE', *, *, #3123, .T. ) ;
#13445=DIRECTION ( 'NONE',  ( 0.000000000000000000, -1.000000000000000000, 0.000000000000000000 ) ) ;
#13449=CARTESIAN_POINT ( 'NONE',  ( 0.9699790962219284607, -0.4829911415283998921, -0.4026641122740337586 ) ) ;
#13456=CARTESIAN_POINT ( 'NONE',  ( 0.7513246802501660770, -0.4429999999999998939, 0.4293820849162031661 ) ) ;
#13460=VERTEX_POINT ( 'NONE', #68 ) ;
#13465=CARTESIAN_POINT ( 'NONE',  ( 0.8374688766003500762, -0.4832241325771656770, -0.3334326046303043856 ) ) ;
#13467=CARTESIAN_POINT ( 'NONE',  ( 0.9672649160634325671, -0.4430530727333169549, -0.4081727571047788494 ) ) ;
#13469=LINE ( 'NONE', #998, #9668 ) ;
#13475=CARTESIAN_POINT ( 'NONE',  ( 0.6552631510457631592, -0.4102150000379021222, -0.5075199847260437602 ) ) ;
#13478=EDGE_CURVE ( 'NONE', #184, #11754, #10390, .T. ) ;
#13479=CARTESIAN_POINT ( 'NONE',  ( 0.3724999999999999423, -0.6290000000000003366, 0.4124999999999999223 ) ) ;
#13481=CARTESIAN_POINT ( 'NONE',  ( 2.372634528609597115, 0.1852128444980938871, 0.4664882128727457777 ) ) ;
#13487=DIRECTION ( 'NONE',  ( 0.000000000000000000, 0.000000000000000000, 1.000000000000000000 ) ) ;
#13504=ORIENTED_EDGE ( 'NONE', *, *, #6560, .F. ) ;
#13506=FACE_OUTER_BOUND ( 'NONE', #2527, .T. ) ;
#13508=ORIENTED_EDGE ( 'NONE', *, *, #3098, .F. ) ;
#13511=EDGE_CURVE ( 'NONE', #13774, #2273, #2306, .T. ) ;
#13512=CARTESIAN_POINT ( 'NONE',  ( 0.6678556410416569555, 0.02086291274669062334, 0.4666787114416893201 ) ) ;
#13519=CARTESIAN_POINT ( 'NONE',  ( -0.3725000000000000533, 0.1859999999999983611, 0.4124999999999999223 ) ) ;
#13532=CYLINDRICAL_SURFACE ( 'NONE', #14002, 0.05999999999999995615 ) ;
#13533=ORIENTED_EDGE ( 'NONE', *, *, #4009, .F. ) ;
#13544=CARTESIAN_POINT ( 'NONE',  ( 0.8258105267240533065, -0.4829999999999998184, -0.3634189688144888741 ) ) ;
#13550=VERTEX_POINT ( 'NONE', #9435 ) ;
#13554=CARTESIAN_POINT ( 'NONE',  ( 0.6766092641689801512, -0.4260904363423368424, -0.4729901586420192094 ) ) ;
#13562=AXIS2_PLACEMENT_3D ( 'NONE', #14767, #3155, #2138 ) ;
#13566=AXIS2_PLACEMENT_3D ( 'NONE', #14108, #2566, #6015 ) ;
#13567=ORIENTED_EDGE ( 'NONE', *, *, #10775, .T. ) ;
#13568=DIRECTION ( 'NONE',  ( -0.000000000000000000, 1.000000000000000000, -0.000000000000000000 ) ) ;
#13570=CARTESIAN_POINT ( 'NONE',  ( 1.250000000000000222, -0.05999999999999997696, -0.4823446327683615364 ) ) ;
#13578=DIRECTION ( 'NONE',  ( 0.9743309173630048114, 0.2251205531944285021, 0.000000000000000000 ) ) ;
#13584=ORIENTED_EDGE ( 'NONE', *, *, #5785, .F. ) ;
#13595=CYLINDRICAL_SURFACE ( 'NONE', #4608, 1.124999999999999778 ) ;
#13597=DIRECTION ( 'NONE',  ( 0.8682164115033647045, 0.000000000000000000, -0.4961857140186728410 ) ) ;
#13598=ADVANCED_FACE ( 'NONE', ( #5282 ), #10395, .F. ) ;
#13599=CARTESIAN_POINT ( 'NONE',  ( 1.012991562538327006, -0.4429593234937804214, -0.3529545607104379590 ) ) ;
#13603=FACE_OUTER_BOUND ( 'NONE', #5933, .T. ) ;
#13614=ORIENTED_EDGE ( 'NONE', *, *, #12315, .T. ) ;
#13617=CARTESIAN_POINT ( 'NONE',  ( 2.684185600477509315, 0.4127059874557739705, -0.4620877740047383275 ) ) ;
#13622=DIRECTION ( 'NONE',  ( -1.000000000000000000, -1.365923996832131609E-16, 0.000000000000000000 ) ) ;
#13624=CIRCLE ( 'NONE', #9736, 0.05999999999999994227 ) ;
#13627=VECTOR ( 'NONE', #13366, 39.37007874015748143 ) ;
#13636=EDGE_CURVE ( 'NONE', #1866, #259, #2062, .T. ) ;
#13637=FACE_OUTER_BOUND ( 'NONE', #4369, .T. ) ;
#13645=VECTOR ( 'NONE', #515, 39.37007874015748143 ) ;
#13648=ORIENTED_EDGE ( 'NONE', *, *, #3515, .T. ) ;
#13657=VERTEX_POINT ( 'NONE', #7877 ) ;
#13659=ADVANCED_FACE ( 'NONE', ( #12527 ), #9357, .T. ) ;
#13660=EDGE_CURVE ( 'NONE', #3117, #10543, #6658, .T. ) ;
#13661=CARTESIAN_POINT ( 'NONE',  ( 0.6601485485260574215, -0.07064835164835239767, -0.5137583810202325241 ) ) ;
#13662=VECTOR ( 'NONE', #5898, 39.37007874015748854 ) ;
#13679=CARTESIAN_POINT ( 'NONE',  ( 3.602264755523620465, 1.056999999999999940, -0.4491205543005138412 ) ) ;
#13680=CARTESIAN_POINT ( 'NONE',  ( 0.9738485687486472253, -0.4432125501547143909, -0.3605661772192202408 ) ) ;
#13682=DIRECTION ( 'NONE',  ( -1.224646799147354933E-16, 0.000000000000000000, -1.000000000000000000 ) ) ;
#13686=FACE_OUTER_BOUND ( 'NONE', #9667, .T. ) ;
#13689=CARTESIAN_POINT ( 'NONE',  ( 0.9749999999999999778, -0.4829448521957645513, -0.3750000000000000555 ) ) ;
#13701=CARTESIAN_POINT ( 'NONE',  ( 8.849999999999999645, 0.8820000000000000062, 0.5000000000000000000 ) ) ;
#13710=AXIS2_PLACEMENT_3D ( 'NONE', #10157, #4343, #6875 ) ;
#13719=CARTESIAN_POINT ( 'NONE',  ( 8.469665986256828205, 0.9969999999999998863, 6.829619984160658046E-17 ) ) ;
#13723=CARTESIAN_POINT ( 'NONE',  ( 0.8108060929038570785, -0.4429999999999998939, -0.3024090436974096185 ) ) ;
#13724=CARTESIAN_POINT ( 'NONE',  ( 0.7513246802501660770, 0.05999999999999999778, 0.4293820849162031661 ) ) ;
#13728=CARTESIAN_POINT ( 'NONE',  ( 0.7017867892446606470, 0.04143956043956046470, -0.4010711782184316343 ) ) ;
#13729=CARTESIAN_POINT ( 'NONE',  ( 8.792093969802149189, 0.8799778768672790186, -0.1855527009831952900 ) ) ;
#13731=DIRECTION ( 'NONE',  ( -1.365923996832131609E-16, 1.000000000000000000, 0.000000000000000000 ) ) ;
#13736=ORIENTED_EDGE ( 'NONE', *, *, #1262, .T. ) ;
#13737=DIRECTION ( 'NONE',  ( -1.000000000000000000, -1.365923996832131609E-16, 0.000000000000000000 ) ) ;
#13740=FACE_OUTER_BOUND ( 'NONE', #1608, .T. ) ;
#13745=CARTESIAN_POINT ( 'NONE',  ( 0.6570999327328049811, -0.3875696543617488388, -0.5130307608016103638 ) ) ;
#13747=CARTESIAN_POINT ( 'NONE',  ( 3.339621231359971798, 1.044107824239214777, -0.3927132934523872576 ) ) ;
#13763=CIRCLE ( 'NONE', #9145, 0.05999999999999997696 ) ;
#13768=CARTESIAN_POINT ( 'NONE',  ( 1.000847373107698779, -0.3829999999999998961, 0.4858637376679703634 ) ) ;
#13769=LINE ( 'NONE', #1848, #54 ) ;
#13774=VERTEX_POINT ( 'NONE', #4377 ) ;
#13775=DIRECTION ( 'NONE',  ( -1.000000000000000000, 0.000000000000000000, 0.000000000000000000 ) ) ;
#13776=CARTESIAN_POINT ( 'NONE',  ( 0.7849999999999999201, -0.4429999999999998939, -0.3750000000000000555 ) ) ;
#13778=CARTESIAN_POINT ( 'NONE',  ( 2.889807021265108578, 0.6241886699583397702, 0.4591835166487979181 ) ) ;
#13779=CARTESIAN_POINT ( 'NONE',  ( 0.7145271609291456993, -0.4320022011844609211, -0.4647412378891554452 ) ) ;
#13792=AXIS2_PLACEMENT_3D ( 'NONE', #5692, #8987, #10349 ) ;
#13795=CARTESIAN_POINT ( 'NONE',  ( -0.3725000000000000533, 0.2159999999999999698, 0.3724999999999999423 ) ) ;
#13798=CARTESIAN_POINT ( 'NONE',  ( 0.6577550957999014347, -0.05999999999999997696, 0.4907096737881370130 ) ) ;
#13801=CARTESIAN_POINT ( 'NONE',  ( -0.4125000000000001998, -0.6590000000000000302, -0.4125000000000000333 ) ) ;
#13802=ORIENTED_EDGE ( 'NONE', *, *, #4878, .T. ) ;
#13804=CARTESIAN_POINT ( 'NONE',  ( 0.6733128806866804927, 0.02908293500952287974, -0.4545362700951161017 ) ) ;
#13815=EDGE_LOOP ( 'NONE', ( #7631, #5037, #3251, #14238 ) ) ;
#13821=DIRECTION ( 'NONE',  ( -1.000000000000000000, 0.000000000000000000, 0.000000000000000000 ) ) ;
#13822=CARTESIAN_POINT ( 'NONE',  ( 0.6583858180919160974, -0.3799808174194639343, -0.5137832783427485062 ) ) ;
#13824=CYLINDRICAL_SURFACE ( 'NONE', #12790, 2.000000000000000000 ) ;
#13830=CARTESIAN_POINT ( 'NONE',  ( 7.623651669702752511E-17, -0.6589999999999998082, 0.000000000000000000 ) ) ;
#13836=ORIENTED_EDGE ( 'NONE', *, *, #2500, .F. ) ;
#13837=CARTESIAN_POINT ( 'NONE',  ( 0.6940273316166111206, 0.04143956043956045082, -0.4146485309448424417 ) ) ;
#13840=CARTESIAN_POINT ( 'NONE',  ( 2.889807021265107689, 0.6241886699584686671, -0.4591835166487980291 ) ) ;
#13842=EDGE_CURVE ( 'NONE', #11117, #10000, #12497, .T. ) ;
#13843=CARTESIAN_POINT ( 'NONE',  ( 2.321652452207092043, 0.05022532746090251771, 0.4077623363514504828 ) ) ;
#13845=CARTESIAN_POINT ( 'NONE',  ( -0.7287617923574203349, -0.6590000000000000302, 0.4424999999999983391 ) ) ;
#13846=VECTOR ( 'NONE', #1720, 39.37007874015748143 ) ;
#13849=ORIENTED_EDGE ( 'NONE', *, *, #5302, .T. ) ;
#13850=DIRECTION ( 'NONE',  ( -0.000000000000000000, -0.000000000000000000, -1.000000000000000000 ) ) ;
#13865=AXIS2_PLACEMENT_3D ( 'NONE', #11093, #3148, #1825 ) ;
#13870=CARTESIAN_POINT ( 'NONE',  ( 3.388933043275772494, 0.7513023213622327390, -0.4521337140780258279 ) ) ;
#13874=DIRECTION ( 'NONE',  ( 1.000000000000000000, 1.365923996832131609E-16, 0.000000000000000000 ) ) ;
#13878=CARTESIAN_POINT ( 'NONE',  ( 0.7051258599873416744, -0.02178283142415348567, -0.4764739269522892395 ) ) ;
#13890=ORIENTED_EDGE ( 'NONE', *, *, #4943, .F. ) ;
#13892=ORIENTED_EDGE ( 'NONE', *, *, #11981, .T. ) ;
#13895=CARTESIAN_POINT ( 'NONE',  ( 0.007060738305901492935, -0.2214999999999999469, -0.4999002720578262782 ) ) ;
#13897=DIRECTION ( 'NONE',  ( -1.000000000000000000, 0.000000000000000000, 1.639108796198557537E-14 ) ) ;
#13907=CYLINDRICAL_SURFACE ( 'NONE', #8224, 1.124999999999999556 ) ;
#13910=DIRECTION ( 'NONE',  ( -1.000000000000000000, -2.130223169792495565E-16, 0.000000000000000000 ) ) ;
#13922=CARTESIAN_POINT ( 'NONE',  ( 3.096478849372235942, 0.7064487239733228119, -0.4562644230314656935 ) ) ;
#13924=CARTESIAN_POINT ( 'NONE',  ( 0.9672769954795885639, -0.4829975555521403008, -0.4081482409674996870 ) ) ;
#13926=ORIENTED_EDGE ( 'NONE', *, *, #11946, .T. ) ;
#13927=CARTESIAN_POINT ( 'NONE',  ( 0.7022716438625806745, -0.4145615347806886342, 0.4812718407965458356 ) ) ;
#13928=DIRECTION ( 'NONE',  ( -0.01412288512831583534, 0.000000000000000000, -0.9999002670844989726 ) ) ;
#13943=DIRECTION ( 'NONE',  ( 0.7071067811865607844, -0.7071067811865343611, -1.170732267570243064E-16 ) ) ;
#13948=DIRECTION ( 'NONE',  ( -0.000000000000000000, 1.000000000000000000, -0.000000000000000000 ) ) ;
#13953=DIRECTION ( 'NONE',  ( 0.000000000000000000, -0.7071067811865587860, -0.7071067811865362485 ) ) ;
#13955=ORIENTED_EDGE ( 'NONE', *, *, #10322, .T. ) ;
#13957=CARTESIAN_POINT ( 'NONE',  ( 0.6867276282385254005, 0.03909868245979658541, -0.4280639610650152638 ) ) ;
#13958=LINE ( 'NONE', #5877, #11512 ) ;
#13959=CARTESIAN_POINT ( 'NONE',  ( 2.372634528609593119, 0.1852128444980909450, -0.4664882128727458888 ) ) ;
#13964=VERTEX_POINT ( 'NONE', #3372 ) ;
#13969=CIRCLE ( 'NONE', #5695, 0.05999999999999997696 ) ;
#13974=CARTESIAN_POINT ( 'NONE',  ( 0.6555297760382666761, -0.4026665662008522828, -0.5099209754895143165 ) ) ;
#13977=CYLINDRICAL_SURFACE ( 'NONE', #10354, 0.06000000000000001166 ) ;
#13979=FACE_OUTER_BOUND ( 'NONE', #1640, .T. ) ;
#13983=CARTESIAN_POINT ( 'NONE',  ( 8.475037399843312613, 0.9289129992088659415, 0.3802960819231170908 ) ) ;
#13987=ORIENTED_EDGE ( 'NONE', *, *, #4145, .F. ) ;
#13992=ORIENTED_EDGE ( 'NONE', *, *, #15049, .F. ) ;
#13994=DIRECTION ( 'NONE',  ( 0.000000000000000000, 0.000000000000000000, -1.000000000000000000 ) ) ;
#14002=AXIS2_PLACEMENT_3D ( 'NONE', #10270, #7889, #3077 ) ;
#14010=LINE ( 'NONE', #5541, #8837 ) ;
#14014=AXIS2_PLACEMENT_3D ( 'NONE', #11793, #5677, #11727 ) ;
#14018=FACE_OUTER_BOUND ( 'NONE', #11835, .T. ) ;
#14020=CIRCLE ( 'NONE', #815, 0.06000000000000003941 ) ;
#14022=PRODUCT_DEFINITION_FORMATION_WITH_SPECIFIED_SOURCE ( 'ANY', '', #8859, .NOT_KNOWN. ) ;
#14030=CIRCLE ( 'NONE', #1815, 0.07500000000000002498 ) ;
#14031=CARTESIAN_POINT ( 'NONE',  ( 0.7238772453881179292, -0.005046247197760479232, -0.4547576871318953495 ) ) ;
#14046=DIRECTION ( 'NONE',  ( 0.000000000000000000, -1.000000000000000000, 0.000000000000000000 ) ) ;
#14053=FACE_BOUND ( 'NONE', #36, .T. ) ;
#14056=FACE_BOUND ( 'NONE', #8564, .T. ) ;
#14057=VECTOR ( 'NONE', #6570, 39.37007874015748854 ) ;
#14058=AXIS2_PLACEMENT_3D ( 'NONE', #2491, #13948, #11897 ) ;
#14069=EDGE_LOOP ( 'NONE', ( #12090, #6576, #4418, #11133 ) ) ;
#14074=CARTESIAN_POINT ( 'NONE',  ( 2.917021349547979536, 0.5710164562863511151, 0.4587991334809356503 ) ) ;
#14075=ORIENTED_EDGE ( 'NONE', *, *, #2823, .T. ) ;
#14078=EDGE_CURVE ( 'NONE', #14557, #2844, #11977, .T. ) ;
#14079=ADVANCED_FACE ( 'NONE', ( #14293 ), #13284, .F. ) ;
#14080=AXIS2_PLACEMENT_3D ( 'NONE', #11303, #12375, #1967 ) ;
#14082=EDGE_CURVE ( 'NONE', #1005, #2093, #12345, .T. ) ;
#14083=DIRECTION ( 'NONE',  ( 0.03489949670248613384, -0.9993908270190963172, 0.000000000000000000 ) ) ;
#14084=ORIENTED_EDGE ( 'NONE', *, *, #2107, .F. ) ;
#14086=CONICAL_SURFACE ( 'NONE', #2853, 0.06999999999999829969, 0.7853981633974298493 ) ;
#14095=EDGE_LOOP ( 'NONE', ( #3009, #217, #12376, #4082 ) ) ;
#14096=( BOUNDED_CURVE ( )  B_SPLINE_CURVE ( 3, ( #11782, #3516, #10257, #5741 ),
 .UNSPECIFIED., .F., .F. ) 
 B_SPLINE_CURVE_WITH_KNOTS ( ( 4, 4 ),
 ( 0.000000000000000000, 1.556672972142351341 ),
 .UNSPECIFIED. ) 
 CURVE ( )  GEOMETRIC_REPRESENTATION_ITEM ( )  RATIONAL_B_SPLINE_CURVE ( ( 1.000000000000000000, 0.8080549792898082950, 0.8080549792898082950, 1.000000000000000000 ) ) 
 REPRESENTATION_ITEM ( '' )  );
#14098=CARTESIAN_POINT ( 'NONE',  ( 8.469665986256828205, 0.9969999999999998863, 6.829619984160658046E-17 ) ) ;
#14103=ORIENTED_EDGE ( 'NONE', *, *, #10363, .T. ) ;
#14105=ORIENTED_EDGE ( 'NONE', *, *, #1455, .F. ) ;
#14108=CARTESIAN_POINT ( 'NONE',  ( -0.7287617923574203349, -0.6590000000000000302, -0.4424999999999983391 ) ) ;
#14109=CARTESIAN_POINT ( 'NONE',  ( 3.085497600961857767, 0.7407061222255643118, -0.4564195254101433008 ) ) ;
#14113=VERTEX_POINT ( 'NONE', #2682 ) ;
#14116=CARTESIAN_POINT ( 'NONE',  ( 1.775981552640430561, 0.05988294188167953003, 0.4749155147932142551 ) ) ;
#14131=ADVANCED_FACE ( 'NONE', ( #1515 ), #7419, .F. ) ;
#14144=CIRCLE ( 'NONE', #1185, 0.8653656741516848605 ) ;
#14145=CARTESIAN_POINT ( 'NONE',  ( 8.476283996537762988, 0.8689495495877206377, 0.3203020658980472168 ) ) ;
#14149=VERTEX_POINT ( 'NONE', #5974 ) ;
#14161=DIRECTION ( 'NONE',  ( -0.000000000000000000, 1.000000000000000000, -0.000000000000000000 ) ) ;
#14162=CARTESIAN_POINT ( 'NONE',  ( 0.9652705920801475381, -0.4828330467331339304, -0.4119425203458965679 ) ) ;
#14163=AXIS2_PLACEMENT_3D ( 'NONE', #14098, #12874, #4630 ) ;
#14174=EDGE_LOOP ( 'NONE', ( #7184, #6748, #8406, #10147, #1247, #13955, #465, #4044, #4713, #1757, #4179, #9916 ) ) ;
#14176=CARTESIAN_POINT ( 'NONE',  ( 0.7983174577546989781, -0.4429999999999998939, -0.4287183451209413132 ) ) ;
#14183=ADVANCED_FACE ( 'NONE', ( #12571 ), #862, .F. ) ;
#14184=FACE_OUTER_BOUND ( 'NONE', #12260, .T. ) ;
#14187=CARTESIAN_POINT ( 'NONE',  ( 0.9318415243661355429, -0.4679825767129147662, -0.4432104562656360991 ) ) ;
#14188=FACE_OUTER_BOUND ( 'NONE', #7251, .T. ) ;
#14193=CARTESIAN_POINT ( 'NONE',  ( 1.250847373107698557, -0.05999999999999990757, 0.4823326642216426707 ) ) ;
#14194=DIRECTION ( 'NONE',  ( 0.000000000000000000, 1.000000000000000000, -0.000000000000000000 ) ) ;
#14215=FACE_OUTER_BOUND ( 'NONE', #3429, .T. ) ;
#14216=EDGE_CURVE ( 'NONE', #1024, #7355, #6865, .T. ) ;
#14219=ADVANCED_BREP_SHAPE_REPRESENTATION ( '', ( #10334, #8424 ), #9874 ) ;
#14221=CARTESIAN_POINT ( 'NONE',  ( 0.7017867892446606470, -0.4844395604395603239, 0.4010711782184315233 ) ) ;
#14228=DIRECTION ( 'NONE',  ( -1.000000000000000000, 0.000000000000000000, 0.000000000000000000 ) ) ;
#14230=DIRECTION ( 'NONE',  ( -1.655665450705613915E-16, -3.103226861728128995E-32, -1.000000000000000000 ) ) ;
#14233=EDGE_CURVE ( 'NONE', #8835, #7260, #3324, .T. ) ;
#14238=ORIENTED_EDGE ( 'NONE', *, *, #5256, .F. ) ;
#14241=CARTESIAN_POINT ( 'NONE',  ( 0.7007556580885032638, -0.04192514642889976634, 0.4875099722676214387 ) ) ;
#14242=ORIENTED_EDGE ( 'NONE', *, *, #2359, .F. ) ;
#14260=CARTESIAN_POINT ( 'NONE',  ( 1.000000000000000222, -0.4429999999999998939, 0.4258697216429003785 ) ) ;
#14265=EDGE_CURVE ( 'NONE', #8543, #6823, #2973, .T. ) ;
#14273=EDGE_LOOP ( 'NONE', ( #5484, #8813, #5378, #14514 ) ) ;
#14277=CARTESIAN_POINT ( 'NONE',  ( 1.569329279054357817, -0.05999999999999986594, -0.4778343322167463159 ) ) ;
#14281=DIRECTION ( 'NONE',  ( 0.9999002670844989726, 1.365787769249574676E-16, 0.01412288512831212997 ) ) ;
#14282=CARTESIAN_POINT ( 'NONE',  ( 0.9999999999999996669, 1.557000000000000162, 0.5000000000000000000 ) ) ;
#14285=CIRCLE ( 'NONE', #7936, 0.7406097974541305806 ) ;
#14288=AXIS2_PLACEMENT_3D ( 'NONE', #8370, #14161, #15083 ) ;
#14289=CARTESIAN_POINT ( 'NONE',  ( 0.8604590016951504383, -0.4457786592069787335, -0.4394318790773389938 ) ) ;
#14293=FACE_OUTER_BOUND ( 'NONE', #2902, .T. ) ;
#14301=CARTESIAN_POINT ( 'NONE',  ( 3.112533253352849805, 0.6487563425743173573, 0.3962704070064358985 ) ) ;
#14303=CARTESIAN_POINT ( 'NONE',  ( 2.414213562373087374, 0.1427864376268978830, -0.4064941968476759038 ) ) ;
#14307=CARTESIAN_POINT ( 'NONE',  ( 0.7073825753665664573, 0.002585322401334269778, 0.4167523536742891443 ) ) ;
#14318=ORIENTED_EDGE ( 'NONE', *, *, #4476, .T. ) ;
#14320=ORIENTED_EDGE ( 'NONE', *, *, #1455, .T. ) ;
#14326=CARTESIAN_POINT ( 'NONE',  ( 0.4124999999999997558, -0.6290000000000003366, -0.3725000000000000533 ) ) ;
#14330=ORIENTED_EDGE ( 'NONE', *, *, #8373, .T. ) ;
#14331=VERTEX_POINT ( 'NONE', #8164 ) ;
#14333=CARTESIAN_POINT ( 'NONE',  ( 8.524379033352612822, 0.9303642257649956671, -0.3795991661955845919 ) ) ;
#14340=CARTESIAN_POINT ( 'NONE',  ( 1.632672928280226810, 0.0005225660665699846837, 0.4769396479056465243 ) ) ;
#14346=FACE_OUTER_BOUND ( 'NONE', #11535, .T. ) ;
#14352=CARTESIAN_POINT ( 'NONE',  ( 3.602264755523620465, 0.9969999999999997753, 0.4491205543005138412 ) ) ;
#14354=ADVANCED_FACE ( 'NONE', ( #14184 ), #1176, .F. ) ;
#14356=CYLINDRICAL_SURFACE ( 'NONE', #1675, 2.000000000000000000 ) ;
#14371=VERTEX_POINT ( 'NONE', #10678 ) ;
#14372=ADVANCED_FACE ( 'NONE', ( #7245 ), #853, .F. ) ;
#14377=EDGE_CURVE ( 'NONE', #1005, #1733, #7060, .T. ) ;
#14382=DIMENSIONAL_EXPONENTS ( 1.000000000000000000, 0.000000000000000000, 0.000000000000000000, 0.000000000000000000, 0.000000000000000000, 0.000000000000000000, 0.000000000000000000 ) ;
#14383=EDGE_CURVE ( 'NONE', #6823, #3261, #373, .T. ) ;
#14385=CIRCLE ( 'NONE', #9997, 0.6700292969071727223 ) ;
#14392=LINE ( 'NONE', #3925, #3881 ) ;
#14395=ADVANCED_FACE ( 'NONE', ( #5019 ), #313, .F. ) ;
#14398=CARTESIAN_POINT ( 'NONE',  ( 0.7095752389709886199, -0.01561891520650799531, 0.4705416541824799515 ) ) ;
#14401=CIRCLE ( 'NONE', #9993, 0.8083085967350902568 ) ;
#14405=DIRECTION ( 'NONE',  ( 0.9999002670844989726, -2.602203049398214110E-17, 0.01412288512831212997 ) ) ;
#14408=CARTESIAN_POINT ( 'NONE',  ( 1.993930392107171823, 0.2778841324403868995, -0.4718371413552246429 ) ) ;
#14418=CARTESIAN_POINT ( 'NONE',  ( -5.764454660286586870E-18, -0.2214999999999999469, 0.000000000000000000 ) ) ;
#14421=ADVANCED_FACE ( 'NONE', ( #469 ), #4663, .T. ) ;
#14427=DIRECTION ( 'NONE',  ( -1.000000000000000000, 0.000000000000000000, -9.106159978880873451E-16 ) ) ;
#14445=ORIENTED_EDGE ( 'NONE', *, *, #8154, .F. ) ;
#14446=DIRECTION ( 'NONE',  ( -0.7071067811865604513, 0.7071067811865345831, 1.170732267570242325E-16 ) ) ;
#14447=CARTESIAN_POINT ( 'NONE',  ( 8.475037399843312613, 0.9289129992088659415, 0.3802960819231170908 ) ) ;
#14452=CARTESIAN_POINT ( 'NONE',  ( 0.6552631510457654906, -0.03278499996209151279, 0.5075199847260384312 ) ) ;
#14460=DIRECTION ( 'NONE',  ( -0.7070715176384863021, -0.7070715176384774203, -0.009986885842351498482 ) ) ;
#14463=EDGE_CURVE ( 'NONE', #12577, #34, #10900, .T. ) ;
#14464=CARTESIAN_POINT ( 'NONE',  ( 0.7034553201775792797, -0.02513445208134620565, 0.4790822413290390935 ) ) ;
#14469=CARTESIAN_POINT ( 'NONE',  ( 0.8254245316410399047, -0.4829999999999998739, -0.3670313414528084683 ) ) ;
#14472=CARTESIAN_POINT ( 'NONE',  ( 2.045923089166570730, 0.3299328314968389964, -0.4711027812264609871 ) ) ;
#14486=AXIS2_PLACEMENT_3D ( 'NONE', #9266, #3514, #2285 ) ;
#14513=ORIENTED_EDGE ( 'NONE', *, *, #5302, .F. ) ;
#14514=ORIENTED_EDGE ( 'NONE', *, *, #4316, .F. ) ;
#14522=EDGE_CURVE ( 'NONE', #12064, #5075, #7485, .T. ) ;
#14525=CARTESIAN_POINT ( 'NONE',  ( 0.7013471289190064129, -0.03216119633915270892, 0.4834044059207765476 ) ) ;
#14526=CARTESIAN_POINT ( 'NONE',  ( 0.4425000000000001155, 0.2159999999999999420, -0.8500000000000000888 ) ) ;
#14531=VECTOR ( 'NONE', #14600, 39.37007874015748854 ) ;
#14534=VERTEX_POINT ( 'NONE', #13776 ) ;
#14545=CARTESIAN_POINT ( 'NONE',  ( 1.131687341751771880, -0.4429445645322995784, 0.4840157155121827537 ) ) ;
#14546=CARTESIAN_POINT ( 'NONE',  ( 0.8395363466603752434, -0.4830000013348689780, -0.3304764024893170338 ) ) ;
#14553=CARTESIAN_POINT ( 'NONE',  ( 1.973685276483752471, 0.1827974636779304551, -0.4721230893152013053 ) ) ;
#14557=VERTEX_POINT ( 'NONE', #12338 ) ;
#14562=EDGE_CURVE ( 'NONE', #11419, #8572, #8703, .T. ) ;
#14567=EDGE_CURVE ( 'NONE', #9809, #6905, #6809, .T. ) ;
#14571=VERTEX_POINT ( 'NONE', #3176 ) ;
#14573=EDGE_LOOP ( 'NONE', ( #478, #12160, #4962, #13317 ) ) ;
#14578=CARTESIAN_POINT ( 'NONE',  ( 3.099256572624754735, 0.9349522984520411972, 0.4562251896521927197 ) ) ;
#14579=ORIENTED_EDGE ( 'NONE', *, *, #7198, .F. ) ;
#14580=( BOUNDED_CURVE ( )  B_SPLINE_CURVE ( 3, ( #397, #543, #9829, #2945 ),
 .UNSPECIFIED., .F., .F. ) 
 B_SPLINE_CURVE_WITH_KNOTS ( ( 4, 4 ),
 ( 0.000000000000000000, 1.556672972142350675 ),
 .UNSPECIFIED. ) 
 CURVE ( )  GEOMETRIC_REPRESENTATION_ITEM ( )  RATIONAL_B_SPLINE_CURVE ( ( 1.000000000000000000, 0.8080549792898082950, 0.8080549792898082950, 1.000000000000000000 ) ) 
 REPRESENTATION_ITEM ( '' )  );
#14582=DIRECTION ( 'NONE',  ( 0.01412288512831583534, 0.000000000000000000, 0.9999002670844989726 ) ) ;
#14600=DIRECTION ( 'NONE',  ( -0.9999002670844989726, -1.365787769249574676E-16, -0.01412288512831212997 ) ) ;
#14605=VECTOR ( 'NONE', #13269, 39.37007874015748143 ) ;
#14607=CARTESIAN_POINT ( 'NONE',  ( 0.7026404547606494022, -0.05184959461285652826, 0.4896627279036661617 ) ) ;
#14608=CARTESIAN_POINT ( 'NONE',  ( 0.3724999999999997757, -0.6290000000000004476, -0.4125000000000000333 ) ) ;
#14609=ORIENTED_EDGE ( 'NONE', *, *, #14377, .F. ) ;
#14614=DIRECTION ( 'NONE',  ( 2.602462600580851747E-17, 1.000000000000000000, -0.000000000000000000 ) ) ;
#14633=ORIENTED_EDGE ( 'NONE', *, *, #364, .T. ) ;
#14637=CARTESIAN_POINT ( 'NONE',  ( 1.612492615670229279, 0.05745813234176332107, -0.4169456318805929707 ) ) ;
#14640=ORIENTED_EDGE ( 'NONE', *, *, #2162, .F. ) ;
#14642=VERTEX_POINT ( 'NONE', #1004 ) ;
#14650=ORIENTED_EDGE ( 'NONE', *, *, #8325, .F. ) ;
#14657=VERTEX_POINT ( 'NONE', #5925 ) ;
#14662=CARTESIAN_POINT ( 'NONE',  ( 3.082852245407272207, 0.9930332973736890612, 0.3962311736271780793 ) ) ;
#14665=DIRECTION ( 'NONE',  ( 0.000000000000000000, 1.000000000000000000, 0.000000000000000000 ) ) ;
#14679=( BOUNDED_SURFACE ( )  B_SPLINE_SURFACE ( 3, 2, ( 
 ( #12012, #10796, #12935 ),
 ( #11507, #4917, #5698 ),
 ( #13000, #286, #9652 ),
 ( #10355, #4547, #14301 ),
 ( #1522, #3837, #7213 ),
 ( #13778, #14074, #1450 ),
 ( #11867, #6057, #13074 ),
 ( #7142, #7359, #15019 ),
 ( #5981, #10721, #2462 ),
 ( #10285, #9584, #7289 ) ),
 .UNSPECIFIED., .F., .F., .F. ) 
 B_SPLINE_SURFACE_WITH_KNOTS ( ( 4, 2, 2, 2, 4 ),
 ( 3, 3 ),
 ( 1.605702911834775426, 1.793325806424166391, 1.980948701013557578, 2.168571595602948765, 2.356194490192339952 ),
 ( 0.000000000000000000, 1.000000000000000000 ),
 .UNSPECIFIED. ) 
 GEOMETRIC_REPRESENTATION_ITEM ( )  RATIONAL_B_SPLINE_SURFACE ( (
 ( 1.000000000000000000, 0.7072810196742752575, 1.000000000000000000),
 ( 1.000000000000000000, 0.7075930366720845077, 1.000000000000000000),
 ( 1.000000000000000000, 0.7079038033994521362, 1.000000000000000000),
 ( 1.000000000000000000, 0.7085120144470745673, 1.000000000000000000),
 ( 1.000000000000000000, 0.7088094415865170417, 1.000000000000000000),
 ( 1.000000000000000000, 0.7093805931376407914, 1.000000000000000000),
 ( 1.000000000000000000, 0.7096543062745851449, 1.000000000000000000),
 ( 1.000000000000000000, 0.7101685202382782558, 1.000000000000000000),
 ( 1.000000000000000000, 0.7104090318599831644, 1.000000000000000000),
 ( 1.000000000000000000, 0.7106287314217426543, 1.000000000000000000) ) ) 
 REPRESENTATION_ITEM ( '' )  SURFACE ( )  );
#14681=EDGE_CURVE ( 'NONE', #14331, #14837, #4493, .T. ) ;
#14690=DIRECTION ( 'NONE',  ( -0.4961857140186726189, -0.000000000000000000, -0.8682164115033648155 ) ) ;
#14695=DIRECTION ( 'NONE',  ( -0.7070715176384851919, -0.7070715176384784195, -0.009986885842354102302 ) ) ;
#14701=CARTESIAN_POINT ( 'NONE',  ( 0.9741570934736516474, -0.4829555140690277582, -0.3620636361668077008 ) ) ;
#14706=CARTESIAN_POINT ( 'NONE',  ( 1.644431316732426263, -0.3408522091762651307, 0.4170406485182424627 ) ) ;
#14707=CARTESIAN_POINT ( 'NONE',  ( 0.8282270537073739280, -0.4835892651647821783, -0.3529439700516306955 ) ) ;
#14712=CARTESIAN_POINT ( 'NONE',  ( 0.7038889044926298633, -0.3873518276109626512, -0.4900580663207255161 ) ) ;
#14716=DIRECTION ( 'NONE',  ( -0.8702745610686326572, 0.000000000000000000, 0.4925669379452895513 ) ) ;
#14719=CARTESIAN_POINT ( 'NONE',  ( 0.6570985677785624590, -0.3875776804055264257, -0.5130299739594079700 ) ) ;
#14730=DIRECTION ( 'NONE',  ( -0.6312257069790480069, 0.000000000000000000, -0.7755991921403740941 ) ) ;
#14731=CARTESIAN_POINT ( 'NONE',  ( 0.7851380656309442374, -0.4451990772328827672, -0.3237718568205412151 ) ) ;
#14733=EDGE_LOOP ( 'NONE', ( #14318, #9094, #3983, #8232 ) ) ;
#14741=AXIS2_PLACEMENT_3D ( 'NONE', #4837, #10644, #7062 ) ;
#14743=CARTESIAN_POINT ( 'NONE',  ( 0.8770054111157354892, -0.4307805394128523813, -0.4639681125059474387 ) ) ;
#14747=ORIENTED_EDGE ( 'NONE', *, *, #8768, .T. ) ;
#14749=CARTESIAN_POINT ( 'NONE',  ( 2.372634528609593119, 0.1852128444980909450, -0.4664882128727458888 ) ) ;
#14750=EDGE_LOOP ( 'NONE', ( #6630, #5731 ) ) ;
#14759=CARTESIAN_POINT ( 'NONE',  ( 0.9652173913043480269, -0.4429999999999998939, -0.3379636412230419551 ) ) ;
#14767=CARTESIAN_POINT ( 'NONE',  ( 2.087921535706059650, 0.2870784642939429587, 0.4105035982572216025 ) ) ;
#14771=DIRECTION ( 'NONE',  ( 0.01412288512831583534, 0.000000000000000000, -0.9999002670844989726 ) ) ;
#14778=VECTOR ( 'NONE', #2363, 39.37007874015748143 ) ;
#14784=DIRECTION ( 'NONE',  ( -1.000000000000000000, -2.130223169792495565E-16, 0.000000000000000000 ) ) ;
#14786=ORIENTED_EDGE ( 'NONE', *, *, #3634, .T. ) ;
#14794=DIRECTION ( 'NONE',  ( 0.000000000000000000, 0.000000000000000000, -1.000000000000000000 ) ) ;
#14798=ORIENTED_EDGE ( 'NONE', *, *, #7281, .T. ) ;
#14799=CARTESIAN_POINT ( 'NONE',  ( -5.764454660286586870E-18, -0.2214999999999999469, 0.000000000000000000 ) ) ;
#14804=VERTEX_POINT ( 'NONE', #9298 ) ;
#14807=DIRECTION ( 'NONE',  ( 0.000000000000000000, -1.000000000000000000, 0.000000000000000000 ) ) ;
#14809=CARTESIAN_POINT ( 'NONE',  ( 0.7926600297304221554, -0.4443591734166930096, -0.3139846204486113623 ) ) ;
#14813=CARTESIAN_POINT ( 'NONE',  ( 2.633946444925666874, 0.3625193201794746356, 0.4033906250602100618 ) ) ;
#14815=CARTESIAN_POINT ( 'NONE',  ( 0.6746175797782247852, -0.05587126532790559486, -0.4907030699473264868 ) ) ;
#14816=CIRCLE ( 'NONE', #11661, 0.07500000000000002498 ) ;
#14823=EDGE_LOOP ( 'NONE', ( #5801, #3482, #9255, #10934 ) ) ;
#14824=CARTESIAN_POINT ( 'NONE',  ( 0.3724999999999999423, -0.6589999999999996971, 0.3724999999999999423 ) ) ;
#14830=AXIS2_PLACEMENT_3D ( 'NONE', #12356, #9153, #3113 ) ;
#14836=CARTESIAN_POINT ( 'NONE',  ( 1.014392645310246754, -0.4429482298831206033, -0.3623584098607407489 ) ) ;
#14837=VERTEX_POINT ( 'NONE', #1468 ) ;
#14843=EDGE_CURVE ( 'NONE', #11355, #14657, #10490, .T. ) ;
#14848=DIRECTION ( 'NONE',  ( 0.000000000000000000, 0.000000000000000000, -1.000000000000000000 ) ) ;
#14852=EDGE_CURVE ( 'NONE', #5216, #1024, #1513, .T. ) ;
#14853=CARTESIAN_POINT ( 'NONE',  ( 0.7429783265673733927, -0.4429999999999999494, -0.4366554833170141481 ) ) ;
#14855=AXIS2_PLACEMENT_3D ( 'NONE', #2988, #10261, #12609 ) ;
#14860=CARTESIAN_POINT ( 'NONE',  ( 0.8293581428695305791, -0.4837316503856468053, -0.3495487851854117145 ) ) ;
#14868=VECTOR ( 'NONE', #1456, 39.37007874015748143 ) ;
#14871=CARTESIAN_POINT ( 'NONE',  ( 0.6734800455634237792, -0.4130371149665958419, -0.4827503109326044539 ) ) ;
#14874=AXIS2_PLACEMENT_3D ( 'NONE', #5814, #10251, #2366 ) ;
#14875=AXIS2_PLACEMENT_3D ( 'NONE', #13428, #11296, #2963 ) ;
#14889=CARTESIAN_POINT ( 'NONE',  ( 0.7811313390194075668, -0.4446478369844531486, -0.3386457300789465497 ) ) ;
#14893=CARTESIAN_POINT ( 'NONE',  ( -0.3725000000000000533, -0.6290000000000005587, 0.3724999999999999423 ) ) ;
#14902=DIRECTION ( 'NONE',  ( 0.7070715176384863021, 0.7070715176384774203, 0.009986885842351498482 ) ) ;
#14907=DIRECTION ( 'NONE',  ( 0.01412288512831213171, -3.675428035873182550E-19, 0.9999002670844991947 ) ) ;
#14909=CARTESIAN_POINT ( 'NONE',  ( 0.7856509485162611606, -0.4429999999999998939, -0.3627813902276396663 ) ) ;
#14910=LINE ( 'NONE', #10321, #10483 ) ;
#14913=CARTESIAN_POINT ( 'NONE',  ( 2.715114969687650870, 0.8546659208687416021, -0.4012693820656907939 ) ) ;
#14924=DIRECTION ( 'NONE',  ( -1.874307916738606601E-16, 1.000000000000000000, 0.000000000000000000 ) ) ;
#14927=DIRECTION ( 'NONE',  ( 0.000000000000000000, 0.000000000000000000, -1.000000000000000000 ) ) ;
#14936=CARTESIAN_POINT ( 'NONE',  ( 2.371787155501894784, 0.1852128444980909727, 0.4064941968476759038 ) ) ;
#14939=EDGE_CURVE ( 'NONE', #6203, #2093, #10677, .T. ) ;
#14940=CARTESIAN_POINT ( 'NONE',  ( 0.7095752389709895080, -0.4273810847934926826, -0.4705416541824789523 ) ) ;
#14942=DIRECTION ( 'NONE',  ( -1.874307916738608820E-16, 1.000000000000000000, 0.000000000000000000 ) ) ;
#14947=CARTESIAN_POINT ( 'NONE',  ( 0.6558077255084636681, -0.4243582046485735448, -0.5013227096633714464 ) ) ;
#14954=ORIENTED_EDGE ( 'NONE', *, *, #3371, .F. ) ;
#14956=ADVANCED_FACE ( 'NONE', ( #7661 ), #13532, .T. ) ;
#14961=DIRECTION ( 'NONE',  ( 0.9999002670844989726, 0.000000000000000000, 0.01412288512831212997 ) ) ;
#14967=CARTESIAN_POINT ( 'NONE',  ( 0.6782634401674636493, -0.01315021828653769632, -0.4690018541713429356 ) ) ;
#14972=ORIENTED_EDGE ( 'NONE', *, *, #14383, .F. ) ;
#14977=EDGE_CURVE ( 'NONE', #5232, #12211, #7656, .T. ) ;
#14991=DIRECTION ( 'NONE',  ( 1.000000000000000000, 0.000000000000000000, 0.000000000000000000 ) ) ;
#14998=CYLINDRICAL_SURFACE ( 'NONE', #14014, 0.03999999999999998002 ) ;
#15002=CARTESIAN_POINT ( 'NONE',  ( 3.112533253352848028, 0.6487563425743168022, -0.3962704070063717832 ) ) ;
#15006=CYLINDRICAL_SURFACE ( 'NONE', #11452, 0.05999999999999994227 ) ;
#15008=CARTESIAN_POINT ( 'NONE',  ( 0.7013557507355877574, -0.4108899945127513220, 0.4833783981792030837 ) ) ;
#15009=CARTESIAN_POINT ( 'NONE',  ( 0.6773491704061629370, -0.2214999999999999469, 0.5135154343835076629 ) ) ;
#15014=ADVANCED_FACE ( 'NONE', ( #9116 ), #753, .T. ) ;
#15019=CARTESIAN_POINT ( 'NONE',  ( 2.738128344600763597, 0.4573395005111794420, 0.4018406495282661473 ) ) ;
#15021=CARTESIAN_POINT ( 'NONE',  ( 0.8117875299037612402, -0.4418393224706574363, -0.4412646976173770774 ) ) ;
#15022=ADVANCED_FACE ( 'NONE', ( #4382 ), #6204, .F. ) ;
#15023=TOROIDAL_SURFACE ( 'NONE', #3793, 0.7173254825712083171, 0.05999999999999999778 ) ;
#15037=AXIS2_PLACEMENT_3D ( 'NONE', #3756, #12007, #8426 ) ;
#15040=CARTESIAN_POINT ( 'NONE',  ( 1.250000000000000000, -0.05999999999999979655, 0.4223386481965726857 ) ) ;
#15043=CARTESIAN_POINT ( 'NONE',  ( 0.6610203958102899291, 0.006418471913053761316, -0.4833908188384093974 ) ) ;
#15044=DIRECTION ( 'NONE',  ( 0.000000000000000000, 0.000000000000000000, -1.000000000000000000 ) ) ;
#15045=ADVANCED_FACE ( 'NONE', ( #10568 ), #14998, .F. ) ;
#15049=EDGE_CURVE ( 'NONE', #10543, #15127, #2554, .T. ) ;
#15052=ORIENTED_EDGE ( 'NONE', *, *, #13440, .F. ) ;
#15054=DIRECTION ( 'NONE',  ( -1.000000000000000000, -1.874307916738609066E-16, 0.000000000000000000 ) ) ;
#15069=EDGE_CURVE ( 'NONE', #12293, #10863, #6460, .T. ) ;
#15070=TOROIDAL_SURFACE ( 'NONE', #2372, 0.1150000000000000050, 0.04000000000000000083 ) ;
#15078=CARTESIAN_POINT ( 'NONE',  ( 0.6610344722576410037, 0.006457978392468126209, -0.4833528575413041928 ) ) ;
#15082=CARTESIAN_POINT ( 'NONE',  ( 3.045371920833404467, 0.6267721954701572784, -0.3972696057387546387 ) ) ;
#15083=DIRECTION ( 'NONE',  ( 0.000000000000000000, 0.000000000000000000, -1.000000000000000000 ) ) ;
#15084=FACE_OUTER_BOUND ( 'NONE', #9601, .T. ) ;
#15085=ORIENTED_EDGE ( 'NONE', *, *, #3996, .T. ) ;
#15087=CARTESIAN_POINT ( 'NONE',  ( 0.7513246802501652999, -0.4429999999999999494, 0.4293820849162024444 ) ) ;
#15089=CARTESIAN_POINT ( 'NONE',  ( 0.7251620530230687978, -0.2214999999999999469, 0.5497635826929317959 ) ) ;
#15091=FACE_OUTER_BOUND ( 'NONE', #2697, .T. ) ;
#15092=VERTEX_POINT ( 'NONE', #5750 ) ;
#15097=CARTESIAN_POINT ( 'NONE',  ( 1.254789639631328058, -0.3704945895125943411, -0.4822769824910831393 ) ) ;
#15108=EDGE_LOOP ( 'NONE', ( #1255, #12179, #5578, #9151 ) ) ;
#15114=CARTESIAN_POINT ( 'NONE',  ( 0.7176122613104025660, -0.008225492514568092176, -0.4611624156322176038 ) ) ;
#15117=CARTESIAN_POINT ( 'NONE',  ( 0.6552615383573133778, -0.03272338206886943324, -0.5074994761915084807 ) ) ;
#15118=DIRECTION ( 'NONE',  ( -0.7071067811865350272, 0.7071067811865600072, 0.000000000000000000 ) ) ;
#15122=EDGE_CURVE ( 'NONE', #2273, #12566, #7432, .T. ) ;
#15127=VERTEX_POINT ( 'NONE', #11489 ) ;
#15142=VECTOR ( 'NONE', #5381, 39.37007874015748143 ) ;
#15152=CARTESIAN_POINT ( 'NONE',  ( -0.7287617923574205570, 0.2159999999999999420, 0.4425000000000005596 ) ) ;
#15179=COLOUR_RGB('Sky Blue',0.24,0.69,0.87);
#15180=FILL_AREA_STYLE_COLOUR('',#15179);
#15181=FILL_AREA_STYLE('',(#15180));
#15182=SURFACE_STYLE_FILL_AREA(#15181);
#15183=SURFACE_SIDE_STYLE('',(#15182));
#15184=SURFACE_STYLE_USAGE(.BOTH.,#15183);
#15185=PRESENTATION_STYLE_ASSIGNMENT((#15184));
ENDSEC;
END-ISO-10303-21;
